ISO-10303-21;
HEADER;
/* Generated by software containing ST-Developer
 * from STEP Tools, Inc. (www.steptools.com) 
 */

FILE_DESCRIPTION(
/* description */ ('STEP AP203'),
/* implementation_level */ '2;1');

FILE_NAME(
/* name */ 'Corkscrew.step',
/* time_stamp */ '2026-11-08T21:40:52-08:00',
/* author */ (''),
/* organization */ (''),
/* preprocessor_version */ 'ST-DEVELOPER v20.2',
/* originating_system */ 'Autodesk Translation Framework v15.17.0.0',
/* authorisation */ '');

FILE_SCHEMA (('AUTOMOTIVE_DESIGN { 1 0 10303 214 3 1 1 }'));
ENDSEC;

DATA;
#10=MECHANICAL_DESIGN_GEOMETRIC_PRESENTATION_REPRESENTATION('',(#189),#12137);
#11=(
BOUNDED_CURVE()
B_SPLINE_CURVE(2,(#7724,#7725,#7726,#7727,#7728,#7729,#7730,#7731,#7732,
#7733,#7734,#7735,#7736,#7737,#7738,#7739,#7740,#7741,#7742,#7743,#7744,
#7745,#7746,#7747,#7748,#7749,#7750,#7751,#7752,#7753,#7754,#7755,#7756,
#7757,#7758,#7759,#7760,#7761,#7762,#7763,#7764,#7765,#7766,#7767,#7768,
#7769,#7770,#7771,#7772,#7773,#7774,#7775,#7776,#7777,#7778,#7779,#7780,
#7781,#7782,#7783,#7784,#7785,#7786,#7787,#7788,#7789,#7790,#7791,#7792,
#7793,#7794,#7795,#7796,#7797,#7798,#7799,#7800,#7801,#7802,#7803,#7804,
#7805,#7806,#7807,#7808,#7809,#7810,#7811,#7812,#7813,#7814,#7815,#7816,
#7817,#7818,#7819,#7820,#7821,#7822,#7823,#7824,#7825,#7826,#7827,#7828,
#7829,#7830,#7831,#7832,#7833,#7834,#7835,#7836,#7837,#7838,#7839,#7840,
#7841,#7842,#7843,#7844,#7845,#7846,#7847,#7848,#7849,#7850,#7851,#7852,
#7853,#7854,#7855,#7856,#7857,#7858,#7859,#7860,#7861,#7862,#7863,#7864,
#7865,#7866,#7867,#7868,#7869,#7870,#7871,#7872,#7873,#7874,#7875,#7876,
#7877,#7878,#7879,#7880,#7881,#7882,#7883,#7884,#7885,#7886,#7887,#7888,
#7889,#7890,#7891,#7892,#7893,#7894,#7895,#7896,#7897,#7898,#7899,#7900,
#7901,#7902,#7903,#7904,#7905,#7906,#7907,#7908,#7909,#7910,#7911,#7912,
#7913,#7914,#7915,#7916),.UNSPECIFIED.,.F.,.F.)
B_SPLINE_CURVE_WITH_KNOTS((3,2,2,2,2,2,2,2,2,2,2,2,2,2,2,2,2,2,2,2,2,2,
2,2,2,2,2,2,2,2,2,2,2,2,2,2,2,2,2,2,2,2,2,2,2,2,2,2,2,2,2,2,2,2,2,2,2,2,
2,2,2,2,2,2,2,2,2,2,2,2,2,2,2,2,2,2,2,2,2,2,2,2,2,2,2,2,2,2,2,2,2,2,2,2,
2,2,3),(0.,0.0104166666666667,0.0208333333333333,0.03125,0.0416666666666667,
0.0520833333333333,0.0625,0.0729166666666667,0.0833333333333333,0.09375,
0.104166666666667,0.114583333333333,0.125,0.135416666666667,0.145833333333333,
0.15625,0.166666666666667,0.177083333333333,0.1875,0.197916666666667,0.208333333333333,
0.21875,0.229166666666667,0.239583333333333,0.25,0.260416666666667,0.270833333333333,
0.28125,0.291666666666667,0.302083333333333,0.3125,0.322916666666667,0.333333333333333,
0.34375,0.354166666666667,0.364583333333333,0.375,0.385416666666667,0.395833333333333,
0.40625,0.416666666666667,0.427083333333333,0.4375,0.447916666666667,0.458333333333333,
0.46875,0.479166666666667,0.489583333333333,0.5,0.510416666666667,0.520833333333333,
0.53125,0.541666666666667,0.552083333333333,0.5625,0.572916666666667,0.583333333333333,
0.59375,0.604166666666667,0.614583333333333,0.625,0.635416666666667,0.645833333333333,
0.65625,0.666666666666667,0.677083333333333,0.6875,0.697916666666667,0.708333333333333,
0.71875,0.729166666666667,0.739583333333333,0.75,0.760416666666667,0.770833333333333,
0.78125,0.791666666666667,0.802083333333333,0.8125,0.822916666666667,0.833333333333333,
0.84375,0.854166666666667,0.864583333333333,0.875,0.885416666666667,0.895833333333333,
0.90625,0.916666666666667,0.927083333333333,0.9375,0.947916666666667,0.958333333333333,
0.96875,0.979166666666667,0.989583333333333,1.),.UNSPECIFIED.)
CURVE()
GEOMETRIC_REPRESENTATION_ITEM()
RATIONAL_B_SPLINE_CURVE((1.,0.965925826289068,1.,0.965925826289068,1.,0.965925826289068,
1.,0.965925826289068,1.,0.965925826289068,1.,0.965925826289068,1.,0.965925826289068,
1.,0.965925826289068,1.,0.965925826289068,1.,0.965925826289068,1.,0.965925826289068,
1.,0.965925826289068,1.,0.965925826289068,1.,0.965925826289068,1.,0.965925826289068,
1.,0.965925826289068,1.,0.965925826289068,1.,0.965925826289068,1.,0.965925826289068,
1.,0.965925826289068,1.,0.965925826289068,1.,0.965925826289068,1.,0.965925826289068,
1.,0.965925826289068,1.,0.965925826289068,1.,0.965925826289068,1.,0.965925826289068,
1.,0.965925826289068,1.,0.965925826289068,1.,0.965925826289068,1.,0.965925826289068,
1.,0.965925826289068,1.,0.965925826289068,1.,0.965925826289068,1.,0.965925826289068,
1.,0.965925826289068,1.,0.965925826289068,1.,0.965925826289068,1.,0.965925826289068,
1.,0.965925826289068,1.,0.965925826289068,1.,0.965925826289068,1.,0.965925826289068,
1.,0.965925826289068,1.,0.965925826289068,1.,0.965925826289068,1.,0.965925826289068,
1.,0.965925826289068,1.,0.965925826289068,1.,0.965925826289068,1.,0.965925826289068,
1.,0.965925826289068,1.,0.965925826289068,1.,0.965925826289068,1.,0.965925826289068,
1.,0.965925826289068,1.,0.965925826289068,1.,0.965925826289068,1.,0.965925826289068,
1.,0.965925826289068,1.,0.965925826289068,1.,0.965925826289068,1.,0.965925826289068,
1.,0.965925826289068,1.,0.965925826289068,1.,0.965925826289068,1.,0.965925826289068,
1.,0.965925826289068,1.,0.965925826289068,1.,0.965925826289068,1.,0.965925826289068,
1.,0.965925826289068,1.,0.965925826289068,1.,0.965925826289068,1.,0.965925826289068,
1.,0.965925826289068,1.,0.965925826289068,1.,0.965925826289068,1.,0.965925826289068,
1.,0.965925826289068,1.,0.965925826289068,1.,0.965925826289068,1.,0.965925826289068,
1.,0.965925826289068,1.,0.965925826289068,1.,0.965925826289068,1.,0.965925826289068,
1.,0.965925826289068,1.,0.965925826289068,1.,0.965925826289068,1.,0.965925826289068,
1.,0.965925826289068,1.,0.965925826289068,1.,0.965925826289068,1.,0.965925826289068,
1.,0.965925826289068,1.))
REPRESENTATION_ITEM('')
);
#12=ELLIPSE('',#2055,0.25726333794061,0.250455511407675);
#13=ELLIPSE('',#2061,0.325552151697954,0.297562874271256);
#14=ELLIPSE('',#2064,0.257263338177418,0.250455511570592);
#15=(
BOUNDED_SURFACE()
B_SPLINE_SURFACE(3,3,((#5281,#5282,#5283,#5284,#5285,#5286,#5287,#5288,
#5289,#5290,#5291,#5292),(#5293,#5294,#5295,#5296,#5297,#5298,#5299,#5300,
#5301,#5302,#5303,#5304),(#5305,#5306,#5307,#5308,#5309,#5310,#5311,#5312,
#5313,#5314,#5315,#5316),(#5317,#5318,#5319,#5320,#5321,#5322,#5323,#5324,
#5325,#5326,#5327,#5328),(#5329,#5330,#5331,#5332,#5333,#5334,#5335,#5336,
#5337,#5338,#5339,#5340),(#5341,#5342,#5343,#5344,#5345,#5346,#5347,#5348,
#5349,#5350,#5351,#5352),(#5353,#5354,#5355,#5356,#5357,#5358,#5359,#5360,
#5361,#5362,#5363,#5364)),.UNSPECIFIED.,.T.,.F.,.F.)
B_SPLINE_SURFACE_WITH_KNOTS((4,3,4),(4,2,2,2,2,4),(0.,0.5,1.),(0.727251200985696,
0.761344800862484,0.795438400739272,0.863625600492848,0.931812800246424,
1.),.UNSPECIFIED.)
GEOMETRIC_REPRESENTATION_ITEM()
RATIONAL_B_SPLINE_SURFACE(((1.,1.,1.,1.,1.,1.,1.,1.,1.,1.,1.,1.),(0.333333333333333,
0.333333333333333,0.333333333333333,0.333333333333333,0.333333333333333,
0.333333333333333,0.333333333333333,0.333333333333333,0.333333333333333,
0.333333333333333,0.333333333333333,0.333333333333333),(0.333333333333333,
0.333333333333333,0.333333333333333,0.333333333333333,0.333333333333333,
0.333333333333333,0.333333333333333,0.333333333333333,0.333333333333333,
0.333333333333333,0.333333333333333,0.333333333333333),(1.,1.,1.,1.,1.,
1.,1.,1.,1.,1.,1.,1.),(0.333333333333333,0.333333333333333,0.333333333333333,
0.333333333333333,0.333333333333333,0.333333333333333,0.333333333333333,
0.333333333333333,0.333333333333333,0.333333333333333,0.333333333333333,
0.333333333333333),(0.333333333333333,0.333333333333333,0.333333333333333,
0.333333333333333,0.333333333333333,0.333333333333333,0.333333333333333,
0.333333333333333,0.333333333333333,0.333333333333333,0.333333333333333,
0.333333333333333),(1.,1.,1.,1.,1.,1.,1.,1.,1.,1.,1.,1.)))
REPRESENTATION_ITEM('')
SURFACE()
);
#16=(
BOUNDED_SURFACE()
B_SPLINE_SURFACE(3,3,((#5394,#5395,#5396,#5397,#5398,#5399,#5400,#5401,
#5402,#5403,#5404,#5405,#5406,#5407,#5408,#5409,#5410,#5411,#5412,#5413,
#5414,#5415,#5416,#5417,#5418,#5419,#5420,#5421,#5422,#5423,#5424,#5425,
#5426,#5427,#5428,#5429,#5430,#5431,#5432,#5433),(#5434,#5435,#5436,#5437,
#5438,#5439,#5440,#5441,#5442,#5443,#5444,#5445,#5446,#5447,#5448,#5449,
#5450,#5451,#5452,#5453,#5454,#5455,#5456,#5457,#5458,#5459,#5460,#5461,
#5462,#5463,#5464,#5465,#5466,#5467,#5468,#5469,#5470,#5471,#5472,#5473),
(#5474,#5475,#5476,#5477,#5478,#5479,#5480,#5481,#5482,#5483,#5484,#5485,
#5486,#5487,#5488,#5489,#5490,#5491,#5492,#5493,#5494,#5495,#5496,#5497,
#5498,#5499,#5500,#5501,#5502,#5503,#5504,#5505,#5506,#5507,#5508,#5509,
#5510,#5511,#5512,#5513),(#5514,#5515,#5516,#5517,#5518,#5519,#5520,#5521,
#5522,#5523,#5524,#5525,#5526,#5527,#5528,#5529,#5530,#5531,#5532,#5533,
#5534,#5535,#5536,#5537,#5538,#5539,#5540,#5541,#5542,#5543,#5544,#5545,
#5546,#5547,#5548,#5549,#5550,#5551,#5552,#5553),(#5554,#5555,#5556,#5557,
#5558,#5559,#5560,#5561,#5562,#5563,#5564,#5565,#5566,#5567,#5568,#5569,
#5570,#5571,#5572,#5573,#5574,#5575,#5576,#5577,#5578,#5579,#5580,#5581,
#5582,#5583,#5584,#5585,#5586,#5587,#5588,#5589,#5590,#5591,#5592,#5593),
(#5594,#5595,#5596,#5597,#5598,#5599,#5600,#5601,#5602,#5603,#5604,#5605,
#5606,#5607,#5608,#5609,#5610,#5611,#5612,#5613,#5614,#5615,#5616,#5617,
#5618,#5619,#5620,#5621,#5622,#5623,#5624,#5625,#5626,#5627,#5628,#5629,
#5630,#5631,#5632,#5633),(#5634,#5635,#5636,#5637,#5638,#5639,#5640,#5641,
#5642,#5643,#5644,#5645,#5646,#5647,#5648,#5649,#5650,#5651,#5652,#5653,
#5654,#5655,#5656,#5657,#5658,#5659,#5660,#5661,#5662,#5663,#5664,#5665,
#5666,#5667,#5668,#5669,#5670,#5671,#5672,#5673)),.UNSPECIFIED.,.T.,.F.,
 .F.)
B_SPLINE_SURFACE_WITH_KNOTS((4,3,4),(4,2,2,2,2,2,2,2,2,2,2,2,2,2,2,2,2,
2,2,4),(0.,0.5,1.),(0.,0.0437517296050676,0.0875034592101352,0.131255188815203,
0.17500691842027,0.196882783222804,0.218758648025338,0.262510377630406,
0.350013836840541,0.418185084306465,0.486356331772389,0.554527579238313,
0.622698826704237,0.669861473366207,0.717024120028178,0.811349413352118,
0.858512060014089,0.905674706676059,0.95283735333803,1.),.UNSPECIFIED.)
GEOMETRIC_REPRESENTATION_ITEM()
RATIONAL_B_SPLINE_SURFACE(((1.,1.,1.,1.,1.,1.,1.,1.,1.,1.,1.,1.,1.,1.,1.,
1.,1.,1.,1.,1.,1.,1.,1.,1.,1.,1.,1.,1.,1.,1.,1.,1.,1.,1.,1.,1.,1.,1.,1.,
1.),(0.333333333333333,0.333333333333333,0.333333333333333,0.333333333333333,
0.333333333333333,0.333333333333333,0.333333333333333,0.333333333333333,
0.333333333333333,0.333333333333333,0.333333333333333,0.333333333333333,
0.333333333333333,0.333333333333333,0.333333333333333,0.333333333333333,
0.333333333333333,0.333333333333333,0.333333333333333,0.333333333333333,
0.333333333333333,0.333333333333333,0.333333333333333,0.333333333333333,
0.333333333333333,0.333333333333333,0.333333333333333,0.333333333333333,
0.333333333333333,0.333333333333333,0.333333333333333,0.333333333333333,
0.333333333333333,0.333333333333333,0.333333333333333,0.333333333333333,
0.333333333333333,0.333333333333333,0.333333333333333,0.333333333333333),
(0.333333333333333,0.333333333333333,0.333333333333333,0.333333333333333,
0.333333333333333,0.333333333333333,0.333333333333333,0.333333333333333,
0.333333333333333,0.333333333333333,0.333333333333333,0.333333333333333,
0.333333333333333,0.333333333333333,0.333333333333333,0.333333333333333,
0.333333333333333,0.333333333333333,0.333333333333333,0.333333333333333,
0.333333333333333,0.333333333333333,0.333333333333333,0.333333333333333,
0.333333333333333,0.333333333333333,0.333333333333333,0.333333333333333,
0.333333333333333,0.333333333333333,0.333333333333333,0.333333333333333,
0.333333333333333,0.333333333333333,0.333333333333333,0.333333333333333,
0.333333333333333,0.333333333333333,0.333333333333333,0.333333333333333),
(1.,1.,1.,1.,1.,1.,1.,1.,1.,1.,1.,1.,1.,1.,1.,1.,1.,1.,1.,1.,1.,1.,1.,1.,
1.,1.,1.,1.,1.,1.,1.,1.,1.,1.,1.,1.,1.,1.,1.,1.),(0.333333333333333,0.333333333333333,
0.333333333333333,0.333333333333333,0.333333333333333,0.333333333333333,
0.333333333333333,0.333333333333333,0.333333333333333,0.333333333333333,
0.333333333333333,0.333333333333333,0.333333333333333,0.333333333333333,
0.333333333333333,0.333333333333333,0.333333333333333,0.333333333333333,
0.333333333333333,0.333333333333333,0.333333333333333,0.333333333333333,
0.333333333333333,0.333333333333333,0.333333333333333,0.333333333333333,
0.333333333333333,0.333333333333333,0.333333333333333,0.333333333333333,
0.333333333333333,0.333333333333333,0.333333333333333,0.333333333333333,
0.333333333333333,0.333333333333333,0.333333333333333,0.333333333333333,
0.333333333333333,0.333333333333333),(0.333333333333333,0.333333333333333,
0.333333333333333,0.333333333333333,0.333333333333333,0.333333333333333,
0.333333333333333,0.333333333333333,0.333333333333333,0.333333333333333,
0.333333333333333,0.333333333333333,0.333333333333333,0.333333333333333,
0.333333333333333,0.333333333333333,0.333333333333333,0.333333333333333,
0.333333333333333,0.333333333333333,0.333333333333333,0.333333333333333,
0.333333333333333,0.333333333333333,0.333333333333333,0.333333333333333,
0.333333333333333,0.333333333333333,0.333333333333333,0.333333333333333,
0.333333333333333,0.333333333333333,0.333333333333333,0.333333333333333,
0.333333333333333,0.333333333333333,0.333333333333333,0.333333333333333,
0.333333333333333,0.333333333333333),(1.,1.,1.,1.,1.,1.,1.,1.,1.,1.,1.,
1.,1.,1.,1.,1.,1.,1.,1.,1.,1.,1.,1.,1.,1.,1.,1.,1.,1.,1.,1.,1.,1.,1.,1.,
1.,1.,1.,1.,1.)))
REPRESENTATION_ITEM('')
SURFACE()
);
#17=(
BOUNDED_SURFACE()
B_SPLINE_SURFACE(3,2,((#5791,#5792,#5793,#5794,#5795,#5796,#5797,#5798,
#5799,#5800,#5801,#5802,#5803,#5804,#5805,#5806,#5807,#5808,#5809,#5810,
#5811,#5812,#5813,#5814,#5815,#5816,#5817,#5818,#5819,#5820,#5821,#5822,
#5823,#5824,#5825,#5826,#5827,#5828,#5829,#5830,#5831,#5832,#5833,#5834,
#5835,#5836,#5837,#5838,#5839,#5840,#5841,#5842,#5843,#5844,#5845,#5846,
#5847,#5848,#5849,#5850,#5851,#5852,#5853,#5854,#5855,#5856,#5857,#5858,
#5859,#5860,#5861,#5862,#5863,#5864,#5865,#5866,#5867,#5868,#5869,#5870,
#5871,#5872,#5873,#5874,#5875,#5876,#5877,#5878,#5879,#5880,#5881,#5882,
#5883,#5884,#5885,#5886,#5887,#5888,#5889,#5890,#5891,#5892,#5893,#5894,
#5895,#5896,#5897,#5898,#5899,#5900,#5901,#5902,#5903,#5904,#5905,#5906,
#5907,#5908,#5909,#5910,#5911,#5912,#5913,#5914,#5915,#5916,#5917,#5918,
#5919,#5920,#5921,#5922,#5923,#5924,#5925,#5926,#5927,#5928,#5929,#5930,
#5931,#5932,#5933,#5934,#5935,#5936,#5937,#5938,#5939,#5940,#5941,#5942,
#5943,#5944,#5945,#5946,#5947,#5948,#5949,#5950,#5951,#5952,#5953,#5954,
#5955,#5956,#5957,#5958,#5959,#5960,#5961,#5962,#5963,#5964,#5965,#5966,
#5967,#5968,#5969,#5970,#5971,#5972,#5973,#5974,#5975,#5976,#5977,#5978,
#5979,#5980,#5981,#5982,#5983),(#5984,#5985,#5986,#5987,#5988,#5989,#5990,
#5991,#5992,#5993,#5994,#5995,#5996,#5997,#5998,#5999,#6000,#6001,#6002,
#6003,#6004,#6005,#6006,#6007,#6008,#6009,#6010,#6011,#6012,#6013,#6014,
#6015,#6016,#6017,#6018,#6019,#6020,#6021,#6022,#6023,#6024,#6025,#6026,
#6027,#6028,#6029,#6030,#6031,#6032,#6033,#6034,#6035,#6036,#6037,#6038,
#6039,#6040,#6041,#6042,#6043,#6044,#6045,#6046,#6047,#6048,#6049,#6050,
#6051,#6052,#6053,#6054,#6055,#6056,#6057,#6058,#6059,#6060,#6061,#6062,
#6063,#6064,#6065,#6066,#6067,#6068,#6069,#6070,#6071,#6072,#6073,#6074,
#6075,#6076,#6077,#6078,#6079,#6080,#6081,#6082,#6083,#6084,#6085,#6086,
#6087,#6088,#6089,#6090,#6091,#6092,#6093,#6094,#6095,#6096,#6097,#6098,
#6099,#6100,#6101,#6102,#6103,#6104,#6105,#6106,#6107,#6108,#6109,#6110,
#6111,#6112,#6113,#6114,#6115,#6116,#6117,#6118,#6119,#6120,#6121,#6122,
#6123,#6124,#6125,#6126,#6127,#6128,#6129,#6130,#6131,#6132,#6133,#6134,
#6135,#6136,#6137,#6138,#6139,#6140,#6141,#6142,#6143,#6144,#6145,#6146,
#6147,#6148,#6149,#6150,#6151,#6152,#6153,#6154,#6155,#6156,#6157,#6158,
#6159,#6160,#6161,#6162,#6163,#6164,#6165,#6166,#6167,#6168,#6169,#6170,
#6171,#6172,#6173,#6174,#6175,#6176),(#6177,#6178,#6179,#6180,#6181,#6182,
#6183,#6184,#6185,#6186,#6187,#6188,#6189,#6190,#6191,#6192,#6193,#6194,
#6195,#6196,#6197,#6198,#6199,#6200,#6201,#6202,#6203,#6204,#6205,#6206,
#6207,#6208,#6209,#6210,#6211,#6212,#6213,#6214,#6215,#6216,#6217,#6218,
#6219,#6220,#6221,#6222,#6223,#6224,#6225,#6226,#6227,#6228,#6229,#6230,
#6231,#6232,#6233,#6234,#6235,#6236,#6237,#6238,#6239,#6240,#6241,#6242,
#6243,#6244,#6245,#6246,#6247,#6248,#6249,#6250,#6251,#6252,#6253,#6254,
#6255,#6256,#6257,#6258,#6259,#6260,#6261,#6262,#6263,#6264,#6265,#6266,
#6267,#6268,#6269,#6270,#6271,#6272,#6273,#6274,#6275,#6276,#6277,#6278,
#6279,#6280,#6281,#6282,#6283,#6284,#6285,#6286,#6287,#6288,#6289,#6290,
#6291,#6292,#6293,#6294,#6295,#6296,#6297,#6298,#6299,#6300,#6301,#6302,
#6303,#6304,#6305,#6306,#6307,#6308,#6309,#6310,#6311,#6312,#6313,#6314,
#6315,#6316,#6317,#6318,#6319,#6320,#6321,#6322,#6323,#6324,#6325,#6326,
#6327,#6328,#6329,#6330,#6331,#6332,#6333,#6334,#6335,#6336,#6337,#6338,
#6339,#6340,#6341,#6342,#6343,#6344,#6345,#6346,#6347,#6348,#6349,#6350,
#6351,#6352,#6353,#6354,#6355,#6356,#6357,#6358,#6359,#6360,#6361,#6362,
#6363,#6364,#6365,#6366,#6367,#6368,#6369),(#6370,#6371,#6372,#6373,#6374,
#6375,#6376,#6377,#6378,#6379,#6380,#6381,#6382,#6383,#6384,#6385,#6386,
#6387,#6388,#6389,#6390,#6391,#6392,#6393,#6394,#6395,#6396,#6397,#6398,
#6399,#6400,#6401,#6402,#6403,#6404,#6405,#6406,#6407,#6408,#6409,#6410,
#6411,#6412,#6413,#6414,#6415,#6416,#6417,#6418,#6419,#6420,#6421,#6422,
#6423,#6424,#6425,#6426,#6427,#6428,#6429,#6430,#6431,#6432,#6433,#6434,
#6435,#6436,#6437,#6438,#6439,#6440,#6441,#6442,#6443,#6444,#6445,#6446,
#6447,#6448,#6449,#6450,#6451,#6452,#6453,#6454,#6455,#6456,#6457,#6458,
#6459,#6460,#6461,#6462,#6463,#6464,#6465,#6466,#6467,#6468,#6469,#6470,
#6471,#6472,#6473,#6474,#6475,#6476,#6477,#6478,#6479,#6480,#6481,#6482,
#6483,#6484,#6485,#6486,#6487,#6488,#6489,#6490,#6491,#6492,#6493,#6494,
#6495,#6496,#6497,#6498,#6499,#6500,#6501,#6502,#6503,#6504,#6505,#6506,
#6507,#6508,#6509,#6510,#6511,#6512,#6513,#6514,#6515,#6516,#6517,#6518,
#6519,#6520,#6521,#6522,#6523,#6524,#6525,#6526,#6527,#6528,#6529,#6530,
#6531,#6532,#6533,#6534,#6535,#6536,#6537,#6538,#6539,#6540,#6541,#6542,
#6543,#6544,#6545,#6546,#6547,#6548,#6549,#6550,#6551,#6552,#6553,#6554,
#6555,#6556,#6557,#6558,#6559,#6560,#6561,#6562),(#6563,#6564,#6565,#6566,
#6567,#6568,#6569,#6570,#6571,#6572,#6573,#6574,#6575,#6576,#6577,#6578,
#6579,#6580,#6581,#6582,#6583,#6584,#6585,#6586,#6587,#6588,#6589,#6590,
#6591,#6592,#6593,#6594,#6595,#6596,#6597,#6598,#6599,#6600,#6601,#6602,
#6603,#6604,#6605,#6606,#6607,#6608,#6609,#6610,#6611,#6612,#6613,#6614,
#6615,#6616,#6617,#6618,#6619,#6620,#6621,#6622,#6623,#6624,#6625,#6626,
#6627,#6628,#6629,#6630,#6631,#6632,#6633,#6634,#6635,#6636,#6637,#6638,
#6639,#6640,#6641,#6642,#6643,#6644,#6645,#6646,#6647,#6648,#6649,#6650,
#6651,#6652,#6653,#6654,#6655,#6656,#6657,#6658,#6659,#6660,#6661,#6662,
#6663,#6664,#6665,#6666,#6667,#6668,#6669,#6670,#6671,#6672,#6673,#6674,
#6675,#6676,#6677,#6678,#6679,#6680,#6681,#6682,#6683,#6684,#6685,#6686,
#6687,#6688,#6689,#6690,#6691,#6692,#6693,#6694,#6695,#6696,#6697,#6698,
#6699,#6700,#6701,#6702,#6703,#6704,#6705,#6706,#6707,#6708,#6709,#6710,
#6711,#6712,#6713,#6714,#6715,#6716,#6717,#6718,#6719,#6720,#6721,#6722,
#6723,#6724,#6725,#6726,#6727,#6728,#6729,#6730,#6731,#6732,#6733,#6734,
#6735,#6736,#6737,#6738,#6739,#6740,#6741,#6742,#6743,#6744,#6745,#6746,
#6747,#6748,#6749,#6750,#6751,#6752,#6753,#6754,#6755),(#6756,#6757,#6758,
#6759,#6760,#6761,#6762,#6763,#6764,#6765,#6766,#6767,#6768,#6769,#6770,
#6771,#6772,#6773,#6774,#6775,#6776,#6777,#6778,#6779,#6780,#6781,#6782,
#6783,#6784,#6785,#6786,#6787,#6788,#6789,#6790,#6791,#6792,#6793,#6794,
#6795,#6796,#6797,#6798,#6799,#6800,#6801,#6802,#6803,#6804,#6805,#6806,
#6807,#6808,#6809,#6810,#6811,#6812,#6813,#6814,#6815,#6816,#6817,#6818,
#6819,#6820,#6821,#6822,#6823,#6824,#6825,#6826,#6827,#6828,#6829,#6830,
#6831,#6832,#6833,#6834,#6835,#6836,#6837,#6838,#6839,#6840,#6841,#6842,
#6843,#6844,#6845,#6846,#6847,#6848,#6849,#6850,#6851,#6852,#6853,#6854,
#6855,#6856,#6857,#6858,#6859,#6860,#6861,#6862,#6863,#6864,#6865,#6866,
#6867,#6868,#6869,#6870,#6871,#6872,#6873,#6874,#6875,#6876,#6877,#6878,
#6879,#6880,#6881,#6882,#6883,#6884,#6885,#6886,#6887,#6888,#6889,#6890,
#6891,#6892,#6893,#6894,#6895,#6896,#6897,#6898,#6899,#6900,#6901,#6902,
#6903,#6904,#6905,#6906,#6907,#6908,#6909,#6910,#6911,#6912,#6913,#6914,
#6915,#6916,#6917,#6918,#6919,#6920,#6921,#6922,#6923,#6924,#6925,#6926,
#6927,#6928,#6929,#6930,#6931,#6932,#6933,#6934,#6935,#6936,#6937,#6938,
#6939,#6940,#6941,#6942,#6943,#6944,#6945,#6946,#6947,#6948),(#6949,#6950,
#6951,#6952,#6953,#6954,#6955,#6956,#6957,#6958,#6959,#6960,#6961,#6962,
#6963,#6964,#6965,#6966,#6967,#6968,#6969,#6970,#6971,#6972,#6973,#6974,
#6975,#6976,#6977,#6978,#6979,#6980,#6981,#6982,#6983,#6984,#6985,#6986,
#6987,#6988,#6989,#6990,#6991,#6992,#6993,#6994,#6995,#6996,#6997,#6998,
#6999,#7000,#7001,#7002,#7003,#7004,#7005,#7006,#7007,#7008,#7009,#7010,
#7011,#7012,#7013,#7014,#7015,#7016,#7017,#7018,#7019,#7020,#7021,#7022,
#7023,#7024,#7025,#7026,#7027,#7028,#7029,#7030,#7031,#7032,#7033,#7034,
#7035,#7036,#7037,#7038,#7039,#7040,#7041,#7042,#7043,#7044,#7045,#7046,
#7047,#7048,#7049,#7050,#7051,#7052,#7053,#7054,#7055,#7056,#7057,#7058,
#7059,#7060,#7061,#7062,#7063,#7064,#7065,#7066,#7067,#7068,#7069,#7070,
#7071,#7072,#7073,#7074,#7075,#7076,#7077,#7078,#7079,#7080,#7081,#7082,
#7083,#7084,#7085,#7086,#7087,#7088,#7089,#7090,#7091,#7092,#7093,#7094,
#7095,#7096,#7097,#7098,#7099,#7100,#7101,#7102,#7103,#7104,#7105,#7106,
#7107,#7108,#7109,#7110,#7111,#7112,#7113,#7114,#7115,#7116,#7117,#7118,
#7119,#7120,#7121,#7122,#7123,#7124,#7125,#7126,#7127,#7128,#7129,#7130,
#7131,#7132,#7133,#7134,#7135,#7136,#7137,#7138,#7139,#7140,#7141),(#7142,
#7143,#7144,#7145,#7146,#7147,#7148,#7149,#7150,#7151,#7152,#7153,#7154,
#7155,#7156,#7157,#7158,#7159,#7160,#7161,#7162,#7163,#7164,#7165,#7166,
#7167,#7168,#7169,#7170,#7171,#7172,#7173,#7174,#7175,#7176,#7177,#7178,
#7179,#7180,#7181,#7182,#7183,#7184,#7185,#7186,#7187,#7188,#7189,#7190,
#7191,#7192,#7193,#7194,#7195,#7196,#7197,#7198,#7199,#7200,#7201,#7202,
#7203,#7204,#7205,#7206,#7207,#7208,#7209,#7210,#7211,#7212,#7213,#7214,
#7215,#7216,#7217,#7218,#7219,#7220,#7221,#7222,#7223,#7224,#7225,#7226,
#7227,#7228,#7229,#7230,#7231,#7232,#7233,#7234,#7235,#7236,#7237,#7238,
#7239,#7240,#7241,#7242,#7243,#7244,#7245,#7246,#7247,#7248,#7249,#7250,
#7251,#7252,#7253,#7254,#7255,#7256,#7257,#7258,#7259,#7260,#7261,#7262,
#7263,#7264,#7265,#7266,#7267,#7268,#7269,#7270,#7271,#7272,#7273,#7274,
#7275,#7276,#7277,#7278,#7279,#7280,#7281,#7282,#7283,#7284,#7285,#7286,
#7287,#7288,#7289,#7290,#7291,#7292,#7293,#7294,#7295,#7296,#7297,#7298,
#7299,#7300,#7301,#7302,#7303,#7304,#7305,#7306,#7307,#7308,#7309,#7310,
#7311,#7312,#7313,#7314,#7315,#7316,#7317,#7318,#7319,#7320,#7321,#7322,
#7323,#7324,#7325,#7326,#7327,#7328,#7329,#7330,#7331,#7332,#7333,#7334),
(#7335,#7336,#7337,#7338,#7339,#7340,#7341,#7342,#7343,#7344,#7345,#7346,
#7347,#7348,#7349,#7350,#7351,#7352,#7353,#7354,#7355,#7356,#7357,#7358,
#7359,#7360,#7361,#7362,#7363,#7364,#7365,#7366,#7367,#7368,#7369,#7370,
#7371,#7372,#7373,#7374,#7375,#7376,#7377,#7378,#7379,#7380,#7381,#7382,
#7383,#7384,#7385,#7386,#7387,#7388,#7389,#7390,#7391,#7392,#7393,#7394,
#7395,#7396,#7397,#7398,#7399,#7400,#7401,#7402,#7403,#7404,#7405,#7406,
#7407,#7408,#7409,#7410,#7411,#7412,#7413,#7414,#7415,#7416,#7417,#7418,
#7419,#7420,#7421,#7422,#7423,#7424,#7425,#7426,#7427,#7428,#7429,#7430,
#7431,#7432,#7433,#7434,#7435,#7436,#7437,#7438,#7439,#7440,#7441,#7442,
#7443,#7444,#7445,#7446,#7447,#7448,#7449,#7450,#7451,#7452,#7453,#7454,
#7455,#7456,#7457,#7458,#7459,#7460,#7461,#7462,#7463,#7464,#7465,#7466,
#7467,#7468,#7469,#7470,#7471,#7472,#7473,#7474,#7475,#7476,#7477,#7478,
#7479,#7480,#7481,#7482,#7483,#7484,#7485,#7486,#7487,#7488,#7489,#7490,
#7491,#7492,#7493,#7494,#7495,#7496,#7497,#7498,#7499,#7500,#7501,#7502,
#7503,#7504,#7505,#7506,#7507,#7508,#7509,#7510,#7511,#7512,#7513,#7514,
#7515,#7516,#7517,#7518,#7519,#7520,#7521,#7522,#7523,#7524,#7525,#7526,
#7527),(#7528,#7529,#7530,#7531,#7532,#7533,#7534,#7535,#7536,#7537,#7538,
#7539,#7540,#7541,#7542,#7543,#7544,#7545,#7546,#7547,#7548,#7549,#7550,
#7551,#7552,#7553,#7554,#7555,#7556,#7557,#7558,#7559,#7560,#7561,#7562,
#7563,#7564,#7565,#7566,#7567,#7568,#7569,#7570,#7571,#7572,#7573,#7574,
#7575,#7576,#7577,#7578,#7579,#7580,#7581,#7582,#7583,#7584,#7585,#7586,
#7587,#7588,#7589,#7590,#7591,#7592,#7593,#7594,#7595,#7596,#7597,#7598,
#7599,#7600,#7601,#7602,#7603,#7604,#7605,#7606,#7607,#7608,#7609,#7610,
#7611,#7612,#7613,#7614,#7615,#7616,#7617,#7618,#7619,#7620,#7621,#7622,
#7623,#7624,#7625,#7626,#7627,#7628,#7629,#7630,#7631,#7632,#7633,#7634,
#7635,#7636,#7637,#7638,#7639,#7640,#7641,#7642,#7643,#7644,#7645,#7646,
#7647,#7648,#7649,#7650,#7651,#7652,#7653,#7654,#7655,#7656,#7657,#7658,
#7659,#7660,#7661,#7662,#7663,#7664,#7665,#7666,#7667,#7668,#7669,#7670,
#7671,#7672,#7673,#7674,#7675,#7676,#7677,#7678,#7679,#7680,#7681,#7682,
#7683,#7684,#7685,#7686,#7687,#7688,#7689,#7690,#7691,#7692,#7693,#7694,
#7695,#7696,#7697,#7698,#7699,#7700,#7701,#7702,#7703,#7704,#7705,#7706,
#7707,#7708,#7709,#7710,#7711,#7712,#7713,#7714,#7715,#7716,#7717,#7718,
#7719,#7720)),.UNSPECIFIED.,.T.,.F.,.F.)
B_SPLINE_SURFACE_WITH_KNOTS((4,3,3,4),(3,2,2,2,2,2,2,2,2,2,2,2,2,2,2,2,
2,2,2,2,2,2,2,2,2,2,2,2,2,2,2,2,2,2,2,2,2,2,2,2,2,2,2,2,2,2,2,2,2,2,2,2,
2,2,2,2,2,2,2,2,2,2,2,2,2,2,2,2,2,2,2,2,2,2,2,2,2,2,2,2,2,2,2,2,2,2,2,2,
2,2,2,2,2,2,2,2,3),(-5.30788478853017E-5,0.,0.5,0.999946921152115),(0.,
0.0104166666666667,0.0208333333333333,0.03125,0.0416666666666667,0.0520833333333333,
0.0625,0.0729166666666667,0.0833333333333333,0.09375,0.104166666666667,
0.114583333333333,0.125,0.135416666666667,0.145833333333333,0.15625,0.166666666666667,
0.177083333333333,0.1875,0.197916666666667,0.208333333333333,0.21875,0.229166666666667,
0.239583333333333,0.25,0.260416666666667,0.270833333333333,0.28125,0.291666666666667,
0.302083333333333,0.3125,0.322916666666667,0.333333333333333,0.34375,0.354166666666667,
0.364583333333333,0.375,0.385416666666667,0.395833333333333,0.40625,0.416666666666667,
0.427083333333333,0.4375,0.447916666666667,0.458333333333333,0.46875,0.479166666666667,
0.489583333333333,0.5,0.510416666666667,0.520833333333333,0.53125,0.541666666666667,
0.552083333333333,0.5625,0.572916666666667,0.583333333333333,0.59375,0.604166666666667,
0.614583333333333,0.625,0.635416666666667,0.645833333333333,0.65625,0.666666666666667,
0.677083333333333,0.6875,0.697916666666667,0.708333333333333,0.71875,0.729166666666667,
0.739583333333333,0.75,0.760416666666667,0.770833333333333,0.78125,0.791666666666667,
0.802083333333333,0.8125,0.822916666666667,0.833333333333333,0.84375,0.854166666666667,
0.864583333333333,0.875,0.885416666666667,0.895833333333333,0.90625,0.916666666666667,
0.927083333333333,0.9375,0.947916666666667,0.958333333333333,0.96875,0.979166666666667,
0.989583333333333,1.),.UNSPECIFIED.)
GEOMETRIC_REPRESENTATION_ITEM()
RATIONAL_B_SPLINE_SURFACE(((0.999787707147372,0.965720767139978,0.999787707147372,
0.965720767139978,0.999787707147372,0.965720767139978,0.999787707147372,
0.965720767139978,0.999787707147372,0.965720767139978,0.999787707147372,
0.965720767139978,0.999787707147372,0.965720767139978,0.999787707147372,
0.965720767139978,0.999787707147372,0.965720767139978,0.999787707147372,
0.965720767139978,0.999787707147372,0.965720767139978,0.999787707147372,
0.965720767139978,0.999787707147372,0.965720767139978,0.999787707147372,
0.965720767139978,0.999787707147372,0.965720767139978,0.999787707147372,
0.965720767139978,0.999787707147372,0.965720767139978,0.999787707147372,
0.965720767139978,0.999787707147372,0.965720767139978,0.999787707147372,
0.965720767139978,0.999787707147372,0.965720767139978,0.999787707147372,
0.965720767139978,0.999787707147372,0.965720767139978,0.999787707147372,
0.965720767139978,0.999787707147372,0.965720767139978,0.999787707147372,
0.965720767139978,0.999787707147372,0.965720767139978,0.999787707147372,
0.965720767139978,0.999787707147372,0.965720767139978,0.999787707147372,
0.965720767139978,0.999787707147372,0.965720767139978,0.999787707147372,
0.965720767139978,0.999787707147372,0.965720767139978,0.999787707147372,
0.965720767139978,0.999787707147372,0.965720767139978,0.999787707147372,
0.965720767139978,0.999787707147372,0.965720767139978,0.999787707147372,
0.965720767139978,0.999787707147372,0.965720767139978,0.999787707147372,
0.965720767139978,0.999787707147372,0.965720767139978,0.999787707147372,
0.965720767139978,0.999787707147372,0.965720767139978,0.999787707147372,
0.965720767139978,0.999787707147372,0.965720767139978,0.999787707147372,
0.965720767139978,0.999787707147372,0.965720767139978,0.999787707147372,
0.965720767139978,0.999787707147372,0.965720767139978,0.999787707147372,
0.965720767139978,0.999787707147372,0.965720767139978,0.999787707147372,
0.965720767139978,0.999787707147372,0.965720767139978,0.999787707147372,
0.965720767139978,0.999787707147372,0.965720767139978,0.999787707147372,
0.965720767139978,0.999787707147372,0.965720767139978,0.999787707147372,
0.965720767139978,0.999787707147372,0.965720767139978,0.999787707147372,
0.965720767139978,0.999787707147372,0.965720767139978,0.999787707147372,
0.965720767139978,0.999787707147372,0.965720767139978,0.999787707147372,
0.965720767139978,0.999787707147372,0.965720767139978,0.999787707147372,
0.965720767139978,0.999787707147372,0.965720767139978,0.999787707147372,
0.965720767139978,0.999787707147372,0.965720767139978,0.999787707147372,
0.965720767139978,0.999787707147372,0.965720767139978,0.999787707147372,
0.965720767139978,0.999787707147372,0.965720767139978,0.999787707147372,
0.965720767139978,0.999787707147372,0.965720767139978,0.999787707147372,
0.965720767139978,0.999787707147372,0.965720767139978,0.999787707147372,
0.965720767139978,0.999787707147372,0.965720767139978,0.999787707147372,
0.965720767139978,0.999787707147372,0.965720767139978,0.999787707147372,
0.965720767139978,0.999787707147372,0.965720767139978,0.999787707147372,
0.965720767139978,0.999787707147372,0.965720767139978,0.999787707147372,
0.965720767139978,0.999787707147372,0.965720767139978,0.999787707147372,
0.965720767139978,0.999787707147372,0.965720767139978,0.999787707147372,
0.965720767139978,0.999787707147372,0.965720767139978,0.999787707147372,
0.965720767139978,0.999787707147372,0.965720767139978,0.999787707147372,
0.965720767139978,0.999787707147372,0.965720767139978,0.999787707147372,
0.965720767139978,0.999787707147372),(0.99985846391861,0.965789112932702,
0.99985846391861,0.965789112932702,0.99985846391861,0.965789112932702,0.99985846391861,
0.965789112932702,0.99985846391861,0.965789112932702,0.99985846391861,0.965789112932702,
0.99985846391861,0.965789112932702,0.99985846391861,0.965789112932702,0.99985846391861,
0.965789112932702,0.99985846391861,0.965789112932702,0.99985846391861,0.965789112932702,
0.99985846391861,0.965789112932702,0.99985846391861,0.965789112932702,0.99985846391861,
0.965789112932702,0.99985846391861,0.965789112932702,0.99985846391861,0.965789112932702,
0.99985846391861,0.965789112932702,0.99985846391861,0.965789112932702,0.99985846391861,
0.965789112932702,0.99985846391861,0.965789112932702,0.99985846391861,0.965789112932702,
0.99985846391861,0.965789112932702,0.99985846391861,0.965789112932702,0.99985846391861,
0.965789112932702,0.99985846391861,0.965789112932702,0.99985846391861,0.965789112932702,
0.99985846391861,0.965789112932702,0.99985846391861,0.965789112932702,0.99985846391861,
0.965789112932702,0.99985846391861,0.965789112932702,0.99985846391861,0.965789112932702,
0.99985846391861,0.965789112932702,0.99985846391861,0.965789112932702,0.99985846391861,
0.965789112932702,0.99985846391861,0.965789112932702,0.99985846391861,0.965789112932702,
0.99985846391861,0.965789112932702,0.99985846391861,0.965789112932702,0.99985846391861,
0.965789112932702,0.99985846391861,0.965789112932702,0.99985846391861,0.965789112932702,
0.99985846391861,0.965789112932702,0.99985846391861,0.965789112932702,0.99985846391861,
0.965789112932702,0.99985846391861,0.965789112932702,0.99985846391861,0.965789112932702,
0.99985846391861,0.965789112932702,0.99985846391861,0.965789112932702,0.99985846391861,
0.965789112932702,0.99985846391861,0.965789112932702,0.99985846391861,0.965789112932702,
0.99985846391861,0.965789112932702,0.99985846391861,0.965789112932702,0.99985846391861,
0.965789112932702,0.99985846391861,0.965789112932702,0.99985846391861,0.965789112932702,
0.99985846391861,0.965789112932702,0.99985846391861,0.965789112932702,0.99985846391861,
0.965789112932702,0.99985846391861,0.965789112932702,0.99985846391861,0.965789112932702,
0.99985846391861,0.965789112932702,0.99985846391861,0.965789112932702,0.99985846391861,
0.965789112932702,0.99985846391861,0.965789112932702,0.99985846391861,0.965789112932702,
0.99985846391861,0.965789112932702,0.99985846391861,0.965789112932702,0.99985846391861,
0.965789112932702,0.99985846391861,0.965789112932702,0.99985846391861,0.965789112932702,
0.99985846391861,0.965789112932702,0.99985846391861,0.965789112932702,0.99985846391861,
0.965789112932702,0.99985846391861,0.965789112932702,0.99985846391861,0.965789112932702,
0.99985846391861,0.965789112932702,0.99985846391861,0.965789112932702,0.99985846391861,
0.965789112932702,0.99985846391861,0.965789112932702,0.99985846391861,0.965789112932702,
0.99985846391861,0.965789112932702,0.99985846391861,0.965789112932702,0.99985846391861,
0.965789112932702,0.99985846391861,0.965789112932702,0.99985846391861,0.965789112932702,
0.99985846391861,0.965789112932702,0.99985846391861,0.965789112932702,0.99985846391861,
0.965789112932702,0.99985846391861,0.965789112932702,0.99985846391861,0.965789112932702,
0.99985846391861,0.965789112932702,0.99985846391861,0.965789112932702,0.99985846391861,
0.965789112932702,0.99985846391861,0.965789112932702,0.99985846391861,0.965789112932702,
0.99985846391861),(0.99992922820282,0.965857465982399,0.99992922820282,
0.965857465982399,0.99992922820282,0.965857465982399,0.99992922820282,0.965857465982399,
0.99992922820282,0.965857465982399,0.99992922820282,0.965857465982399,0.99992922820282,
0.965857465982399,0.99992922820282,0.965857465982399,0.99992922820282,0.965857465982399,
0.99992922820282,0.965857465982399,0.99992922820282,0.965857465982399,0.99992922820282,
0.965857465982399,0.99992922820282,0.965857465982399,0.99992922820282,0.965857465982399,
0.99992922820282,0.965857465982399,0.99992922820282,0.965857465982399,0.99992922820282,
0.965857465982399,0.99992922820282,0.965857465982399,0.99992922820282,0.965857465982399,
0.99992922820282,0.965857465982399,0.99992922820282,0.965857465982399,0.99992922820282,
0.965857465982399,0.99992922820282,0.965857465982399,0.99992922820282,0.965857465982399,
0.99992922820282,0.965857465982399,0.99992922820282,0.965857465982399,0.99992922820282,
0.965857465982399,0.99992922820282,0.965857465982399,0.99992922820282,0.965857465982399,
0.99992922820282,0.965857465982399,0.99992922820282,0.965857465982399,0.99992922820282,
0.965857465982399,0.99992922820282,0.965857465982399,0.99992922820282,0.965857465982399,
0.99992922820282,0.965857465982399,0.99992922820282,0.965857465982399,0.99992922820282,
0.965857465982399,0.99992922820282,0.965857465982399,0.99992922820282,0.965857465982399,
0.99992922820282,0.965857465982399,0.99992922820282,0.965857465982399,0.99992922820282,
0.965857465982399,0.99992922820282,0.965857465982399,0.99992922820282,0.965857465982399,
0.99992922820282,0.965857465982399,0.99992922820282,0.965857465982399,0.99992922820282,
0.965857465982399,0.99992922820282,0.965857465982399,0.99992922820282,0.965857465982399,
0.99992922820282,0.965857465982399,0.99992922820282,0.965857465982399,0.99992922820282,
0.965857465982399,0.99992922820282,0.965857465982399,0.99992922820282,0.965857465982399,
0.99992922820282,0.965857465982399,0.99992922820282,0.965857465982399,0.99992922820282,
0.965857465982399,0.99992922820282,0.965857465982399,0.99992922820282,0.965857465982399,
0.99992922820282,0.965857465982399,0.99992922820282,0.965857465982399,0.99992922820282,
0.965857465982399,0.99992922820282,0.965857465982399,0.99992922820282,0.965857465982399,
0.99992922820282,0.965857465982399,0.99992922820282,0.965857465982399,0.99992922820282,
0.965857465982399,0.99992922820282,0.965857465982399,0.99992922820282,0.965857465982399,
0.99992922820282,0.965857465982399,0.99992922820282,0.965857465982399,0.99992922820282,
0.965857465982399,0.99992922820282,0.965857465982399,0.99992922820282,0.965857465982399,
0.99992922820282,0.965857465982399,0.99992922820282,0.965857465982399,0.99992922820282,
0.965857465982399,0.99992922820282,0.965857465982399,0.99992922820282,0.965857465982399,
0.99992922820282,0.965857465982399,0.99992922820282,0.965857465982399,0.99992922820282,
0.965857465982399,0.99992922820282,0.965857465982399,0.99992922820282,0.965857465982399,
0.99992922820282,0.965857465982399,0.99992922820282,0.965857465982399,0.99992922820282,
0.965857465982399,0.99992922820282,0.965857465982399,0.99992922820282,0.965857465982399,
0.99992922820282,0.965857465982399,0.99992922820282,0.965857465982399,0.99992922820282,
0.965857465982399,0.99992922820282,0.965857465982399,0.99992922820282,0.965857465982399,
0.99992922820282,0.965857465982399,0.99992922820282,0.965857465982399,0.99992922820282),
(1.,0.965925826289068,1.,0.965925826289068,1.,0.965925826289068,1.,0.965925826289068,
1.,0.965925826289068,1.,0.965925826289068,1.,0.965925826289068,1.,0.965925826289068,
1.,0.965925826289068,1.,0.965925826289068,1.,0.965925826289068,1.,0.965925826289068,
1.,0.965925826289068,1.,0.965925826289068,1.,0.965925826289068,1.,0.965925826289068,
1.,0.965925826289068,1.,0.965925826289068,1.,0.965925826289068,1.,0.965925826289068,
1.,0.965925826289068,1.,0.965925826289068,1.,0.965925826289068,1.,0.965925826289068,
1.,0.965925826289068,1.,0.965925826289068,1.,0.965925826289068,1.,0.965925826289068,
1.,0.965925826289068,1.,0.965925826289068,1.,0.965925826289068,1.,0.965925826289068,
1.,0.965925826289068,1.,0.965925826289068,1.,0.965925826289068,1.,0.965925826289068,
1.,0.965925826289068,1.,0.965925826289068,1.,0.965925826289068,1.,0.965925826289068,
1.,0.965925826289068,1.,0.965925826289068,1.,0.965925826289068,1.,0.965925826289068,
1.,0.965925826289068,1.,0.965925826289068,1.,0.965925826289068,1.,0.965925826289068,
1.,0.965925826289068,1.,0.965925826289068,1.,0.965925826289068,1.,0.965925826289068,
1.,0.965925826289068,1.,0.965925826289068,1.,0.965925826289068,1.,0.965925826289068,
1.,0.965925826289068,1.,0.965925826289068,1.,0.965925826289068,1.,0.965925826289068,
1.,0.965925826289068,1.,0.965925826289068,1.,0.965925826289068,1.,0.965925826289068,
1.,0.965925826289068,1.,0.965925826289068,1.,0.965925826289068,1.,0.965925826289068,
1.,0.965925826289068,1.,0.965925826289068,1.,0.965925826289068,1.,0.965925826289068,
1.,0.965925826289068,1.,0.965925826289068,1.,0.965925826289068,1.,0.965925826289068,
1.,0.965925826289068,1.,0.965925826289068,1.,0.965925826289068,1.,0.965925826289068,
1.,0.965925826289068,1.,0.965925826289068,1.,0.965925826289068,1.,0.965925826289068,
1.,0.965925826289068,1.,0.965925826289068,1.,0.965925826289068,1.,0.965925826289068,
1.,0.965925826289068,1.,0.965925826289068,1.,0.965925826289068,1.,0.965925826289068,
1.,0.965925826289068,1.,0.965925826289068,1.,0.965925826289068,1.,0.965925826289068,
1.),(0.333333333333333,0.321975275429689,0.333333333333333,0.321975275429689,
0.333333333333333,0.321975275429689,0.333333333333333,0.321975275429689,
0.333333333333333,0.321975275429689,0.333333333333333,0.321975275429689,
0.333333333333333,0.321975275429689,0.333333333333333,0.321975275429689,
0.333333333333333,0.321975275429689,0.333333333333333,0.321975275429689,
0.333333333333333,0.321975275429689,0.333333333333333,0.321975275429689,
0.333333333333333,0.321975275429689,0.333333333333333,0.321975275429689,
0.333333333333333,0.321975275429689,0.333333333333333,0.321975275429689,
0.333333333333333,0.321975275429689,0.333333333333333,0.321975275429689,
0.333333333333333,0.321975275429689,0.333333333333333,0.321975275429689,
0.333333333333333,0.321975275429689,0.333333333333333,0.321975275429689,
0.333333333333333,0.321975275429689,0.333333333333333,0.321975275429689,
0.333333333333333,0.321975275429689,0.333333333333333,0.321975275429689,
0.333333333333333,0.321975275429689,0.333333333333333,0.321975275429689,
0.333333333333333,0.321975275429689,0.333333333333333,0.321975275429689,
0.333333333333333,0.321975275429689,0.333333333333333,0.321975275429689,
0.333333333333333,0.321975275429689,0.333333333333333,0.321975275429689,
0.333333333333333,0.321975275429689,0.333333333333333,0.321975275429689,
0.333333333333333,0.321975275429689,0.333333333333333,0.321975275429689,
0.333333333333333,0.321975275429689,0.333333333333333,0.321975275429689,
0.333333333333333,0.321975275429689,0.333333333333333,0.321975275429689,
0.333333333333333,0.321975275429689,0.333333333333333,0.321975275429689,
0.333333333333333,0.321975275429689,0.333333333333333,0.321975275429689,
0.333333333333333,0.321975275429689,0.333333333333333,0.321975275429689,
0.333333333333333,0.321975275429689,0.333333333333333,0.321975275429689,
0.333333333333333,0.321975275429689,0.333333333333333,0.321975275429689,
0.333333333333333,0.321975275429689,0.333333333333333,0.321975275429689,
0.333333333333333,0.321975275429689,0.333333333333333,0.321975275429689,
0.333333333333333,0.321975275429689,0.333333333333333,0.321975275429689,
0.333333333333333,0.321975275429689,0.333333333333333,0.321975275429689,
0.333333333333333,0.321975275429689,0.333333333333333,0.321975275429689,
0.333333333333333,0.321975275429689,0.333333333333333,0.321975275429689,
0.333333333333333,0.321975275429689,0.333333333333333,0.321975275429689,
0.333333333333333,0.321975275429689,0.333333333333333,0.321975275429689,
0.333333333333333,0.321975275429689,0.333333333333333,0.321975275429689,
0.333333333333333,0.321975275429689,0.333333333333333,0.321975275429689,
0.333333333333333,0.321975275429689,0.333333333333333,0.321975275429689,
0.333333333333333,0.321975275429689,0.333333333333333,0.321975275429689,
0.333333333333333,0.321975275429689,0.333333333333333,0.321975275429689,
0.333333333333333,0.321975275429689,0.333333333333333,0.321975275429689,
0.333333333333333,0.321975275429689,0.333333333333333,0.321975275429689,
0.333333333333333,0.321975275429689,0.333333333333333,0.321975275429689,
0.333333333333333,0.321975275429689,0.333333333333333,0.321975275429689,
0.333333333333333,0.321975275429689,0.333333333333333,0.321975275429689,
0.333333333333333,0.321975275429689,0.333333333333333,0.321975275429689,
0.333333333333333,0.321975275429689,0.333333333333333,0.321975275429689,
0.333333333333333,0.321975275429689,0.333333333333333,0.321975275429689,
0.333333333333333,0.321975275429689,0.333333333333333,0.321975275429689,
0.333333333333333),(0.333333333333333,0.321975275429689,0.333333333333333,
0.321975275429689,0.333333333333333,0.321975275429689,0.333333333333333,
0.321975275429689,0.333333333333333,0.321975275429689,0.333333333333333,
0.321975275429689,0.333333333333333,0.321975275429689,0.333333333333333,
0.321975275429689,0.333333333333333,0.321975275429689,0.333333333333333,
0.321975275429689,0.333333333333333,0.321975275429689,0.333333333333333,
0.321975275429689,0.333333333333333,0.321975275429689,0.333333333333333,
0.321975275429689,0.333333333333333,0.321975275429689,0.333333333333333,
0.321975275429689,0.333333333333333,0.321975275429689,0.333333333333333,
0.321975275429689,0.333333333333333,0.321975275429689,0.333333333333333,
0.321975275429689,0.333333333333333,0.321975275429689,0.333333333333333,
0.321975275429689,0.333333333333333,0.321975275429689,0.333333333333333,
0.321975275429689,0.333333333333333,0.321975275429689,0.333333333333333,
0.321975275429689,0.333333333333333,0.321975275429689,0.333333333333333,
0.321975275429689,0.333333333333333,0.321975275429689,0.333333333333333,
0.321975275429689,0.333333333333333,0.321975275429689,0.333333333333333,
0.321975275429689,0.333333333333333,0.321975275429689,0.333333333333333,
0.321975275429689,0.333333333333333,0.321975275429689,0.333333333333333,
0.321975275429689,0.333333333333333,0.321975275429689,0.333333333333333,
0.321975275429689,0.333333333333333,0.321975275429689,0.333333333333333,
0.321975275429689,0.333333333333333,0.321975275429689,0.333333333333333,
0.321975275429689,0.333333333333333,0.321975275429689,0.333333333333333,
0.321975275429689,0.333333333333333,0.321975275429689,0.333333333333333,
0.321975275429689,0.333333333333333,0.321975275429689,0.333333333333333,
0.321975275429689,0.333333333333333,0.321975275429689,0.333333333333333,
0.321975275429689,0.333333333333333,0.321975275429689,0.333333333333333,
0.321975275429689,0.333333333333333,0.321975275429689,0.333333333333333,
0.321975275429689,0.333333333333333,0.321975275429689,0.333333333333333,
0.321975275429689,0.333333333333333,0.321975275429689,0.333333333333333,
0.321975275429689,0.333333333333333,0.321975275429689,0.333333333333333,
0.321975275429689,0.333333333333333,0.321975275429689,0.333333333333333,
0.321975275429689,0.333333333333333,0.321975275429689,0.333333333333333,
0.321975275429689,0.333333333333333,0.321975275429689,0.333333333333333,
0.321975275429689,0.333333333333333,0.321975275429689,0.333333333333333,
0.321975275429689,0.333333333333333,0.321975275429689,0.333333333333333,
0.321975275429689,0.333333333333333,0.321975275429689,0.333333333333333,
0.321975275429689,0.333333333333333,0.321975275429689,0.333333333333333,
0.321975275429689,0.333333333333333,0.321975275429689,0.333333333333333,
0.321975275429689,0.333333333333333,0.321975275429689,0.333333333333333,
0.321975275429689,0.333333333333333,0.321975275429689,0.333333333333333,
0.321975275429689,0.333333333333333,0.321975275429689,0.333333333333333,
0.321975275429689,0.333333333333333,0.321975275429689,0.333333333333333,
0.321975275429689,0.333333333333333,0.321975275429689,0.333333333333333,
0.321975275429689,0.333333333333333,0.321975275429689,0.333333333333333,
0.321975275429689,0.333333333333333,0.321975275429689,0.333333333333333,
0.321975275429689,0.333333333333333,0.321975275429689,0.333333333333333,
0.321975275429689,0.333333333333333,0.321975275429689,0.333333333333333,
0.321975275429689,0.333333333333333,0.321975275429689,0.333333333333333,
0.321975275429689,0.333333333333333),(1.,0.965925826289068,1.,0.965925826289068,
1.,0.965925826289068,1.,0.965925826289068,1.,0.965925826289068,1.,0.965925826289068,
1.,0.965925826289068,1.,0.965925826289068,1.,0.965925826289068,1.,0.965925826289068,
1.,0.965925826289068,1.,0.965925826289068,1.,0.965925826289068,1.,0.965925826289068,
1.,0.965925826289068,1.,0.965925826289068,1.,0.965925826289068,1.,0.965925826289068,
1.,0.965925826289068,1.,0.965925826289068,1.,0.965925826289068,1.,0.965925826289068,
1.,0.965925826289068,1.,0.965925826289068,1.,0.965925826289068,1.,0.965925826289068,
1.,0.965925826289068,1.,0.965925826289068,1.,0.965925826289068,1.,0.965925826289068,
1.,0.965925826289068,1.,0.965925826289068,1.,0.965925826289068,1.,0.965925826289068,
1.,0.965925826289068,1.,0.965925826289068,1.,0.965925826289068,1.,0.965925826289068,
1.,0.965925826289068,1.,0.965925826289068,1.,0.965925826289068,1.,0.965925826289068,
1.,0.965925826289068,1.,0.965925826289068,1.,0.965925826289068,1.,0.965925826289068,
1.,0.965925826289068,1.,0.965925826289068,1.,0.965925826289068,1.,0.965925826289068,
1.,0.965925826289068,1.,0.965925826289068,1.,0.965925826289068,1.,0.965925826289068,
1.,0.965925826289068,1.,0.965925826289068,1.,0.965925826289068,1.,0.965925826289068,
1.,0.965925826289068,1.,0.965925826289068,1.,0.965925826289068,1.,0.965925826289068,
1.,0.965925826289068,1.,0.965925826289068,1.,0.965925826289068,1.,0.965925826289068,
1.,0.965925826289068,1.,0.965925826289068,1.,0.965925826289068,1.,0.965925826289068,
1.,0.965925826289068,1.,0.965925826289068,1.,0.965925826289068,1.,0.965925826289068,
1.,0.965925826289068,1.,0.965925826289068,1.,0.965925826289068,1.,0.965925826289068,
1.,0.965925826289068,1.,0.965925826289068,1.,0.965925826289068,1.,0.965925826289068,
1.,0.965925826289068,1.,0.965925826289068,1.,0.965925826289068,1.,0.965925826289068,
1.,0.965925826289068,1.,0.965925826289068,1.,0.965925826289068,1.,0.965925826289068,
1.,0.965925826289068,1.,0.965925826289068,1.,0.965925826289068,1.,0.965925826289068,
1.,0.965925826289068,1.,0.965925826289068,1.),(0.333404105130514,0.322043635736359,
0.333404105130514,0.322043635736359,0.333404105130514,0.322043635736359,
0.333404105130514,0.322043635736359,0.333404105130514,0.322043635736359,
0.333404105130514,0.322043635736359,0.333404105130514,0.322043635736359,
0.333404105130514,0.322043635736359,0.333404105130514,0.322043635736359,
0.333404105130514,0.322043635736359,0.333404105130514,0.322043635736359,
0.333404105130514,0.322043635736359,0.333404105130514,0.322043635736359,
0.333404105130514,0.322043635736359,0.333404105130514,0.322043635736359,
0.333404105130514,0.322043635736359,0.333404105130514,0.322043635736359,
0.333404105130514,0.322043635736359,0.333404105130514,0.322043635736359,
0.333404105130514,0.322043635736359,0.333404105130514,0.322043635736359,
0.333404105130514,0.322043635736359,0.333404105130514,0.322043635736359,
0.333404105130514,0.322043635736359,0.333404105130514,0.322043635736359,
0.333404105130514,0.322043635736359,0.333404105130514,0.322043635736359,
0.333404105130514,0.322043635736359,0.333404105130514,0.322043635736359,
0.333404105130514,0.322043635736359,0.333404105130514,0.322043635736359,
0.333404105130514,0.322043635736359,0.333404105130514,0.322043635736359,
0.333404105130514,0.322043635736359,0.333404105130514,0.322043635736359,
0.333404105130514,0.322043635736359,0.333404105130514,0.322043635736359,
0.333404105130514,0.322043635736359,0.333404105130514,0.322043635736359,
0.333404105130514,0.322043635736359,0.333404105130514,0.322043635736359,
0.333404105130514,0.322043635736359,0.333404105130514,0.322043635736359,
0.333404105130514,0.322043635736359,0.333404105130514,0.322043635736359,
0.333404105130514,0.322043635736359,0.333404105130514,0.322043635736359,
0.333404105130514,0.322043635736359,0.333404105130514,0.322043635736359,
0.333404105130514,0.322043635736359,0.333404105130514,0.322043635736359,
0.333404105130514,0.322043635736359,0.333404105130514,0.322043635736359,
0.333404105130514,0.322043635736359,0.333404105130514,0.322043635736359,
0.333404105130514,0.322043635736359,0.333404105130514,0.322043635736359,
0.333404105130514,0.322043635736359,0.333404105130514,0.322043635736359,
0.333404105130514,0.322043635736359,0.333404105130514,0.322043635736359,
0.333404105130514,0.322043635736359,0.333404105130514,0.322043635736359,
0.333404105130514,0.322043635736359,0.333404105130514,0.322043635736359,
0.333404105130514,0.322043635736359,0.333404105130514,0.322043635736359,
0.333404105130514,0.322043635736359,0.333404105130514,0.322043635736359,
0.333404105130514,0.322043635736359,0.333404105130514,0.322043635736359,
0.333404105130514,0.322043635736359,0.333404105130514,0.322043635736359,
0.333404105130514,0.322043635736359,0.333404105130514,0.322043635736359,
0.333404105130514,0.322043635736359,0.333404105130514,0.322043635736359,
0.333404105130514,0.322043635736359,0.333404105130514,0.322043635736359,
0.333404105130514,0.322043635736359,0.333404105130514,0.322043635736359,
0.333404105130514,0.322043635736359,0.333404105130514,0.322043635736359,
0.333404105130514,0.322043635736359,0.333404105130514,0.322043635736359,
0.333404105130514,0.322043635736359,0.333404105130514,0.322043635736359,
0.333404105130514,0.322043635736359,0.333404105130514,0.322043635736359,
0.333404105130514,0.322043635736359,0.333404105130514,0.322043635736359,
0.333404105130514,0.322043635736359,0.333404105130514,0.322043635736359,
0.333404105130514,0.322043635736359,0.333404105130514,0.322043635736359,
0.333404105130514,0.322043635736359,0.333404105130514),(0.333333340846304,
0.321975282686662,0.333333340846304,0.321975282686662,0.333333340846304,
0.321975282686662,0.333333340846304,0.321975282686662,0.333333340846304,
0.321975282686662,0.333333340846304,0.321975282686662,0.333333340846304,
0.321975282686662,0.333333340846304,0.321975282686662,0.333333340846304,
0.321975282686662,0.333333340846304,0.321975282686662,0.333333340846304,
0.321975282686662,0.333333340846304,0.321975282686662,0.333333340846304,
0.321975282686662,0.333333340846304,0.321975282686662,0.333333340846304,
0.321975282686662,0.333333340846304,0.321975282686662,0.333333340846304,
0.321975282686662,0.333333340846304,0.321975282686662,0.333333340846304,
0.321975282686662,0.333333340846304,0.321975282686662,0.333333340846304,
0.321975282686662,0.333333340846304,0.321975282686662,0.333333340846304,
0.321975282686662,0.333333340846304,0.321975282686662,0.333333340846304,
0.321975282686662,0.333333340846304,0.321975282686662,0.333333340846304,
0.321975282686662,0.333333340846304,0.321975282686662,0.333333340846304,
0.321975282686662,0.333333340846304,0.321975282686662,0.333333340846304,
0.321975282686662,0.333333340846304,0.321975282686662,0.333333340846304,
0.321975282686662,0.333333340846304,0.321975282686662,0.333333340846304,
0.321975282686662,0.333333340846304,0.321975282686662,0.333333340846304,
0.321975282686662,0.333333340846304,0.321975282686662,0.333333340846304,
0.321975282686662,0.333333340846304,0.321975282686662,0.333333340846304,
0.321975282686662,0.333333340846304,0.321975282686662,0.333333340846304,
0.321975282686662,0.333333340846304,0.321975282686662,0.333333340846304,
0.321975282686662,0.333333340846304,0.321975282686662,0.333333340846304,
0.321975282686662,0.333333340846304,0.321975282686662,0.333333340846304,
0.321975282686662,0.333333340846304,0.321975282686662,0.333333340846304,
0.321975282686662,0.333333340846304,0.321975282686662,0.333333340846304,
0.321975282686662,0.333333340846304,0.321975282686662,0.333333340846304,
0.321975282686662,0.333333340846304,0.321975282686662,0.333333340846304,
0.321975282686662,0.333333340846304,0.321975282686662,0.333333340846304,
0.321975282686662,0.333333340846304,0.321975282686662,0.333333340846304,
0.321975282686662,0.333333340846304,0.321975282686662,0.333333340846304,
0.321975282686662,0.333333340846304,0.321975282686662,0.333333340846304,
0.321975282686662,0.333333340846304,0.321975282686662,0.333333340846304,
0.321975282686662,0.333333340846304,0.321975282686662,0.333333340846304,
0.321975282686662,0.333333340846304,0.321975282686662,0.333333340846304,
0.321975282686662,0.333333340846304,0.321975282686662,0.333333340846304,
0.321975282686662,0.333333340846304,0.321975282686662,0.333333340846304,
0.321975282686662,0.333333340846304,0.321975282686662,0.333333340846304,
0.321975282686662,0.333333340846304,0.321975282686662,0.333333340846304,
0.321975282686662,0.333333340846304,0.321975282686662,0.333333340846304,
0.321975282686662,0.333333340846304,0.321975282686662,0.333333340846304,
0.321975282686662,0.333333340846304,0.321975282686662,0.333333340846304,
0.321975282686662,0.333333340846304,0.321975282686662,0.333333340846304,
0.321975282686662,0.333333340846304,0.321975282686662,0.333333340846304,
0.321975282686662,0.333333340846304,0.321975282686662,0.333333340846304,
0.321975282686662,0.333333340846304,0.321975282686662,0.333333340846304,
0.321975282686662,0.333333340846304,0.321975282686662,0.333333340846304,
0.321975282686662,0.333333340846304,0.321975282686662,0.333333340846304),
(0.999787707147372,0.965720767139978,0.999787707147372,0.965720767139978,
0.999787707147372,0.965720767139978,0.999787707147372,0.965720767139978,
0.999787707147372,0.965720767139978,0.999787707147372,0.965720767139978,
0.999787707147372,0.965720767139978,0.999787707147372,0.965720767139978,
0.999787707147372,0.965720767139978,0.999787707147372,0.965720767139978,
0.999787707147372,0.965720767139978,0.999787707147372,0.965720767139978,
0.999787707147372,0.965720767139978,0.999787707147372,0.965720767139978,
0.999787707147372,0.965720767139978,0.999787707147372,0.965720767139978,
0.999787707147372,0.965720767139978,0.999787707147372,0.965720767139978,
0.999787707147372,0.965720767139978,0.999787707147372,0.965720767139978,
0.999787707147372,0.965720767139978,0.999787707147372,0.965720767139978,
0.999787707147372,0.965720767139978,0.999787707147372,0.965720767139978,
0.999787707147372,0.965720767139978,0.999787707147372,0.965720767139978,
0.999787707147372,0.965720767139978,0.999787707147372,0.965720767139978,
0.999787707147372,0.965720767139978,0.999787707147372,0.965720767139978,
0.999787707147372,0.965720767139978,0.999787707147372,0.965720767139978,
0.999787707147372,0.965720767139978,0.999787707147372,0.965720767139978,
0.999787707147372,0.965720767139978,0.999787707147372,0.965720767139978,
0.999787707147372,0.965720767139978,0.999787707147372,0.965720767139978,
0.999787707147372,0.965720767139978,0.999787707147372,0.965720767139978,
0.999787707147372,0.965720767139978,0.999787707147372,0.965720767139978,
0.999787707147372,0.965720767139978,0.999787707147372,0.965720767139978,
0.999787707147372,0.965720767139978,0.999787707147372,0.965720767139978,
0.999787707147372,0.965720767139978,0.999787707147372,0.965720767139978,
0.999787707147372,0.965720767139978,0.999787707147372,0.965720767139978,
0.999787707147372,0.965720767139978,0.999787707147372,0.965720767139978,
0.999787707147372,0.965720767139978,0.999787707147372,0.965720767139978,
0.999787707147372,0.965720767139978,0.999787707147372,0.965720767139978,
0.999787707147372,0.965720767139978,0.999787707147372,0.965720767139978,
0.999787707147372,0.965720767139978,0.999787707147372,0.965720767139978,
0.999787707147372,0.965720767139978,0.999787707147372,0.965720767139978,
0.999787707147372,0.965720767139978,0.999787707147372,0.965720767139978,
0.999787707147372,0.965720767139978,0.999787707147372,0.965720767139978,
0.999787707147372,0.965720767139978,0.999787707147372,0.965720767139978,
0.999787707147372,0.965720767139978,0.999787707147372,0.965720767139978,
0.999787707147372,0.965720767139978,0.999787707147372,0.965720767139978,
0.999787707147372,0.965720767139978,0.999787707147372,0.965720767139978,
0.999787707147372,0.965720767139978,0.999787707147372,0.965720767139978,
0.999787707147372,0.965720767139978,0.999787707147372,0.965720767139978,
0.999787707147372,0.965720767139978,0.999787707147372,0.965720767139978,
0.999787707147372,0.965720767139978,0.999787707147372,0.965720767139978,
0.999787707147372,0.965720767139978,0.999787707147372,0.965720767139978,
0.999787707147372,0.965720767139978,0.999787707147372,0.965720767139978,
0.999787707147372,0.965720767139978,0.999787707147372,0.965720767139978,
0.999787707147372,0.965720767139978,0.999787707147372,0.965720767139978,
0.999787707147372,0.965720767139978,0.999787707147372,0.965720767139978,
0.999787707147372,0.965720767139978,0.999787707147372,0.965720767139978,
0.999787707147372,0.965720767139978,0.999787707147372,0.965720767139978,
0.999787707147372)))
REPRESENTATION_ITEM('')
SURFACE()
);
#18=(
BOUNDED_SURFACE()
B_SPLINE_SURFACE(3,2,((#9944,#9945,#9946,#9947,#9948,#9949,#9950,#9951,
#9952,#9953,#9954,#9955,#9956,#9957,#9958,#9959,#9960,#9961,#9962,#9963,
#9964,#9965,#9966,#9967,#9968,#9969,#9970,#9971,#9972,#9973,#9974,#9975,
#9976,#9977,#9978,#9979,#9980,#9981,#9982,#9983,#9984,#9985,#9986,#9987,
#9988,#9989,#9990,#9991,#9992,#9993,#9994,#9995,#9996,#9997,#9998,#9999,
#10000,#10001,#10002,#10003,#10004,#10005,#10006,#10007,#10008,#10009,#10010,
#10011,#10012,#10013,#10014,#10015,#10016,#10017,#10018,#10019,#10020,#10021,
#10022,#10023,#10024,#10025,#10026,#10027,#10028,#10029,#10030,#10031,#10032,
#10033,#10034,#10035,#10036,#10037,#10038,#10039,#10040,#10041,#10042,#10043,
#10044,#10045,#10046,#10047,#10048,#10049,#10050,#10051,#10052,#10053,#10054,
#10055,#10056,#10057,#10058,#10059,#10060,#10061,#10062,#10063,#10064,#10065,
#10066,#10067,#10068,#10069,#10070,#10071,#10072,#10073,#10074,#10075,#10076,
#10077,#10078,#10079,#10080,#10081,#10082,#10083,#10084,#10085,#10086,#10087,
#10088,#10089,#10090,#10091,#10092,#10093,#10094,#10095,#10096,#10097,#10098,
#10099,#10100,#10101,#10102,#10103,#10104,#10105,#10106,#10107,#10108,#10109,
#10110,#10111,#10112,#10113,#10114,#10115,#10116,#10117,#10118,#10119,#10120,
#10121,#10122,#10123,#10124,#10125,#10126,#10127,#10128,#10129,#10130,#10131,
#10132,#10133,#10134,#10135,#10136),(#10137,#10138,#10139,#10140,#10141,
#10142,#10143,#10144,#10145,#10146,#10147,#10148,#10149,#10150,#10151,#10152,
#10153,#10154,#10155,#10156,#10157,#10158,#10159,#10160,#10161,#10162,#10163,
#10164,#10165,#10166,#10167,#10168,#10169,#10170,#10171,#10172,#10173,#10174,
#10175,#10176,#10177,#10178,#10179,#10180,#10181,#10182,#10183,#10184,#10185,
#10186,#10187,#10188,#10189,#10190,#10191,#10192,#10193,#10194,#10195,#10196,
#10197,#10198,#10199,#10200,#10201,#10202,#10203,#10204,#10205,#10206,#10207,
#10208,#10209,#10210,#10211,#10212,#10213,#10214,#10215,#10216,#10217,#10218,
#10219,#10220,#10221,#10222,#10223,#10224,#10225,#10226,#10227,#10228,#10229,
#10230,#10231,#10232,#10233,#10234,#10235,#10236,#10237,#10238,#10239,#10240,
#10241,#10242,#10243,#10244,#10245,#10246,#10247,#10248,#10249,#10250,#10251,
#10252,#10253,#10254,#10255,#10256,#10257,#10258,#10259,#10260,#10261,#10262,
#10263,#10264,#10265,#10266,#10267,#10268,#10269,#10270,#10271,#10272,#10273,
#10274,#10275,#10276,#10277,#10278,#10279,#10280,#10281,#10282,#10283,#10284,
#10285,#10286,#10287,#10288,#10289,#10290,#10291,#10292,#10293,#10294,#10295,
#10296,#10297,#10298,#10299,#10300,#10301,#10302,#10303,#10304,#10305,#10306,
#10307,#10308,#10309,#10310,#10311,#10312,#10313,#10314,#10315,#10316,#10317,
#10318,#10319,#10320,#10321,#10322,#10323,#10324,#10325,#10326,#10327,#10328,
#10329),(#10330,#10331,#10332,#10333,#10334,#10335,#10336,#10337,#10338,
#10339,#10340,#10341,#10342,#10343,#10344,#10345,#10346,#10347,#10348,#10349,
#10350,#10351,#10352,#10353,#10354,#10355,#10356,#10357,#10358,#10359,#10360,
#10361,#10362,#10363,#10364,#10365,#10366,#10367,#10368,#10369,#10370,#10371,
#10372,#10373,#10374,#10375,#10376,#10377,#10378,#10379,#10380,#10381,#10382,
#10383,#10384,#10385,#10386,#10387,#10388,#10389,#10390,#10391,#10392,#10393,
#10394,#10395,#10396,#10397,#10398,#10399,#10400,#10401,#10402,#10403,#10404,
#10405,#10406,#10407,#10408,#10409,#10410,#10411,#10412,#10413,#10414,#10415,
#10416,#10417,#10418,#10419,#10420,#10421,#10422,#10423,#10424,#10425,#10426,
#10427,#10428,#10429,#10430,#10431,#10432,#10433,#10434,#10435,#10436,#10437,
#10438,#10439,#10440,#10441,#10442,#10443,#10444,#10445,#10446,#10447,#10448,
#10449,#10450,#10451,#10452,#10453,#10454,#10455,#10456,#10457,#10458,#10459,
#10460,#10461,#10462,#10463,#10464,#10465,#10466,#10467,#10468,#10469,#10470,
#10471,#10472,#10473,#10474,#10475,#10476,#10477,#10478,#10479,#10480,#10481,
#10482,#10483,#10484,#10485,#10486,#10487,#10488,#10489,#10490,#10491,#10492,
#10493,#10494,#10495,#10496,#10497,#10498,#10499,#10500,#10501,#10502,#10503,
#10504,#10505,#10506,#10507,#10508,#10509,#10510,#10511,#10512,#10513,#10514,
#10515,#10516,#10517,#10518,#10519,#10520,#10521,#10522),(#10523,#10524,
#10525,#10526,#10527,#10528,#10529,#10530,#10531,#10532,#10533,#10534,#10535,
#10536,#10537,#10538,#10539,#10540,#10541,#10542,#10543,#10544,#10545,#10546,
#10547,#10548,#10549,#10550,#10551,#10552,#10553,#10554,#10555,#10556,#10557,
#10558,#10559,#10560,#10561,#10562,#10563,#10564,#10565,#10566,#10567,#10568,
#10569,#10570,#10571,#10572,#10573,#10574,#10575,#10576,#10577,#10578,#10579,
#10580,#10581,#10582,#10583,#10584,#10585,#10586,#10587,#10588,#10589,#10590,
#10591,#10592,#10593,#10594,#10595,#10596,#10597,#10598,#10599,#10600,#10601,
#10602,#10603,#10604,#10605,#10606,#10607,#10608,#10609,#10610,#10611,#10612,
#10613,#10614,#10615,#10616,#10617,#10618,#10619,#10620,#10621,#10622,#10623,
#10624,#10625,#10626,#10627,#10628,#10629,#10630,#10631,#10632,#10633,#10634,
#10635,#10636,#10637,#10638,#10639,#10640,#10641,#10642,#10643,#10644,#10645,
#10646,#10647,#10648,#10649,#10650,#10651,#10652,#10653,#10654,#10655,#10656,
#10657,#10658,#10659,#10660,#10661,#10662,#10663,#10664,#10665,#10666,#10667,
#10668,#10669,#10670,#10671,#10672,#10673,#10674,#10675,#10676,#10677,#10678,
#10679,#10680,#10681,#10682,#10683,#10684,#10685,#10686,#10687,#10688,#10689,
#10690,#10691,#10692,#10693,#10694,#10695,#10696,#10697,#10698,#10699,#10700,
#10701,#10702,#10703,#10704,#10705,#10706,#10707,#10708,#10709,#10710,#10711,
#10712,#10713,#10714,#10715),(#10716,#10717,#10718,#10719,#10720,#10721,
#10722,#10723,#10724,#10725,#10726,#10727,#10728,#10729,#10730,#10731,#10732,
#10733,#10734,#10735,#10736,#10737,#10738,#10739,#10740,#10741,#10742,#10743,
#10744,#10745,#10746,#10747,#10748,#10749,#10750,#10751,#10752,#10753,#10754,
#10755,#10756,#10757,#10758,#10759,#10760,#10761,#10762,#10763,#10764,#10765,
#10766,#10767,#10768,#10769,#10770,#10771,#10772,#10773,#10774,#10775,#10776,
#10777,#10778,#10779,#10780,#10781,#10782,#10783,#10784,#10785,#10786,#10787,
#10788,#10789,#10790,#10791,#10792,#10793,#10794,#10795,#10796,#10797,#10798,
#10799,#10800,#10801,#10802,#10803,#10804,#10805,#10806,#10807,#10808,#10809,
#10810,#10811,#10812,#10813,#10814,#10815,#10816,#10817,#10818,#10819,#10820,
#10821,#10822,#10823,#10824,#10825,#10826,#10827,#10828,#10829,#10830,#10831,
#10832,#10833,#10834,#10835,#10836,#10837,#10838,#10839,#10840,#10841,#10842,
#10843,#10844,#10845,#10846,#10847,#10848,#10849,#10850,#10851,#10852,#10853,
#10854,#10855,#10856,#10857,#10858,#10859,#10860,#10861,#10862,#10863,#10864,
#10865,#10866,#10867,#10868,#10869,#10870,#10871,#10872,#10873,#10874,#10875,
#10876,#10877,#10878,#10879,#10880,#10881,#10882,#10883,#10884,#10885,#10886,
#10887,#10888,#10889,#10890,#10891,#10892,#10893,#10894,#10895,#10896,#10897,
#10898,#10899,#10900,#10901,#10902,#10903,#10904,#10905,#10906,#10907,#10908),
(#10909,#10910,#10911,#10912,#10913,#10914,#10915,#10916,#10917,#10918,
#10919,#10920,#10921,#10922,#10923,#10924,#10925,#10926,#10927,#10928,#10929,
#10930,#10931,#10932,#10933,#10934,#10935,#10936,#10937,#10938,#10939,#10940,
#10941,#10942,#10943,#10944,#10945,#10946,#10947,#10948,#10949,#10950,#10951,
#10952,#10953,#10954,#10955,#10956,#10957,#10958,#10959,#10960,#10961,#10962,
#10963,#10964,#10965,#10966,#10967,#10968,#10969,#10970,#10971,#10972,#10973,
#10974,#10975,#10976,#10977,#10978,#10979,#10980,#10981,#10982,#10983,#10984,
#10985,#10986,#10987,#10988,#10989,#10990,#10991,#10992,#10993,#10994,#10995,
#10996,#10997,#10998,#10999,#11000,#11001,#11002,#11003,#11004,#11005,#11006,
#11007,#11008,#11009,#11010,#11011,#11012,#11013,#11014,#11015,#11016,#11017,
#11018,#11019,#11020,#11021,#11022,#11023,#11024,#11025,#11026,#11027,#11028,
#11029,#11030,#11031,#11032,#11033,#11034,#11035,#11036,#11037,#11038,#11039,
#11040,#11041,#11042,#11043,#11044,#11045,#11046,#11047,#11048,#11049,#11050,
#11051,#11052,#11053,#11054,#11055,#11056,#11057,#11058,#11059,#11060,#11061,
#11062,#11063,#11064,#11065,#11066,#11067,#11068,#11069,#11070,#11071,#11072,
#11073,#11074,#11075,#11076,#11077,#11078,#11079,#11080,#11081,#11082,#11083,
#11084,#11085,#11086,#11087,#11088,#11089,#11090,#11091,#11092,#11093,#11094,
#11095,#11096,#11097,#11098,#11099,#11100,#11101),(#11102,#11103,#11104,
#11105,#11106,#11107,#11108,#11109,#11110,#11111,#11112,#11113,#11114,#11115,
#11116,#11117,#11118,#11119,#11120,#11121,#11122,#11123,#11124,#11125,#11126,
#11127,#11128,#11129,#11130,#11131,#11132,#11133,#11134,#11135,#11136,#11137,
#11138,#11139,#11140,#11141,#11142,#11143,#11144,#11145,#11146,#11147,#11148,
#11149,#11150,#11151,#11152,#11153,#11154,#11155,#11156,#11157,#11158,#11159,
#11160,#11161,#11162,#11163,#11164,#11165,#11166,#11167,#11168,#11169,#11170,
#11171,#11172,#11173,#11174,#11175,#11176,#11177,#11178,#11179,#11180,#11181,
#11182,#11183,#11184,#11185,#11186,#11187,#11188,#11189,#11190,#11191,#11192,
#11193,#11194,#11195,#11196,#11197,#11198,#11199,#11200,#11201,#11202,#11203,
#11204,#11205,#11206,#11207,#11208,#11209,#11210,#11211,#11212,#11213,#11214,
#11215,#11216,#11217,#11218,#11219,#11220,#11221,#11222,#11223,#11224,#11225,
#11226,#11227,#11228,#11229,#11230,#11231,#11232,#11233,#11234,#11235,#11236,
#11237,#11238,#11239,#11240,#11241,#11242,#11243,#11244,#11245,#11246,#11247,
#11248,#11249,#11250,#11251,#11252,#11253,#11254,#11255,#11256,#11257,#11258,
#11259,#11260,#11261,#11262,#11263,#11264,#11265,#11266,#11267,#11268,#11269,
#11270,#11271,#11272,#11273,#11274,#11275,#11276,#11277,#11278,#11279,#11280,
#11281,#11282,#11283,#11284,#11285,#11286,#11287,#11288,#11289,#11290,#11291,
#11292,#11293,#11294)),.UNSPECIFIED.,.T.,.F.,.F.)
B_SPLINE_SURFACE_WITH_KNOTS((4,3,4),(3,2,2,2,2,2,2,2,2,2,2,2,2,2,2,2,2,
2,2,2,2,2,2,2,2,2,2,2,2,2,2,2,2,2,2,2,2,2,2,2,2,2,2,2,2,2,2,2,2,2,2,2,2,
2,2,2,2,2,2,2,2,2,2,2,2,2,2,2,2,2,2,2,2,2,2,2,2,2,2,2,2,2,2,2,2,2,2,2,2,
2,2,2,2,2,2,2,3),(0.,0.5,1.),(0.,0.0104166666666667,0.0208333333333333,
0.03125,0.0416666666666667,0.0520833333333333,0.0625,0.0729166666666667,
0.0833333333333333,0.09375,0.104166666666667,0.114583333333333,0.125,0.135416666666667,
0.145833333333333,0.15625,0.166666666666667,0.177083333333333,0.1875,0.197916666666667,
0.208333333333333,0.21875,0.229166666666667,0.239583333333333,0.25,0.260416666666667,
0.270833333333333,0.28125,0.291666666666667,0.302083333333333,0.3125,0.322916666666667,
0.333333333333333,0.34375,0.354166666666667,0.364583333333333,0.375,0.385416666666667,
0.395833333333333,0.40625,0.416666666666667,0.427083333333333,0.4375,0.447916666666667,
0.458333333333333,0.46875,0.479166666666667,0.489583333333333,0.5,0.510416666666667,
0.520833333333333,0.53125,0.541666666666667,0.552083333333333,0.5625,0.572916666666667,
0.583333333333333,0.59375,0.604166666666667,0.614583333333333,0.625,0.635416666666667,
0.645833333333333,0.65625,0.666666666666667,0.677083333333333,0.6875,0.697916666666667,
0.708333333333333,0.71875,0.729166666666667,0.739583333333333,0.75,0.760416666666667,
0.770833333333333,0.78125,0.791666666666667,0.802083333333333,0.8125,0.822916666666667,
0.833333333333333,0.84375,0.854166666666667,0.864583333333333,0.875,0.885416666666667,
0.895833333333333,0.90625,0.916666666666667,0.927083333333333,0.9375,0.947916666666667,
0.958333333333333,0.96875,0.979166666666667,0.989583333333333,1.),
 .UNSPECIFIED.)
GEOMETRIC_REPRESENTATION_ITEM()
RATIONAL_B_SPLINE_SURFACE(((1.,0.965925826289068,1.,0.965925826289068,1.,
0.965925826289068,1.,0.965925826289068,1.,0.965925826289068,1.,0.965925826289068,
1.,0.965925826289068,1.,0.965925826289068,1.,0.965925826289068,1.,0.965925826289068,
1.,0.965925826289068,1.,0.965925826289068,1.,0.965925826289068,1.,0.965925826289068,
1.,0.965925826289068,1.,0.965925826289068,1.,0.965925826289068,1.,0.965925826289068,
1.,0.965925826289068,1.,0.965925826289068,1.,0.965925826289068,1.,0.965925826289068,
1.,0.965925826289068,1.,0.965925826289068,1.,0.965925826289068,1.,0.965925826289068,
1.,0.965925826289068,1.,0.965925826289068,1.,0.965925826289068,1.,0.965925826289068,
1.,0.965925826289068,1.,0.965925826289068,1.,0.965925826289068,1.,0.965925826289068,
1.,0.965925826289068,1.,0.965925826289068,1.,0.965925826289068,1.,0.965925826289068,
1.,0.965925826289068,1.,0.965925826289068,1.,0.965925826289068,1.,0.965925826289068,
1.,0.965925826289068,1.,0.965925826289068,1.,0.965925826289068,1.,0.965925826289068,
1.,0.965925826289068,1.,0.965925826289068,1.,0.965925826289068,1.,0.965925826289068,
1.,0.965925826289068,1.,0.965925826289068,1.,0.965925826289068,1.,0.965925826289068,
1.,0.965925826289068,1.,0.965925826289068,1.,0.965925826289068,1.,0.965925826289068,
1.,0.965925826289068,1.,0.965925826289068,1.,0.965925826289068,1.,0.965925826289068,
1.,0.965925826289068,1.,0.965925826289068,1.,0.965925826289068,1.,0.965925826289068,
1.,0.965925826289068,1.,0.965925826289068,1.,0.965925826289068,1.,0.965925826289068,
1.,0.965925826289068,1.,0.965925826289068,1.,0.965925826289068,1.,0.965925826289068,
1.,0.965925826289068,1.,0.965925826289068,1.,0.965925826289068,1.,0.965925826289068,
1.,0.965925826289068,1.,0.965925826289068,1.,0.965925826289068,1.,0.965925826289068,
1.,0.965925826289068,1.,0.965925826289068,1.,0.965925826289068,1.,0.965925826289068,
1.,0.965925826289068,1.,0.965925826289068,1.,0.965925826289068,1.,0.965925826289068,
1.,0.965925826289068,1.,0.965925826289068,1.,0.965925826289068,1.,0.965925826289068,
1.,0.965925826289068,1.,0.965925826289068,1.),(0.333333333333333,0.321975275429689,
0.333333333333333,0.321975275429689,0.333333333333333,0.321975275429689,
0.333333333333333,0.321975275429689,0.333333333333333,0.321975275429689,
0.333333333333333,0.321975275429689,0.333333333333333,0.321975275429689,
0.333333333333333,0.321975275429689,0.333333333333333,0.321975275429689,
0.333333333333333,0.321975275429689,0.333333333333333,0.321975275429689,
0.333333333333333,0.321975275429689,0.333333333333333,0.321975275429689,
0.333333333333333,0.321975275429689,0.333333333333333,0.321975275429689,
0.333333333333333,0.321975275429689,0.333333333333333,0.321975275429689,
0.333333333333333,0.321975275429689,0.333333333333333,0.321975275429689,
0.333333333333333,0.321975275429689,0.333333333333333,0.321975275429689,
0.333333333333333,0.321975275429689,0.333333333333333,0.321975275429689,
0.333333333333333,0.321975275429689,0.333333333333333,0.321975275429689,
0.333333333333333,0.321975275429689,0.333333333333333,0.321975275429689,
0.333333333333333,0.321975275429689,0.333333333333333,0.321975275429689,
0.333333333333333,0.321975275429689,0.333333333333333,0.321975275429689,
0.333333333333333,0.321975275429689,0.333333333333333,0.321975275429689,
0.333333333333333,0.321975275429689,0.333333333333333,0.321975275429689,
0.333333333333333,0.321975275429689,0.333333333333333,0.321975275429689,
0.333333333333333,0.321975275429689,0.333333333333333,0.321975275429689,
0.333333333333333,0.321975275429689,0.333333333333333,0.321975275429689,
0.333333333333333,0.321975275429689,0.333333333333333,0.321975275429689,
0.333333333333333,0.321975275429689,0.333333333333333,0.321975275429689,
0.333333333333333,0.321975275429689,0.333333333333333,0.321975275429689,
0.333333333333333,0.321975275429689,0.333333333333333,0.321975275429689,
0.333333333333333,0.321975275429689,0.333333333333333,0.321975275429689,
0.333333333333333,0.321975275429689,0.333333333333333,0.321975275429689,
0.333333333333333,0.321975275429689,0.333333333333333,0.321975275429689,
0.333333333333333,0.321975275429689,0.333333333333333,0.321975275429689,
0.333333333333333,0.321975275429689,0.333333333333333,0.321975275429689,
0.333333333333333,0.321975275429689,0.333333333333333,0.321975275429689,
0.333333333333333,0.321975275429689,0.333333333333333,0.321975275429689,
0.333333333333333,0.321975275429689,0.333333333333333,0.321975275429689,
0.333333333333333,0.321975275429689,0.333333333333333,0.321975275429689,
0.333333333333333,0.321975275429689,0.333333333333333,0.321975275429689,
0.333333333333333,0.321975275429689,0.333333333333333,0.321975275429689,
0.333333333333333,0.321975275429689,0.333333333333333,0.321975275429689,
0.333333333333333,0.321975275429689,0.333333333333333,0.321975275429689,
0.333333333333333,0.321975275429689,0.333333333333333,0.321975275429689,
0.333333333333333,0.321975275429689,0.333333333333333,0.321975275429689,
0.333333333333333,0.321975275429689,0.333333333333333,0.321975275429689,
0.333333333333333,0.321975275429689,0.333333333333333,0.321975275429689,
0.333333333333333,0.321975275429689,0.333333333333333,0.321975275429689,
0.333333333333333,0.321975275429689,0.333333333333333,0.321975275429689,
0.333333333333333,0.321975275429689,0.333333333333333,0.321975275429689,
0.333333333333333,0.321975275429689,0.333333333333333,0.321975275429689,
0.333333333333333,0.321975275429689,0.333333333333333,0.321975275429689,
0.333333333333333,0.321975275429689,0.333333333333333,0.321975275429689,
0.333333333333333,0.321975275429689,0.333333333333333),(0.333333333333333,
0.321975275429689,0.333333333333333,0.321975275429689,0.333333333333333,
0.321975275429689,0.333333333333333,0.321975275429689,0.333333333333333,
0.321975275429689,0.333333333333333,0.321975275429689,0.333333333333333,
0.321975275429689,0.333333333333333,0.321975275429689,0.333333333333333,
0.321975275429689,0.333333333333333,0.321975275429689,0.333333333333333,
0.321975275429689,0.333333333333333,0.321975275429689,0.333333333333333,
0.321975275429689,0.333333333333333,0.321975275429689,0.333333333333333,
0.321975275429689,0.333333333333333,0.321975275429689,0.333333333333333,
0.321975275429689,0.333333333333333,0.321975275429689,0.333333333333333,
0.321975275429689,0.333333333333333,0.321975275429689,0.333333333333333,
0.321975275429689,0.333333333333333,0.321975275429689,0.333333333333333,
0.321975275429689,0.333333333333333,0.321975275429689,0.333333333333333,
0.321975275429689,0.333333333333333,0.321975275429689,0.333333333333333,
0.321975275429689,0.333333333333333,0.321975275429689,0.333333333333333,
0.321975275429689,0.333333333333333,0.321975275429689,0.333333333333333,
0.321975275429689,0.333333333333333,0.321975275429689,0.333333333333333,
0.321975275429689,0.333333333333333,0.321975275429689,0.333333333333333,
0.321975275429689,0.333333333333333,0.321975275429689,0.333333333333333,
0.321975275429689,0.333333333333333,0.321975275429689,0.333333333333333,
0.321975275429689,0.333333333333333,0.321975275429689,0.333333333333333,
0.321975275429689,0.333333333333333,0.321975275429689,0.333333333333333,
0.321975275429689,0.333333333333333,0.321975275429689,0.333333333333333,
0.321975275429689,0.333333333333333,0.321975275429689,0.333333333333333,
0.321975275429689,0.333333333333333,0.321975275429689,0.333333333333333,
0.321975275429689,0.333333333333333,0.321975275429689,0.333333333333333,
0.321975275429689,0.333333333333333,0.321975275429689,0.333333333333333,
0.321975275429689,0.333333333333333,0.321975275429689,0.333333333333333,
0.321975275429689,0.333333333333333,0.321975275429689,0.333333333333333,
0.321975275429689,0.333333333333333,0.321975275429689,0.333333333333333,
0.321975275429689,0.333333333333333,0.321975275429689,0.333333333333333,
0.321975275429689,0.333333333333333,0.321975275429689,0.333333333333333,
0.321975275429689,0.333333333333333,0.321975275429689,0.333333333333333,
0.321975275429689,0.333333333333333,0.321975275429689,0.333333333333333,
0.321975275429689,0.333333333333333,0.321975275429689,0.333333333333333,
0.321975275429689,0.333333333333333,0.321975275429689,0.333333333333333,
0.321975275429689,0.333333333333333,0.321975275429689,0.333333333333333,
0.321975275429689,0.333333333333333,0.321975275429689,0.333333333333333,
0.321975275429689,0.333333333333333,0.321975275429689,0.333333333333333,
0.321975275429689,0.333333333333333,0.321975275429689,0.333333333333333,
0.321975275429689,0.333333333333333,0.321975275429689,0.333333333333333,
0.321975275429689,0.333333333333333,0.321975275429689,0.333333333333333,
0.321975275429689,0.333333333333333,0.321975275429689,0.333333333333333,
0.321975275429689,0.333333333333333,0.321975275429689,0.333333333333333,
0.321975275429689,0.333333333333333,0.321975275429689,0.333333333333333,
0.321975275429689,0.333333333333333,0.321975275429689,0.333333333333333,
0.321975275429689,0.333333333333333,0.321975275429689,0.333333333333333,
0.321975275429689,0.333333333333333,0.321975275429689,0.333333333333333,
0.321975275429689,0.333333333333333,0.321975275429689,0.333333333333333),
(1.,0.965925826289068,1.,0.965925826289068,1.,0.965925826289068,1.,0.965925826289068,
1.,0.965925826289068,1.,0.965925826289068,1.,0.965925826289068,1.,0.965925826289068,
1.,0.965925826289068,1.,0.965925826289068,1.,0.965925826289068,1.,0.965925826289068,
1.,0.965925826289068,1.,0.965925826289068,1.,0.965925826289068,1.,0.965925826289068,
1.,0.965925826289068,1.,0.965925826289068,1.,0.965925826289068,1.,0.965925826289068,
1.,0.965925826289068,1.,0.965925826289068,1.,0.965925826289068,1.,0.965925826289068,
1.,0.965925826289068,1.,0.965925826289068,1.,0.965925826289068,1.,0.965925826289068,
1.,0.965925826289068,1.,0.965925826289068,1.,0.965925826289068,1.,0.965925826289068,
1.,0.965925826289068,1.,0.965925826289068,1.,0.965925826289068,1.,0.965925826289068,
1.,0.965925826289068,1.,0.965925826289068,1.,0.965925826289068,1.,0.965925826289068,
1.,0.965925826289068,1.,0.965925826289068,1.,0.965925826289068,1.,0.965925826289068,
1.,0.965925826289068,1.,0.965925826289068,1.,0.965925826289068,1.,0.965925826289068,
1.,0.965925826289068,1.,0.965925826289068,1.,0.965925826289068,1.,0.965925826289068,
1.,0.965925826289068,1.,0.965925826289068,1.,0.965925826289068,1.,0.965925826289068,
1.,0.965925826289068,1.,0.965925826289068,1.,0.965925826289068,1.,0.965925826289068,
1.,0.965925826289068,1.,0.965925826289068,1.,0.965925826289068,1.,0.965925826289068,
1.,0.965925826289068,1.,0.965925826289068,1.,0.965925826289068,1.,0.965925826289068,
1.,0.965925826289068,1.,0.965925826289068,1.,0.965925826289068,1.,0.965925826289068,
1.,0.965925826289068,1.,0.965925826289068,1.,0.965925826289068,1.,0.965925826289068,
1.,0.965925826289068,1.,0.965925826289068,1.,0.965925826289068,1.,0.965925826289068,
1.,0.965925826289068,1.,0.965925826289068,1.,0.965925826289068,1.,0.965925826289068,
1.,0.965925826289068,1.,0.965925826289068,1.,0.965925826289068,1.,0.965925826289068,
1.,0.965925826289068,1.,0.965925826289068,1.,0.965925826289068,1.,0.965925826289068,
1.,0.965925826289068,1.,0.965925826289068,1.,0.965925826289068,1.,0.965925826289068,
1.),(0.333333333333333,0.321975275429689,0.333333333333333,0.321975275429689,
0.333333333333333,0.321975275429689,0.333333333333333,0.321975275429689,
0.333333333333333,0.321975275429689,0.333333333333333,0.321975275429689,
0.333333333333333,0.321975275429689,0.333333333333333,0.321975275429689,
0.333333333333333,0.321975275429689,0.333333333333333,0.321975275429689,
0.333333333333333,0.321975275429689,0.333333333333333,0.321975275429689,
0.333333333333333,0.321975275429689,0.333333333333333,0.321975275429689,
0.333333333333333,0.321975275429689,0.333333333333333,0.321975275429689,
0.333333333333333,0.321975275429689,0.333333333333333,0.321975275429689,
0.333333333333333,0.321975275429689,0.333333333333333,0.321975275429689,
0.333333333333333,0.321975275429689,0.333333333333333,0.321975275429689,
0.333333333333333,0.321975275429689,0.333333333333333,0.321975275429689,
0.333333333333333,0.321975275429689,0.333333333333333,0.321975275429689,
0.333333333333333,0.321975275429689,0.333333333333333,0.321975275429689,
0.333333333333333,0.321975275429689,0.333333333333333,0.321975275429689,
0.333333333333333,0.321975275429689,0.333333333333333,0.321975275429689,
0.333333333333333,0.321975275429689,0.333333333333333,0.321975275429689,
0.333333333333333,0.321975275429689,0.333333333333333,0.321975275429689,
0.333333333333333,0.321975275429689,0.333333333333333,0.321975275429689,
0.333333333333333,0.321975275429689,0.333333333333333,0.321975275429689,
0.333333333333333,0.321975275429689,0.333333333333333,0.321975275429689,
0.333333333333333,0.321975275429689,0.333333333333333,0.321975275429689,
0.333333333333333,0.321975275429689,0.333333333333333,0.321975275429689,
0.333333333333333,0.321975275429689,0.333333333333333,0.321975275429689,
0.333333333333333,0.321975275429689,0.333333333333333,0.321975275429689,
0.333333333333333,0.321975275429689,0.333333333333333,0.321975275429689,
0.333333333333333,0.321975275429689,0.333333333333333,0.321975275429689,
0.333333333333333,0.321975275429689,0.333333333333333,0.321975275429689,
0.333333333333333,0.321975275429689,0.333333333333333,0.321975275429689,
0.333333333333333,0.321975275429689,0.333333333333333,0.321975275429689,
0.333333333333333,0.321975275429689,0.333333333333333,0.321975275429689,
0.333333333333333,0.321975275429689,0.333333333333333,0.321975275429689,
0.333333333333333,0.321975275429689,0.333333333333333,0.321975275429689,
0.333333333333333,0.321975275429689,0.333333333333333,0.321975275429689,
0.333333333333333,0.321975275429689,0.333333333333333,0.321975275429689,
0.333333333333333,0.321975275429689,0.333333333333333,0.321975275429689,
0.333333333333333,0.321975275429689,0.333333333333333,0.321975275429689,
0.333333333333333,0.321975275429689,0.333333333333333,0.321975275429689,
0.333333333333333,0.321975275429689,0.333333333333333,0.321975275429689,
0.333333333333333,0.321975275429689,0.333333333333333,0.321975275429689,
0.333333333333333,0.321975275429689,0.333333333333333,0.321975275429689,
0.333333333333333,0.321975275429689,0.333333333333333,0.321975275429689,
0.333333333333333,0.321975275429689,0.333333333333333,0.321975275429689,
0.333333333333333,0.321975275429689,0.333333333333333,0.321975275429689,
0.333333333333333,0.321975275429689,0.333333333333333,0.321975275429689,
0.333333333333333,0.321975275429689,0.333333333333333,0.321975275429689,
0.333333333333333,0.321975275429689,0.333333333333333,0.321975275429689,
0.333333333333333,0.321975275429689,0.333333333333333,0.321975275429689,
0.333333333333333),(0.333333333333333,0.321975275429689,0.333333333333333,
0.321975275429689,0.333333333333333,0.321975275429689,0.333333333333333,
0.321975275429689,0.333333333333333,0.321975275429689,0.333333333333333,
0.321975275429689,0.333333333333333,0.321975275429689,0.333333333333333,
0.321975275429689,0.333333333333333,0.321975275429689,0.333333333333333,
0.321975275429689,0.333333333333333,0.321975275429689,0.333333333333333,
0.321975275429689,0.333333333333333,0.321975275429689,0.333333333333333,
0.321975275429689,0.333333333333333,0.321975275429689,0.333333333333333,
0.321975275429689,0.333333333333333,0.321975275429689,0.333333333333333,
0.321975275429689,0.333333333333333,0.321975275429689,0.333333333333333,
0.321975275429689,0.333333333333333,0.321975275429689,0.333333333333333,
0.321975275429689,0.333333333333333,0.321975275429689,0.333333333333333,
0.321975275429689,0.333333333333333,0.321975275429689,0.333333333333333,
0.321975275429689,0.333333333333333,0.321975275429689,0.333333333333333,
0.321975275429689,0.333333333333333,0.321975275429689,0.333333333333333,
0.321975275429689,0.333333333333333,0.321975275429689,0.333333333333333,
0.321975275429689,0.333333333333333,0.321975275429689,0.333333333333333,
0.321975275429689,0.333333333333333,0.321975275429689,0.333333333333333,
0.321975275429689,0.333333333333333,0.321975275429689,0.333333333333333,
0.321975275429689,0.333333333333333,0.321975275429689,0.333333333333333,
0.321975275429689,0.333333333333333,0.321975275429689,0.333333333333333,
0.321975275429689,0.333333333333333,0.321975275429689,0.333333333333333,
0.321975275429689,0.333333333333333,0.321975275429689,0.333333333333333,
0.321975275429689,0.333333333333333,0.321975275429689,0.333333333333333,
0.321975275429689,0.333333333333333,0.321975275429689,0.333333333333333,
0.321975275429689,0.333333333333333,0.321975275429689,0.333333333333333,
0.321975275429689,0.333333333333333,0.321975275429689,0.333333333333333,
0.321975275429689,0.333333333333333,0.321975275429689,0.333333333333333,
0.321975275429689,0.333333333333333,0.321975275429689,0.333333333333333,
0.321975275429689,0.333333333333333,0.321975275429689,0.333333333333333,
0.321975275429689,0.333333333333333,0.321975275429689,0.333333333333333,
0.321975275429689,0.333333333333333,0.321975275429689,0.333333333333333,
0.321975275429689,0.333333333333333,0.321975275429689,0.333333333333333,
0.321975275429689,0.333333333333333,0.321975275429689,0.333333333333333,
0.321975275429689,0.333333333333333,0.321975275429689,0.333333333333333,
0.321975275429689,0.333333333333333,0.321975275429689,0.333333333333333,
0.321975275429689,0.333333333333333,0.321975275429689,0.333333333333333,
0.321975275429689,0.333333333333333,0.321975275429689,0.333333333333333,
0.321975275429689,0.333333333333333,0.321975275429689,0.333333333333333,
0.321975275429689,0.333333333333333,0.321975275429689,0.333333333333333,
0.321975275429689,0.333333333333333,0.321975275429689,0.333333333333333,
0.321975275429689,0.333333333333333,0.321975275429689,0.333333333333333,
0.321975275429689,0.333333333333333,0.321975275429689,0.333333333333333,
0.321975275429689,0.333333333333333,0.321975275429689,0.333333333333333,
0.321975275429689,0.333333333333333,0.321975275429689,0.333333333333333,
0.321975275429689,0.333333333333333,0.321975275429689,0.333333333333333,
0.321975275429689,0.333333333333333,0.321975275429689,0.333333333333333,
0.321975275429689,0.333333333333333,0.321975275429689,0.333333333333333,
0.321975275429689,0.333333333333333),(1.,0.965925826289068,1.,0.965925826289068,
1.,0.965925826289068,1.,0.965925826289068,1.,0.965925826289068,1.,0.965925826289068,
1.,0.965925826289068,1.,0.965925826289068,1.,0.965925826289068,1.,0.965925826289068,
1.,0.965925826289068,1.,0.965925826289068,1.,0.965925826289068,1.,0.965925826289068,
1.,0.965925826289068,1.,0.965925826289068,1.,0.965925826289068,1.,0.965925826289068,
1.,0.965925826289068,1.,0.965925826289068,1.,0.965925826289068,1.,0.965925826289068,
1.,0.965925826289068,1.,0.965925826289068,1.,0.965925826289068,1.,0.965925826289068,
1.,0.965925826289068,1.,0.965925826289068,1.,0.965925826289068,1.,0.965925826289068,
1.,0.965925826289068,1.,0.965925826289068,1.,0.965925826289068,1.,0.965925826289068,
1.,0.965925826289068,1.,0.965925826289068,1.,0.965925826289068,1.,0.965925826289068,
1.,0.965925826289068,1.,0.965925826289068,1.,0.965925826289068,1.,0.965925826289068,
1.,0.965925826289068,1.,0.965925826289068,1.,0.965925826289068,1.,0.965925826289068,
1.,0.965925826289068,1.,0.965925826289068,1.,0.965925826289068,1.,0.965925826289068,
1.,0.965925826289068,1.,0.965925826289068,1.,0.965925826289068,1.,0.965925826289068,
1.,0.965925826289068,1.,0.965925826289068,1.,0.965925826289068,1.,0.965925826289068,
1.,0.965925826289068,1.,0.965925826289068,1.,0.965925826289068,1.,0.965925826289068,
1.,0.965925826289068,1.,0.965925826289068,1.,0.965925826289068,1.,0.965925826289068,
1.,0.965925826289068,1.,0.965925826289068,1.,0.965925826289068,1.,0.965925826289068,
1.,0.965925826289068,1.,0.965925826289068,1.,0.965925826289068,1.,0.965925826289068,
1.,0.965925826289068,1.,0.965925826289068,1.,0.965925826289068,1.,0.965925826289068,
1.,0.965925826289068,1.,0.965925826289068,1.,0.965925826289068,1.,0.965925826289068,
1.,0.965925826289068,1.,0.965925826289068,1.,0.965925826289068,1.,0.965925826289068,
1.,0.965925826289068,1.,0.965925826289068,1.,0.965925826289068,1.,0.965925826289068,
1.,0.965925826289068,1.,0.965925826289068,1.,0.965925826289068,1.,0.965925826289068,
1.,0.965925826289068,1.,0.965925826289068,1.)))
REPRESENTATION_ITEM('')
SURFACE()
);
#19=(
BOUNDED_SURFACE()
B_SPLINE_SURFACE(3,3,((#11307,#11308,#11309,#11310,#11311,#11312,#11313,
#11314,#11315,#11316,#11317,#11318,#11319,#11320,#11321,#11322,#11323,#11324,
#11325,#11326,#11327,#11328,#11329,#11330,#11331,#11332,#11333,#11334,#11335,
#11336,#11337,#11338,#11339,#11340,#11341,#11342,#11343,#11344,#11345,#11346),
(#11347,#11348,#11349,#11350,#11351,#11352,#11353,#11354,#11355,#11356,
#11357,#11358,#11359,#11360,#11361,#11362,#11363,#11364,#11365,#11366,#11367,
#11368,#11369,#11370,#11371,#11372,#11373,#11374,#11375,#11376,#11377,#11378,
#11379,#11380,#11381,#11382,#11383,#11384,#11385,#11386),(#11387,#11388,
#11389,#11390,#11391,#11392,#11393,#11394,#11395,#11396,#11397,#11398,#11399,
#11400,#11401,#11402,#11403,#11404,#11405,#11406,#11407,#11408,#11409,#11410,
#11411,#11412,#11413,#11414,#11415,#11416,#11417,#11418,#11419,#11420,#11421,
#11422,#11423,#11424,#11425,#11426),(#11427,#11428,#11429,#11430,#11431,
#11432,#11433,#11434,#11435,#11436,#11437,#11438,#11439,#11440,#11441,#11442,
#11443,#11444,#11445,#11446,#11447,#11448,#11449,#11450,#11451,#11452,#11453,
#11454,#11455,#11456,#11457,#11458,#11459,#11460,#11461,#11462,#11463,#11464,
#11465,#11466),(#11467,#11468,#11469,#11470,#11471,#11472,#11473,#11474,
#11475,#11476,#11477,#11478,#11479,#11480,#11481,#11482,#11483,#11484,#11485,
#11486,#11487,#11488,#11489,#11490,#11491,#11492,#11493,#11494,#11495,#11496,
#11497,#11498,#11499,#11500,#11501,#11502,#11503,#11504,#11505,#11506),
(#11507,#11508,#11509,#11510,#11511,#11512,#11513,#11514,#11515,#11516,
#11517,#11518,#11519,#11520,#11521,#11522,#11523,#11524,#11525,#11526,#11527,
#11528,#11529,#11530,#11531,#11532,#11533,#11534,#11535,#11536,#11537,#11538,
#11539,#11540,#11541,#11542,#11543,#11544,#11545,#11546),(#11547,#11548,
#11549,#11550,#11551,#11552,#11553,#11554,#11555,#11556,#11557,#11558,#11559,
#11560,#11561,#11562,#11563,#11564,#11565,#11566,#11567,#11568,#11569,#11570,
#11571,#11572,#11573,#11574,#11575,#11576,#11577,#11578,#11579,#11580,#11581,
#11582,#11583,#11584,#11585,#11586)),.UNSPECIFIED.,.T.,.F.,.F.)
B_SPLINE_SURFACE_WITH_KNOTS((4,3,4),(4,2,2,2,2,2,2,2,2,2,2,2,2,2,2,2,2,
2,2,4),(0.,0.5,1.),(-2.95233260527408E-7,0.0437517296050676,0.0875034592101352,
0.131255188815203,0.17500691842027,0.196882783222804,0.218758648025338,
0.262510377630406,0.350013836840541,0.418185084306465,0.486356331772389,
0.554527579238313,0.622698826704237,0.669861473366207,0.717024120028178,
0.811349413352118,0.858512060014089,0.905674706676059,0.95283735333803,
1.),.UNSPECIFIED.)
GEOMETRIC_REPRESENTATION_ITEM()
RATIONAL_B_SPLINE_SURFACE(((1.,1.,1.,1.,1.,1.,1.,1.,1.,1.,1.,1.,1.,1.,1.,
1.,1.,1.,1.,1.,1.,1.,1.,1.,1.,1.,1.,1.,1.,1.,1.,1.,1.,1.,1.,1.,1.,1.,1.,
1.),(0.333333333333334,0.333333333333333,0.333333333333333,0.333333333333333,
0.333333333333333,0.333333333333333,0.333333333333333,0.333333333333333,
0.333333333333333,0.333333333333333,0.333333333333333,0.333333333333333,
0.333333333333333,0.333333333333333,0.333333333333333,0.333333333333333,
0.333333333333333,0.333333333333333,0.333333333333333,0.333333333333333,
0.333333333333333,0.333333333333333,0.333333333333333,0.333333333333333,
0.333333333333333,0.333333333333333,0.333333333333333,0.333333333333333,
0.333333333333333,0.333333333333333,0.333333333333333,0.333333333333333,
0.333333333333333,0.333333333333333,0.333333333333333,0.333333333333333,
0.333333333333333,0.333333333333333,0.333333333333333,0.333333333333333),
(0.333333333333334,0.333333333333333,0.333333333333333,0.333333333333333,
0.333333333333333,0.333333333333333,0.333333333333333,0.333333333333333,
0.333333333333333,0.333333333333333,0.333333333333333,0.333333333333333,
0.333333333333333,0.333333333333333,0.333333333333333,0.333333333333333,
0.333333333333333,0.333333333333333,0.333333333333333,0.333333333333333,
0.333333333333333,0.333333333333333,0.333333333333333,0.333333333333333,
0.333333333333333,0.333333333333333,0.333333333333333,0.333333333333333,
0.333333333333333,0.333333333333333,0.333333333333333,0.333333333333333,
0.333333333333333,0.333333333333333,0.333333333333333,0.333333333333333,
0.333333333333333,0.333333333333333,0.333333333333333,0.333333333333333),
(1.,1.,1.,1.,1.,1.,1.,1.,1.,1.,1.,1.,1.,1.,1.,1.,1.,1.,1.,1.,1.,1.,1.,1.,
1.,1.,1.,1.,1.,1.,1.,1.,1.,1.,1.,1.,1.,1.,1.,1.),(0.333333333333334,0.333333333333333,
0.333333333333333,0.333333333333333,0.333333333333333,0.333333333333333,
0.333333333333333,0.333333333333333,0.333333333333333,0.333333333333333,
0.333333333333333,0.333333333333333,0.333333333333333,0.333333333333333,
0.333333333333333,0.333333333333333,0.333333333333333,0.333333333333333,
0.333333333333333,0.333333333333333,0.333333333333333,0.333333333333333,
0.333333333333333,0.333333333333333,0.333333333333333,0.333333333333333,
0.333333333333333,0.333333333333333,0.333333333333333,0.333333333333333,
0.333333333333333,0.333333333333333,0.333333333333333,0.333333333333333,
0.333333333333333,0.333333333333333,0.333333333333333,0.333333333333333,
0.333333333333333,0.333333333333333),(0.333333333333334,0.333333333333333,
0.333333333333333,0.333333333333333,0.333333333333333,0.333333333333333,
0.333333333333333,0.333333333333333,0.333333333333333,0.333333333333333,
0.333333333333333,0.333333333333333,0.333333333333333,0.333333333333333,
0.333333333333333,0.333333333333333,0.333333333333333,0.333333333333333,
0.333333333333333,0.333333333333333,0.333333333333333,0.333333333333333,
0.333333333333333,0.333333333333333,0.333333333333333,0.333333333333333,
0.333333333333333,0.333333333333333,0.333333333333333,0.333333333333333,
0.333333333333333,0.333333333333333,0.333333333333333,0.333333333333333,
0.333333333333333,0.333333333333333,0.333333333333333,0.333333333333333,
0.333333333333333,0.333333333333333),(1.,1.,1.,1.,1.,1.,1.,1.,1.,1.,1.,
1.,1.,1.,1.,1.,1.,1.,1.,1.,1.,1.,1.,1.,1.,1.,1.,1.,1.,1.,1.,1.,1.,1.,1.,
1.,1.,1.,1.,1.)))
REPRESENTATION_ITEM('')
SURFACE()
);
#20=(
BOUNDED_SURFACE()
B_SPLINE_SURFACE(3,3,((#11593,#11594,#11595,#11596,#11597,#11598,#11599,
#11600,#11601,#11602,#11603,#11604),(#11605,#11606,#11607,#11608,#11609,
#11610,#11611,#11612,#11613,#11614,#11615,#11616),(#11617,#11618,#11619,
#11620,#11621,#11622,#11623,#11624,#11625,#11626,#11627,#11628),(#11629,
#11630,#11631,#11632,#11633,#11634,#11635,#11636,#11637,#11638,#11639,#11640),
(#11641,#11642,#11643,#11644,#11645,#11646,#11647,#11648,#11649,#11650,
#11651,#11652),(#11653,#11654,#11655,#11656,#11657,#11658,#11659,#11660,
#11661,#11662,#11663,#11664),(#11665,#11666,#11667,#11668,#11669,#11670,
#11671,#11672,#11673,#11674,#11675,#11676)),.UNSPECIFIED.,.T.,.F.,.F.)
B_SPLINE_SURFACE_WITH_KNOTS((4,3,4),(4,2,2,2,2,4),(0.,0.5,1.),(0.727251200985696,
0.761344800862484,0.795438400739272,0.863625600492848,0.931812800246424,
1.),.UNSPECIFIED.)
GEOMETRIC_REPRESENTATION_ITEM()
RATIONAL_B_SPLINE_SURFACE(((1.,1.,1.,1.,1.,1.,1.,1.,1.,1.,1.,1.),(0.333333333333333,
0.333333333333333,0.333333333333333,0.333333333333333,0.333333333333333,
0.333333333333333,0.333333333333333,0.333333333333333,0.333333333333333,
0.333333333333333,0.333333333333333,0.333333333333333),(0.333333333333333,
0.333333333333333,0.333333333333333,0.333333333333333,0.333333333333333,
0.333333333333333,0.333333333333333,0.333333333333333,0.333333333333333,
0.333333333333333,0.333333333333333,0.333333333333333),(1.,1.,1.,1.,1.,
1.,1.,1.,1.,1.,1.,1.),(0.333333333333333,0.333333333333333,0.333333333333333,
0.333333333333333,0.333333333333333,0.333333333333333,0.333333333333333,
0.333333333333333,0.333333333333333,0.333333333333333,0.333333333333333,
0.333333333333333),(0.333333333333333,0.333333333333333,0.333333333333333,
0.333333333333333,0.333333333333333,0.333333333333333,0.333333333333333,
0.333333333333333,0.333333333333333,0.333333333333333,0.333333333333333,
0.333333333333333),(1.,1.,1.,1.,1.,1.,1.,1.,1.,1.,1.,1.)))
REPRESENTATION_ITEM('')
SURFACE()
);
#121=B_SPLINE_CURVE_WITH_KNOTS('',3,(#5366,#5367,#5368,#5369,#5370,#5371,
#5372,#5373,#5374,#5375,#5376,#5377),.UNSPECIFIED.,.F.,.F.,(4,2,2,2,2,4),
(0.727251200985696,0.761344800862484,0.795438400739272,0.863625600492848,
0.931812800246424,0.997527670949997),.UNSPECIFIED.);
#122=B_SPLINE_CURVE_WITH_KNOTS('',3,(#5382,#5383,#5384,#5385,#5386,#5387,
#5388,#5389,#5390,#5391,#5392,#5393),.UNSPECIFIED.,.F.,.F.,(4,2,2,2,2,4),
(0.727251200985696,0.761344800862484,0.795438400739272,0.863625600492848,
0.931812800246424,1.),.UNSPECIFIED.);
#123=B_SPLINE_CURVE_WITH_KNOTS('',3,(#5676,#5677,#5678,#5679,#5680,#5681,
#5682,#5683,#5684,#5685,#5686,#5687,#5688,#5689,#5690,#5691,#5692,#5693,
#5694,#5695,#5696,#5697,#5698,#5699),.UNSPECIFIED.,.F.,.F.,(4,2,2,2,2,2,
2,2,2,2,2,4),(-0.0558533803830892,-0.0554200089354374,-0.0551962315488395,
-0.0547444182972245,-0.0538796394902973,-0.0521571275021974,-0.0487120777231514,
-0.041906416333374,-0.0288960116062435,-0.0178108635562527,-0.00795577739213343,
-1.45747604985572E-5),.UNSPECIFIED.);
#124=B_SPLINE_CURVE_WITH_KNOTS('',3,(#5701,#5702,#5703,#5704,#5705,#5706,
#5707,#5708,#5709,#5710,#5711,#5712,#5713,#5714,#5715,#5716,#5717,#5718,
#5719,#5720,#5721,#5722,#5723,#5724,#5725,#5726,#5727,#5728,#5729,#5730,
#5731,#5732,#5733,#5734,#5735,#5736,#5737,#5738,#5739,#5740,#5741,#5742,
#5743,#5744,#5745,#5746),.UNSPECIFIED.,.F.,.F.,(4,2,2,2,2,2,2,2,2,2,2,2,
2,2,2,2,2,2,2,2,2,2,4),(0.00725097420749211,0.0166371724554133,0.0261818111535564,
0.0359748592316744,0.0437517296050677,0.0875034592101353,0.131255188815203,
0.175006918420271,0.196882783222805,0.218758648025338,0.262510377630406,
0.350013836840541,0.418185084306466,0.48635633177239,0.554527579238314,
0.622698826704238,0.669861473366208,0.717024120028179,0.81134941335212,
0.85851206001409,0.905674706676061,0.952837353338031,1.),.UNSPECIFIED.);
#125=B_SPLINE_CURVE_WITH_KNOTS('',3,(#5750,#5751,#5752,#5753,#5754,#5755,
#5756,#5757,#5758,#5759,#5760,#5761,#5762,#5763,#5764,#5765,#5766,#5767,
#5768,#5769,#5770,#5771,#5772,#5773,#5774,#5775,#5776,#5777,#5778,#5779,
#5780,#5781,#5782,#5783,#5784,#5785,#5786,#5787,#5788,#5789),
 .UNSPECIFIED.,.F.,.F.,(4,2,2,2,2,2,2,2,2,2,2,2,2,2,2,2,2,2,2,4),(0.,0.0437517296050676,
0.0875034592101352,0.131255188815203,0.17500691842027,0.196882783222804,
0.218758648025338,0.262510377630406,0.350013836840541,0.418185084306465,
0.486356331772389,0.554527579238313,0.622698826704237,0.669861473366207,
0.717024120028178,0.811349413352118,0.858512060014089,0.905674706676059,
0.95283735333803,1.),.UNSPECIFIED.);
#126=B_SPLINE_CURVE_WITH_KNOTS('',3,(#7920,#7921,#7922,#7923,#7924,#7925,
#7926,#7927,#7928,#7929,#7930,#7931,#7932,#7933,#7934,#7935,#7936,#7937,
#7938,#7939,#7940,#7941,#7942,#7943,#7944,#7945,#7946,#7947,#7948,#7949,
#7950,#7951,#7952,#7953,#7954,#7955,#7956,#7957,#7958,#7959,#7960,#7961,
#7962,#7963,#7964,#7965,#7966,#7967,#7968,#7969,#7970,#7971,#7972,#7973,
#7974,#7975,#7976,#7977,#7978,#7979,#7980,#7981,#7982,#7983,#7984,#7985,
#7986,#7987,#7988,#7989,#7990,#7991,#7992,#7993,#7994,#7995,#7996,#7997,
#7998,#7999,#8000,#8001,#8002,#8003,#8004,#8005,#8006,#8007,#8008,#8009,
#8010,#8011,#8012,#8013,#8014,#8015,#8016,#8017,#8018,#8019,#8020,#8021,
#8022,#8023,#8024,#8025,#8026,#8027,#8028,#8029,#8030,#8031,#8032,#8033,
#8034,#8035,#8036,#8037,#8038,#8039,#8040,#8041,#8042,#8043,#8044,#8045,
#8046,#8047,#8048,#8049,#8050,#8051,#8052,#8053,#8054,#8055,#8056,#8057,
#8058,#8059,#8060,#8061,#8062,#8063,#8064,#8065,#8066,#8067,#8068,#8069,
#8070,#8071,#8072,#8073,#8074,#8075,#8076,#8077,#8078,#8079,#8080,#8081,
#8082,#8083,#8084,#8085,#8086,#8087,#8088,#8089,#8090,#8091,#8092,#8093,
#8094,#8095,#8096,#8097,#8098,#8099,#8100,#8101,#8102,#8103,#8104,#8105,
#8106,#8107,#8108,#8109,#8110,#8111,#8112,#8113,#8114,#8115,#8116,#8117,
#8118,#8119,#8120,#8121,#8122,#8123,#8124,#8125,#8126,#8127,#8128,#8129,
#8130,#8131,#8132,#8133,#8134,#8135,#8136,#8137,#8138,#8139,#8140,#8141,
#8142,#8143,#8144,#8145,#8146,#8147,#8148,#8149,#8150,#8151,#8152,#8153,
#8154,#8155,#8156,#8157,#8158,#8159,#8160,#8161,#8162,#8163,#8164,#8165,
#8166,#8167,#8168,#8169,#8170,#8171,#8172,#8173,#8174,#8175,#8176,#8177,
#8178,#8179,#8180,#8181,#8182,#8183,#8184,#8185,#8186,#8187,#8188,#8189,
#8190,#8191,#8192,#8193,#8194,#8195,#8196,#8197,#8198,#8199,#8200,#8201,
#8202,#8203,#8204,#8205,#8206,#8207,#8208,#8209,#8210,#8211,#8212,#8213,
#8214,#8215,#8216,#8217,#8218,#8219,#8220,#8221,#8222,#8223,#8224,#8225,
#8226,#8227,#8228,#8229,#8230,#8231,#8232,#8233,#8234,#8235,#8236,#8237,
#8238,#8239,#8240,#8241,#8242,#8243,#8244,#8245,#8246,#8247,#8248,#8249,
#8250,#8251,#8252,#8253,#8254,#8255,#8256,#8257,#8258,#8259,#8260,#8261,
#8262,#8263,#8264,#8265,#8266,#8267,#8268,#8269,#8270,#8271,#8272,#8273,
#8274,#8275,#8276,#8277,#8278,#8279,#8280,#8281,#8282,#8283,#8284,#8285,
#8286,#8287,#8288,#8289,#8290,#8291,#8292,#8293,#8294,#8295,#8296,#8297,
#8298,#8299,#8300,#8301,#8302,#8303,#8304,#8305,#8306,#8307,#8308,#8309,
#8310,#8311,#8312,#8313,#8314,#8315,#8316,#8317,#8318,#8319,#8320,#8321,
#8322,#8323,#8324,#8325,#8326,#8327,#8328,#8329,#8330,#8331,#8332,#8333,
#8334,#8335,#8336,#8337,#8338,#8339,#8340,#8341,#8342,#8343,#8344,#8345,
#8346,#8347,#8348,#8349,#8350,#8351,#8352,#8353,#8354,#8355,#8356,#8357,
#8358,#8359,#8360,#8361,#8362,#8363,#8364,#8365,#8366,#8367,#8368,#8369,
#8370,#8371,#8372,#8373,#8374,#8375,#8376,#8377,#8378,#8379,#8380,#8381,
#8382,#8383,#8384,#8385,#8386,#8387,#8388,#8389,#8390,#8391,#8392,#8393,
#8394,#8395,#8396,#8397,#8398,#8399,#8400,#8401,#8402,#8403,#8404,#8405,
#8406,#8407,#8408,#8409,#8410,#8411,#8412,#8413,#8414,#8415,#8416,#8417,
#8418,#8419,#8420,#8421,#8422,#8423,#8424,#8425,#8426,#8427,#8428,#8429,
#8430,#8431,#8432,#8433,#8434,#8435,#8436,#8437,#8438,#8439,#8440,#8441,
#8442,#8443,#8444,#8445,#8446,#8447,#8448,#8449,#8450,#8451,#8452,#8453,
#8454,#8455,#8456,#8457,#8458,#8459,#8460,#8461,#8462,#8463,#8464,#8465,
#8466,#8467,#8468,#8469,#8470,#8471,#8472,#8473,#8474,#8475,#8476,#8477,
#8478,#8479,#8480,#8481,#8482,#8483,#8484,#8485,#8486,#8487,#8488,#8489,
#8490,#8491,#8492,#8493,#8494,#8495,#8496,#8497,#8498,#8499,#8500,#8501,
#8502,#8503,#8504,#8505,#8506,#8507,#8508,#8509,#8510,#8511,#8512,#8513,
#8514,#8515,#8516,#8517,#8518,#8519,#8520,#8521,#8522,#8523,#8524,#8525,
#8526,#8527,#8528,#8529,#8530,#8531,#8532,#8533,#8534,#8535,#8536,#8537,
#8538,#8539,#8540,#8541,#8542,#8543,#8544,#8545,#8546,#8547,#8548,#8549,
#8550,#8551,#8552,#8553,#8554,#8555,#8556,#8557,#8558,#8559,#8560,#8561,
#8562,#8563,#8564,#8565,#8566,#8567,#8568,#8569,#8570,#8571,#8572,#8573,
#8574,#8575,#8576,#8577,#8578,#8579,#8580,#8581,#8582,#8583,#8584,#8585,
#8586,#8587,#8588,#8589,#8590,#8591,#8592,#8593,#8594,#8595,#8596,#8597,
#8598,#8599,#8600,#8601,#8602,#8603,#8604,#8605,#8606,#8607,#8608,#8609,
#8610,#8611,#8612,#8613,#8614,#8615,#8616,#8617,#8618,#8619,#8620,#8621,
#8622,#8623,#8624,#8625,#8626,#8627,#8628,#8629,#8630,#8631,#8632,#8633,
#8634,#8635,#8636,#8637,#8638,#8639,#8640,#8641,#8642,#8643,#8644,#8645,
#8646,#8647,#8648,#8649,#8650,#8651,#8652,#8653,#8654,#8655,#8656,#8657,
#8658,#8659,#8660,#8661,#8662,#8663,#8664,#8665,#8666,#8667,#8668,#8669,
#8670,#8671,#8672,#8673,#8674,#8675,#8676,#8677,#8678,#8679,#8680,#8681,
#8682,#8683,#8684,#8685,#8686,#8687,#8688,#8689,#8690,#8691,#8692,#8693,
#8694,#8695,#8696,#8697,#8698,#8699,#8700,#8701,#8702,#8703,#8704,#8705,
#8706,#8707,#8708,#8709,#8710,#8711,#8712,#8713,#8714,#8715,#8716,#8717,
#8718,#8719,#8720,#8721,#8722,#8723,#8724,#8725,#8726,#8727,#8728,#8729,
#8730,#8731,#8732,#8733,#8734,#8735,#8736,#8737,#8738,#8739,#8740,#8741,
#8742,#8743,#8744,#8745,#8746,#8747,#8748,#8749,#8750,#8751,#8752,#8753,
#8754,#8755,#8756,#8757,#8758,#8759,#8760,#8761,#8762,#8763,#8764,#8765,
#8766,#8767,#8768,#8769,#8770,#8771,#8772,#8773,#8774,#8775,#8776,#8777,
#8778,#8779,#8780,#8781,#8782,#8783,#8784,#8785,#8786,#8787,#8788,#8789,
#8790,#8791,#8792,#8793,#8794,#8795,#8796,#8797,#8798,#8799,#8800,#8801,
#8802,#8803,#8804,#8805,#8806,#8807,#8808,#8809,#8810,#8811,#8812,#8813,
#8814,#8815,#8816,#8817,#8818,#8819,#8820,#8821,#8822,#8823,#8824,#8825,
#8826,#8827,#8828,#8829,#8830,#8831,#8832,#8833,#8834,#8835,#8836,#8837,
#8838,#8839,#8840,#8841,#8842,#8843,#8844,#8845,#8846,#8847,#8848,#8849,
#8850,#8851,#8852,#8853,#8854,#8855,#8856,#8857,#8858,#8859,#8860,#8861,
#8862,#8863,#8864,#8865,#8866,#8867,#8868,#8869,#8870,#8871,#8872,#8873,
#8874,#8875,#8876,#8877,#8878,#8879,#8880,#8881,#8882,#8883,#8884,#8885,
#8886,#8887,#8888,#8889,#8890,#8891,#8892,#8893,#8894,#8895,#8896,#8897,
#8898,#8899,#8900,#8901,#8902,#8903,#8904,#8905,#8906,#8907,#8908,#8909,
#8910,#8911,#8912,#8913,#8914,#8915,#8916,#8917,#8918,#8919,#8920,#8921,
#8922,#8923,#8924,#8925,#8926,#8927,#8928,#8929,#8930,#8931,#8932,#8933,
#8934,#8935,#8936,#8937,#8938,#8939,#8940,#8941,#8942,#8943,#8944,#8945,
#8946,#8947,#8948,#8949,#8950,#8951,#8952,#8953,#8954,#8955,#8956,#8957,
#8958,#8959,#8960,#8961,#8962,#8963,#8964,#8965,#8966,#8967,#8968,#8969,
#8970,#8971,#8972,#8973,#8974,#8975,#8976,#8977,#8978,#8979,#8980,#8981,
#8982,#8983,#8984,#8985,#8986,#8987,#8988,#8989,#8990,#8991,#8992,#8993,
#8994,#8995,#8996,#8997,#8998,#8999,#9000,#9001,#9002,#9003,#9004,#9005,
#9006,#9007,#9008,#9009,#9010,#9011,#9012,#9013,#9014,#9015,#9016,#9017,
#9018,#9019,#9020,#9021,#9022,#9023,#9024,#9025,#9026,#9027,#9028,#9029,
#9030,#9031,#9032,#9033,#9034,#9035,#9036,#9037,#9038,#9039,#9040,#9041,
#9042,#9043,#9044,#9045,#9046,#9047,#9048,#9049,#9050,#9051,#9052,#9053,
#9054,#9055,#9056,#9057,#9058,#9059,#9060,#9061,#9062,#9063,#9064,#9065,
#9066,#9067,#9068,#9069,#9070,#9071,#9072,#9073,#9074,#9075,#9076,#9077,
#9078,#9079,#9080,#9081,#9082,#9083,#9084,#9085,#9086,#9087,#9088,#9089,
#9090,#9091,#9092,#9093,#9094,#9095,#9096,#9097,#9098,#9099,#9100,#9101,
#9102,#9103,#9104,#9105,#9106,#9107,#9108,#9109,#9110,#9111,#9112,#9113,
#9114,#9115,#9116,#9117,#9118,#9119,#9120,#9121,#9122,#9123,#9124,#9125,
#9126,#9127,#9128,#9129,#9130,#9131,#9132,#9133,#9134,#9135,#9136,#9137,
#9138,#9139,#9140,#9141,#9142,#9143,#9144,#9145,#9146,#9147,#9148,#9149,
#9150,#9151,#9152,#9153,#9154,#9155,#9156,#9157,#9158,#9159,#9160,#9161,
#9162,#9163,#9164,#9165,#9166,#9167,#9168,#9169,#9170,#9171,#9172,#9173,
#9174,#9175,#9176,#9177,#9178,#9179,#9180,#9181,#9182,#9183,#9184,#9185,
#9186,#9187,#9188,#9189,#9190,#9191,#9192,#9193,#9194,#9195,#9196,#9197,
#9198,#9199,#9200,#9201,#9202,#9203,#9204,#9205,#9206,#9207,#9208,#9209,
#9210,#9211,#9212,#9213,#9214,#9215,#9216,#9217,#9218,#9219,#9220,#9221,
#9222,#9223,#9224,#9225,#9226,#9227,#9228,#9229,#9230,#9231,#9232,#9233,
#9234,#9235,#9236,#9237,#9238,#9239,#9240,#9241,#9242,#9243,#9244,#9245,
#9246,#9247,#9248,#9249,#9250,#9251,#9252,#9253,#9254,#9255,#9256,#9257,
#9258,#9259,#9260,#9261,#9262,#9263,#9264,#9265,#9266,#9267,#9268,#9269,
#9270,#9271,#9272,#9273,#9274,#9275,#9276,#9277,#9278,#9279,#9280,#9281,
#9282,#9283,#9284,#9285,#9286,#9287,#9288,#9289,#9290,#9291,#9292,#9293,
#9294,#9295,#9296,#9297,#9298,#9299,#9300,#9301,#9302,#9303,#9304,#9305,
#9306,#9307,#9308,#9309,#9310,#9311,#9312,#9313,#9314,#9315,#9316,#9317,
#9318,#9319,#9320,#9321,#9322,#9323,#9324,#9325,#9326,#9327,#9328,#9329,
#9330,#9331,#9332,#9333,#9334,#9335,#9336,#9337,#9338,#9339,#9340,#9341,
#9342,#9343,#9344,#9345,#9346,#9347,#9348,#9349,#9350,#9351,#9352,#9353,
#9354,#9355,#9356,#9357,#9358,#9359,#9360,#9361,#9362,#9363,#9364,#9365,
#9366,#9367,#9368,#9369,#9370,#9371,#9372,#9373,#9374,#9375,#9376,#9377,
#9378,#9379,#9380,#9381,#9382,#9383,#9384,#9385,#9386,#9387,#9388,#9389,
#9390,#9391,#9392,#9393,#9394,#9395,#9396,#9397,#9398,#9399,#9400,#9401,
#9402,#9403,#9404,#9405,#9406,#9407,#9408,#9409,#9410,#9411,#9412,#9413,
#9414,#9415,#9416,#9417,#9418,#9419,#9420,#9421,#9422,#9423,#9424,#9425,
#9426,#9427,#9428,#9429,#9430,#9431,#9432,#9433,#9434,#9435,#9436,#9437,
#9438,#9439,#9440,#9441,#9442,#9443,#9444,#9445,#9446,#9447,#9448,#9449,
#9450,#9451,#9452,#9453,#9454,#9455,#9456,#9457,#9458,#9459,#9460,#9461,
#9462,#9463,#9464,#9465,#9466,#9467,#9468,#9469,#9470,#9471,#9472,#9473,
#9474,#9475,#9476,#9477,#9478,#9479,#9480,#9481,#9482,#9483,#9484,#9485,
#9486,#9487,#9488,#9489,#9490,#9491,#9492,#9493,#9494,#9495,#9496,#9497,
#9498,#9499,#9500,#9501,#9502,#9503,#9504,#9505,#9506,#9507,#9508,#9509,
#9510,#9511,#9512,#9513,#9514,#9515,#9516,#9517,#9518,#9519,#9520,#9521,
#9522,#9523,#9524,#9525,#9526,#9527,#9528,#9529,#9530,#9531,#9532,#9533,
#9534,#9535,#9536,#9537,#9538,#9539,#9540,#9541,#9542,#9543,#9544,#9545,
#9546,#9547,#9548,#9549,#9550,#9551,#9552,#9553,#9554,#9555,#9556,#9557,
#9558,#9559,#9560,#9561,#9562,#9563,#9564,#9565,#9566,#9567,#9568,#9569,
#9570,#9571,#9572,#9573,#9574,#9575,#9576,#9577,#9578,#9579,#9580,#9581,
#9582,#9583,#9584,#9585,#9586,#9587,#9588,#9589,#9590,#9591,#9592,#9593,
#9594,#9595,#9596,#9597,#9598,#9599,#9600,#9601,#9602,#9603,#9604,#9605,
#9606,#9607,#9608,#9609,#9610,#9611,#9612,#9613,#9614,#9615,#9616,#9617,
#9618,#9619,#9620,#9621,#9622,#9623,#9624,#9625,#9626,#9627,#9628,#9629,
#9630,#9631,#9632,#9633,#9634,#9635,#9636,#9637,#9638,#9639,#9640,#9641,
#9642,#9643,#9644,#9645,#9646,#9647,#9648,#9649,#9650,#9651,#9652,#9653,
#9654,#9655,#9656,#9657,#9658,#9659,#9660,#9661,#9662,#9663,#9664,#9665,
#9666,#9667,#9668,#9669,#9670,#9671,#9672,#9673,#9674,#9675,#9676,#9677,
#9678,#9679,#9680,#9681,#9682,#9683,#9684,#9685,#9686,#9687,#9688,#9689,
#9690,#9691,#9692,#9693,#9694,#9695,#9696,#9697,#9698,#9699,#9700,#9701,
#9702,#9703,#9704,#9705,#9706,#9707,#9708,#9709,#9710,#9711,#9712,#9713,
#9714,#9715,#9716,#9717,#9718,#9719,#9720,#9721,#9722,#9723,#9724,#9725,
#9726,#9727,#9728,#9729,#9730,#9731,#9732,#9733,#9734,#9735,#9736,#9737,
#9738,#9739,#9740,#9741,#9742,#9743,#9744,#9745,#9746,#9747,#9748,#9749,
#9750,#9751,#9752,#9753,#9754,#9755,#9756,#9757,#9758,#9759,#9760,#9761,
#9762,#9763,#9764,#9765,#9766,#9767,#9768,#9769,#9770,#9771,#9772,#9773,
#9774,#9775,#9776,#9777,#9778,#9779,#9780,#9781,#9782,#9783,#9784,#9785,
#9786,#9787,#9788,#9789,#9790,#9791,#9792,#9793,#9794,#9795,#9796,#9797,
#9798,#9799,#9800,#9801,#9802,#9803,#9804,#9805,#9806,#9807,#9808,#9809,
#9810,#9811,#9812,#9813,#9814,#9815,#9816,#9817,#9818,#9819,#9820,#9821,
#9822,#9823,#9824,#9825,#9826,#9827,#9828,#9829,#9830,#9831,#9832,#9833,
#9834,#9835,#9836,#9837,#9838,#9839,#9840,#9841,#9842,#9843,#9844,#9845,
#9846,#9847,#9848,#9849,#9850,#9851,#9852,#9853,#9854,#9855,#9856,#9857,
#9858,#9859,#9860,#9861,#9862,#9863,#9864,#9865,#9866,#9867,#9868,#9869,
#9870,#9871,#9872,#9873,#9874,#9875,#9876,#9877,#9878,#9879,#9880,#9881,
#9882,#9883,#9884,#9885,#9886,#9887,#9888,#9889,#9890,#9891,#9892,#9893,
#9894,#9895,#9896,#9897,#9898,#9899,#9900,#9901,#9902,#9903,#9904,#9905,
#9906,#9907,#9908,#9909,#9910,#9911,#9912,#9913,#9914,#9915,#9916,#9917,
#9918,#9919,#9920,#9921,#9922,#9923,#9924,#9925,#9926,#9927,#9928,#9929,
#9930,#9931,#9932,#9933),.UNSPECIFIED.,.F.,.F.,(4,3,3,3,3,3,3,3,3,3,3,3,
3,3,3,3,3,3,3,3,3,3,3,3,3,3,3,3,3,3,3,3,3,3,3,3,3,3,3,3,3,3,3,3,3,3,3,3,
3,3,3,3,3,3,3,3,3,3,3,3,3,3,3,3,3,3,3,3,3,3,3,3,3,3,3,3,3,3,3,3,3,3,3,3,
3,3,3,3,3,3,3,3,3,3,3,3,3,3,3,3,3,3,3,3,3,3,3,3,3,3,3,3,3,3,3,3,3,3,3,3,
3,3,3,3,3,3,3,3,3,3,3,3,3,3,3,3,3,3,3,3,3,3,3,3,3,3,3,3,3,3,3,3,3,3,3,3,
3,3,3,3,3,3,3,3,3,3,3,3,3,3,3,3,3,3,3,3,3,3,3,3,3,3,3,3,3,3,3,3,3,3,3,3,
3,3,3,3,3,3,3,3,3,3,3,3,3,3,3,3,3,3,3,3,3,3,3,3,3,3,3,3,3,3,3,3,3,3,3,3,
3,3,3,3,3,3,3,3,3,3,3,3,3,3,3,3,3,3,3,3,3,3,3,3,3,3,3,3,3,3,3,3,3,3,3,3,
3,3,3,3,3,3,3,3,3,3,3,3,3,3,3,3,3,3,3,3,3,3,3,3,3,3,3,3,3,3,3,3,3,3,3,3,
3,3,3,3,3,3,3,3,3,3,3,3,3,3,3,3,3,3,3,3,3,3,3,3,3,3,3,3,3,3,3,3,3,3,3,3,
3,3,3,3,3,3,3,3,3,3,3,3,3,3,3,3,3,3,3,3,3,3,3,3,3,3,3,3,3,3,3,3,3,3,3,3,
3,3,3,3,3,3,3,3,3,3,3,3,3,3,3,3,3,3,3,3,3,3,3,3,3,3,3,3,3,3,3,3,3,3,3,3,
3,3,3,3,3,3,3,3,3,3,3,3,3,3,3,3,3,3,3,3,3,3,3,3,3,3,3,3,3,3,3,3,3,3,3,3,
3,3,3,3,3,3,3,3,3,3,3,3,3,3,3,3,3,3,3,3,3,3,3,3,3,3,3,3,3,3,3,3,3,3,3,3,
3,3,3,3,3,3,3,3,3,3,3,3,3,3,3,3,3,3,3,3,3,3,3,3,3,3,3,3,3,3,3,3,3,3,3,3,
3,3,3,3,3,3,3,3,3,3,3,3,3,3,3,3,3,3,3,3,3,3,3,3,3,3,3,3,3,3,3,3,3,3,3,3,
3,3,3,3,3,3,3,3,3,3,3,3,3,3,3,3,3,3,3,3,3,3,3,3,3,3,3,3,3,3,3,3,3,3,3,3,
3,3,3,3,3,3,3,3,3,3,3,3,3,3,3,3,3,3,3,3,3,3,3,3,3,3,3,3,3,3,3,3,3,3,3,3,
3,3,3,3,3,3,3,3,3,3,3,3,3,3,3,3,3,3,3,3,3,3,3,3,3,3,3,3,3,3,3,3,3,3,3,3,
3,3,3,3,3,3,3,3,3,3,3,4),(0.00125565797610475,0.00293779707252473,0.00462005004901106,
0.00630132145657572,0.00798471684523592,0.00966590002453388,0.0104166666666667,
0.012100881513486,0.0137828211688803,0.0154854158976119,0.0171670252582823,
0.0188801126710445,0.0205932000838067,0.0208333333333333,0.022517548180085,
0.0241994878356134,0.0259020825643315,0.0275836919248216,0.0292967793376537,
0.0310098667504858,0.03125,0.0329342148472603,0.0346161545021281,0.0363187492308837,
0.0380003585915209,0.0397134460043357,0.0414265334171504,0.0416666666666667,
0.0433508815137824,0.0450328211690335,0.0467354158977296,0.0484170252579816,
0.0501301126708997,0.0518432000838178,0.0520833333333333,0.0537675481803484,
0.0554494878353327,0.0571520825641202,0.0588336919246883,0.0605467793375856,
0.0622598667504829,0.0625,0.064184214846777,0.0658661545020901,0.0675687492308563,
0.0692503585913632,0.0709634460042591,0.0726765334171549,0.0729166666666667,
0.0746008815139086,0.0762828211685875,0.0779854158973962,0.0796670252578115,
0.081380112670817,0.0830932000838225,0.0833333333333333,0.0850175481801576,
0.0866994878356449,0.0884020825643555,0.0900836919248141,0.0917967793376506,
0.0935098667504872,0.09375,0.0954342148471595,0.0971161545021867,0.0988187492309266,
0.100500358591525,0.102213446004336,0.103926533417146,0.104166666666667,
0.105850881513497,0.107532821168975,0.109235415897687,0.110917025258164,
0.112630112670993,0.114343200083822,0.114583333333333,0.116267548180165,
0.117949487835598,0.119652082564317,0.121333691924794,0.123046779337634,
0.124759866750474,0.125,0.126684214846945,0.128366154502066,0.130068749230835,
0.131750358591032,0.133463446004086,0.135176533417139,0.135416666666667,
0.137100881513744,0.138782821169231,0.140485415897875,0.142167025258217,
0.143880112671013,0.14559320008381,0.145833333333333,0.147517548180376,
0.149199487835436,0.150902082564201,0.152583691924607,0.154296779337552,
0.156009866750498,0.15625,0.157934214846695,0.159616154502591,0.161318749231229,
0.163000358591745,0.164713446004444,0.166426533417143,0.166666666666667,
0.168350881513626,0.170032821168768,0.17173541589753,0.173417025257758,
0.175130112670786,0.176843200083815,0.177083333333333,0.17876754818045,
0.180449487835452,0.182152082564211,0.183833691924545,0.185546779337517,
0.187259866750489,0.1875,0.189184214846864,0.190866154502186,0.192568749230926,
0.19425035859113,0.195963446004139,0.197676533417148,0.197916666666667,
0.199600881513898,0.201282821168701,0.202985415897484,0.204667025258033,
0.206380112670933,0.208093200083834,0.208333333333333,0.21001754818046,
0.211699487835182,0.213402082564005,0.215083691924369,0.216796779337423,
0.218509866750476,0.21875,0.220434214847214,0.222116154502313,0.223818749231029,
0.225500358591701,0.227213446004438,0.228926533417176,0.229166666666667,
0.230850881513923,0.232532821168741,0.234235415897509,0.235917025257756,
0.237630112670783,0.23934320008381,0.239583333333333,0.241267548180357,
0.242949487835833,0.244652082564497,0.246333691924975,0.248046779337732,
0.249759866750488,0.25,0.251684214846835,0.253366154502682,0.255068749231299,
0.256750358591701,0.258463446004426,0.26017653341715,0.260416666666667,
0.262100881513437,0.263782821168335,0.265485415897202,0.26716702525756,
0.268880112670682,0.270593200083804,0.270833333333333,0.272517548179882,
0.27419948783552,0.275902082564257,0.2775836919246,0.279296779337534,0.281009866750468,
0.28125,0.282934214846406,0.284616154502373,0.286318749231068,0.288000358591586,
0.289713446004369,0.291426533417152,0.291666666666667,0.293350881513846,
0.295032821168853,0.296735415897596,0.298417025257966,0.300130112670895,
0.301843200083824,0.302083333333333,0.303767548180358,0.30544948783509,
0.307152082563931,0.308833691924725,0.310546779337589,0.312259866750454,
0.3125,0.314184214846726,0.315866154501688,0.317568749230567,0.319250358591126,
0.320963446004165,0.322676533417204,0.322916666666667,0.32460088151406,
0.326282821168734,0.327985415897512,0.329667025257995,0.331380112670921,
0.333093200083847,0.333333333333333,0.335017548180048,0.336699487834948,
0.338402082563829,0.340083691924322,0.341796779337397,0.343509866750471,
0.34375,0.345434214847071,0.347116154502291,0.348818749231006,0.350500358591492,
0.352213446004321,0.35392653341715,0.354166666666667,0.35585088151403,0.357532821168803,
0.359235415897553,0.36091702525804,0.362630112670922,0.364343200083804,
0.364583333333333,0.36626754818007,0.36794948783571,0.369652082564395,0.371333691924692,
0.373046779337572,0.374759866750451,0.375,0.376684214846999,0.378366154502077,
0.380068749230849,0.3817503585914,0.383463446004282,0.385176533417163,0.385416666666667,
0.38710088928785,0.388782855752899,0.390545475148008,0.392227213127909,
0.393908936242942,0.395593200101389,0.395833333333333,0.397517548180182,
0.399199487835114,0.400902082563955,0.402583691924499,0.404296779337489,
0.40600986675048,0.40625,0.40793421484716,0.4096161545024,0.411318749231088,
0.413000358591541,0.414713446004348,0.416426533417155,0.416666666666667,
0.418350881513887,0.420032821169324,0.421735415897952,0.423417025258456,
0.425130112671146,0.426843200083836,0.427083333333333,0.428767548180366,
0.430449487835149,0.432152082563989,0.433833691924315,0.435546779337412,
0.437259866750508,0.4375,0.439184214846839,0.440866154501917,0.442568749230727,
0.444250358591221,0.445963446004191,0.44767653341716,0.447916666666667,
0.449600881513151,0.451282821169071,0.452985415897763,0.454667025258216,
0.456380112671027,0.458093200083838,0.458333333333333,0.460017548180184,
0.461699487835326,0.463402082564116,0.465083691924321,0.466796779337403,
0.468509866750486,0.46875,0.470434214846899,0.472116154502217,0.473818749230949,
0.475500358591599,0.477213446004371,0.478926533417144,0.479166666666667,
0.480850881514302,0.482532821168333,0.484235415897197,0.485917025257881,
0.487630112670835,0.489343200083788,0.489583333333333,0.491267548180153,
0.49294948783568,0.494652082564382,0.49633369192484,0.498046779337664,0.499759866750487,
0.5,0.501684214847251,0.503366154502004,0.505068749230785,0.506750358591275,
0.508463446004202,0.510176533417129,0.510416666666667,0.512100881513675,
0.513782821169851,0.515485415898353,0.517167025258938,0.518880112671398,
0.520593200083858,0.520833333333333,0.522517555953995,0.524199495600808,
0.525902088388242,0.527583697746963,0.529296782248755,0.531009866750547,
0.53125,0.532934214846679,0.534616154501946,0.536318749230739,0.53800035859119,
0.539713446004154,0.541426533417118,0.541666666666667,0.543350881514246,
0.545032821169243,0.546735415897896,0.548417025258523,0.55013011267119,
0.551843200083857,0.552083333333333,0.553767548180513,0.55544948783573,
0.557152082564415,0.558833691924724,0.560546779337596,0.562259866750468,
0.5625,0.564184214846736,0.5658661545017,0.567568749230563,0.569250358591102,
0.570963446004127,0.572676533417152,0.572916666666667,0.574600881513633,
0.576282821168363,0.57798541589723,0.579667025257621,0.581380112670727,
0.583093200083833,0.583333333333333,0.585017548180279,0.586699487835742,
0.588402082564422,0.590083691924783,0.591796779337622,0.593509866750461,
0.59375,0.595434222620651,0.597116189086285,0.598818775168995,0.600500384522268,
0.602213458969697,0.603926533417125,0.604166666666667,0.605850881513831,
0.607532821167997,0.609235415896949,0.610917025257753,0.612630112670779,
0.614343200083805,0.614583333333333,0.61626754818061,0.617949487835351,
0.619652082564126,0.621333691924504,0.623046779337477,0.62475986675045,
0.625,0.626684214847365,0.62836615450299,0.630068749231531,0.631750358591773,
0.633463446004463,0.635176533417153,0.635416666666667,0.637100881513971,
0.638782821168762,0.640485415897536,0.642167025258001,0.64388011267093,
0.645593200083859,0.645833333333333,0.647517548180316,0.649199487835431,
0.650902082564188,0.652583691924302,0.654296779337381,0.65600986675046,
0.65625,0.657934214847428,0.65961615450275,0.661318749231359,0.663000358591569,
0.664713446004377,0.666426533417185,0.666666666666667,0.668350881513661,
0.670032821169161,0.671735415897832,0.673417025258327,0.675130112671086,
0.676843200083846,0.677083333333333,0.678767548180001,0.680449487835573,
0.682152082564307,0.683833691924787,0.685546779337648,0.68725986675051,
0.6875,0.689184214847388,0.6908661545025,0.692568749231162,0.69425035859202,
0.695963446004585,0.69767653341715,0.697916666666667,0.699600881514463,
0.70128282116929,0.702985415897923,0.70466702525867,0.706380112671246,0.708093200083822,
0.708333333333333,0.710017548180411,0.711699487835929,0.713402082564578,
0.715083691925223,0.716796779337875,0.718509866750527,0.71875,0.720434214846616,
0.72211615450235,0.723818749231043,0.725500358591602,0.727213446004362,
0.728926533417123,0.729166666666667,0.730850881513419,0.732532821169214,
0.73423541589785,0.735917025258065,0.737630112670911,0.739343200083758,
0.739583333333333,0.741267548180221,0.742949487835294,0.744652082564087,
0.746333691924615,0.748046779337542,0.749759866750469,0.75,0.751684214846416,
0.753366154502443,0.755068749231134,0.756750358591587,0.758463446004397,
0.760176533417206,0.760416666666667,0.762100881513496,0.763782821168422,
0.765485415897281,0.767167025257607,0.768880112670732,0.770593200083858,
0.770833333333333,0.772517548179594,0.774199487835344,0.775902082564116,
0.777583691924374,0.779296779337404,0.781009866750434,0.78125,0.78293421484669,
0.784616154502112,0.786318749230868,0.788000358591228,0.789713446004183,
0.791426533417138,0.791666666666667,0.793350881513279,0.795032821168849,
0.796735415897573,0.798417025258128,0.800130112670938,0.801843200083748,
0.802083333333333,0.80376754817991,0.805449487834996,0.807152082563882,
0.808833691924143,0.810546779337342,0.81225986675054,0.8125,0.814184214846875,
0.815866154502397,0.817568749231082,0.819250358591479,0.820963446004308,
0.822676533417138,0.822916666666667,0.824600881513549,0.82628282116942,
0.827985415898024,0.829667025258528,0.831380112671183,0.833093200083837,
0.833333333333333,0.835017548180832,0.836699487835411,0.838402082564181,
0.840083691924666,0.841796779337578,0.843509866750491,0.84375,0.845434214847378,
0.847116154502397,0.84881874923109,0.850500358591155,0.852213446004163,
0.853926533417171,0.854166666666667,0.855850881513812,0.857532821168573,
0.859235415897376,0.860917025258013,0.862630112670899,0.864343200083785,
0.864583333333333,0.866267548179718,0.867949487835134,0.86965208256396,
0.871333691924431,0.873046779337435,0.874759866750439,0.875,0.876684214846492,
0.878366154501995,0.880068749230787,0.881750358591456,0.88346344600431,
0.885176533417163,0.885416666666667,0.887100881513135,0.888782821168991,
0.890485415897707,0.892167025258341,0.893880112671098,0.895593200083855,
0.895833333333333,0.897517548179665,0.899199487834624,0.900902082563594,
0.902583691923825,0.904296779337165,0.906009866750505,0.90625,0.907934214846278,
0.909616154501992,0.91131874923077,0.913000358591198,0.914713446004152,
0.916426533417106,0.916666666666667,0.918350881512217,0.920032821168928,
0.921735415897672,0.923417025258493,0.925130112671199,0.926843200083906,
0.927083333333333,0.928767548179258,0.93044948783491,0.932152082563814,
0.933833691923954,0.935546779337241,0.937259866750527,0.9375,0.939184214847346,
0.940866154502457,0.942568749231125,0.94425035859122,0.945963446004174,
0.947676533417128,0.947916666666667,0.949600881513474,0.951282821169022,
0.952985415897738,0.95466702525834,0.956380112671114,0.958093200083887,
0.958333333333333,0.960017548181036,0.961699487835379,0.963402082564164,
0.965083691924602,0.966796779337562,0.968509866750522,0.96875,0.970434214847239,
0.972116154502219,0.973818749230962,0.975500358591352,0.977213446004272,
0.978926533417192,0.979166666666667,0.980850881513793,0.982532821168591,
0.98423541589741,0.985917025258421,0.987630112671144,0.989343200083866,
0.989583333333333,0.991267548181292,0.992949487836093,0.994652082564706,
0.996333691925092,0.998046779337818,0.999759866750545,1.),.UNSPECIFIED.);
#127=B_SPLINE_CURVE_WITH_KNOTS('',3,(#11295,#11296,#11297,#11298,#11299,
#11300,#11301,#11302,#11303,#11304,#11305,#11306),.UNSPECIFIED.,.F.,.F.,
(4,2,2,2,2,4),(2.72017260531256E-6,0.00801802930125374,0.0194025153047282,
0.0282740905432685,0.0382285674272786,0.0405127362382465),.UNSPECIFIED.);
#167=SHAPE_REPRESENTATION_RELATIONSHIP('SRR','None',#12191,#178);
#178=ADVANCED_BREP_SHAPE_REPRESENTATION('',(#200),#12132);
#189=STYLED_ITEM('',(#12253),#200);
#200=MANIFOLD_SOLID_BREP('Body1',#1834);
#220=FACE_BOUND('',#680,.T.);
#257=PLANE('',#2062);
#258=PLANE('',#2065);
#259=PLANE('',#2069);
#260=PLANE('',#2070);
#261=PLANE('',#2071);
#262=PLANE('',#2073);
#338=LINE('',#9938,#432);
#339=LINE('',#9942,#433);
#432=VECTOR('',#2428,1000.);
#433=VECTOR('',#2433,1000.);
#550=FACE_OUTER_BOUND('',#675,.T.);
#551=FACE_OUTER_BOUND('',#676,.T.);
#552=FACE_OUTER_BOUND('',#677,.T.);
#553=FACE_OUTER_BOUND('',#678,.T.);
#554=FACE_OUTER_BOUND('',#679,.T.);
#555=FACE_OUTER_BOUND('',#681,.T.);
#556=FACE_OUTER_BOUND('',#682,.T.);
#557=FACE_OUTER_BOUND('',#683,.T.);
#558=FACE_OUTER_BOUND('',#684,.T.);
#559=FACE_OUTER_BOUND('',#685,.T.);
#560=FACE_OUTER_BOUND('',#686,.T.);
#561=FACE_OUTER_BOUND('',#687,.T.);
#562=FACE_OUTER_BOUND('',#688,.T.);
#675=EDGE_LOOP('',(#1497,#1498,#1499,#1500,#1501));
#676=EDGE_LOOP('',(#1502,#1503,#1504,#1505,#1506));
#677=EDGE_LOOP('',(#1507,#1508,#1509,#1510,#1511));
#678=EDGE_LOOP('',(#1512,#1513,#1514,#1515,#1516,#1517));
#679=EDGE_LOOP('',(#1518,#1519));
#680=EDGE_LOOP('',(#1520,#1521,#1522));
#681=EDGE_LOOP('',(#1523,#1524,#1525));
#682=EDGE_LOOP('',(#1526,#1527,#1528,#1529,#1530));
#683=EDGE_LOOP('',(#1531,#1532,#1533,#1534,#1535,#1536));
#684=EDGE_LOOP('',(#1537,#1538));
#685=EDGE_LOOP('',(#1539,#1540,#1541));
#686=EDGE_LOOP('',(#1542,#1543,#1544));
#687=EDGE_LOOP('',(#1545,#1546,#1547,#1548,#1549));
#688=EDGE_LOOP('',(#1550));
#772=CIRCLE('',#2051,0.250000000000001);
#773=CIRCLE('',#2052,0.250000000000001);
#774=CIRCLE('',#2053,1.74999999999999);
#775=CIRCLE('',#2054,0.249999999999999);
#776=CIRCLE('',#2056,0.25);
#777=CIRCLE('',#2057,0.3);
#778=CIRCLE('',#2058,0.300000000000001);
#779=CIRCLE('',#2059,0.300000000000001);
#780=CIRCLE('',#2060,0.299999999999999);
#781=CIRCLE('',#2063,0.299999999999999);
#782=CIRCLE('',#2066,0.300000000000001);
#783=CIRCLE('',#2067,0.300000000000001);
#784=CIRCLE('',#2068,0.3);
#785=CIRCLE('',#2072,0.25);
#914=VERTEX_POINT('',#5274);
#915=VERTEX_POINT('',#5275);
#916=VERTEX_POINT('',#5278);
#917=VERTEX_POINT('',#5365);
#918=VERTEX_POINT('',#5378);
#919=VERTEX_POINT('',#5380);
#920=VERTEX_POINT('',#5674);
#921=VERTEX_POINT('',#5675);
#922=VERTEX_POINT('',#5700);
#923=VERTEX_POINT('',#5747);
#924=VERTEX_POINT('',#5749);
#925=VERTEX_POINT('',#7721);
#926=VERTEX_POINT('',#7723);
#927=VERTEX_POINT('',#7917);
#928=VERTEX_POINT('',#7919);
#929=VERTEX_POINT('',#9937);
#930=VERTEX_POINT('',#9941);
#1118=EDGE_CURVE('',#914,#915,#772,.T.);
#1119=EDGE_CURVE('',#915,#914,#773,.T.);
#1120=EDGE_CURVE('',#914,#916,#774,.T.);
#1121=EDGE_CURVE('',#916,#916,#775,.T.);
#1122=EDGE_CURVE('',#915,#917,#121,.T.);
#1123=EDGE_CURVE('',#917,#918,#12,.T.);
#1124=EDGE_CURVE('',#918,#919,#776,.T.);
#1125=EDGE_CURVE('',#914,#919,#122,.T.);
#1126=EDGE_CURVE('',#920,#921,#123,.T.);
#1127=EDGE_CURVE('',#921,#922,#124,.T.);
#1128=EDGE_CURVE('',#923,#922,#777,.T.);
#1129=EDGE_CURVE('',#924,#923,#125,.T.);
#1130=EDGE_CURVE('',#924,#920,#778,.T.);
#1131=EDGE_CURVE('',#920,#925,#779,.T.);
#1132=EDGE_CURVE('',#925,#926,#11,.T.);
#1133=EDGE_CURVE('',#926,#927,#780,.T.);
#1134=EDGE_CURVE('',#928,#927,#126,.T.);
#1135=EDGE_CURVE('',#921,#928,#13,.T.);
#1136=EDGE_CURVE('',#927,#926,#781,.T.);
#1137=EDGE_CURVE('',#918,#929,#338,.T.);
#1138=EDGE_CURVE('',#929,#917,#14,.T.);
#1139=EDGE_CURVE('',#920,#930,#339,.T.);
#1140=EDGE_CURVE('',#925,#930,#782,.T.);
#1141=EDGE_CURVE('',#928,#930,#127,.T.);
#1142=EDGE_CURVE('',#930,#924,#783,.T.);
#1143=EDGE_CURVE('',#922,#923,#784,.T.);
#1144=EDGE_CURVE('',#919,#929,#785,.T.);
#1497=ORIENTED_EDGE('',*,*,#1118,.T.);
#1498=ORIENTED_EDGE('',*,*,#1119,.T.);
#1499=ORIENTED_EDGE('',*,*,#1120,.T.);
#1500=ORIENTED_EDGE('',*,*,#1121,.F.);
#1501=ORIENTED_EDGE('',*,*,#1120,.F.);
#1502=ORIENTED_EDGE('',*,*,#1119,.F.);
#1503=ORIENTED_EDGE('',*,*,#1122,.T.);
#1504=ORIENTED_EDGE('',*,*,#1123,.T.);
#1505=ORIENTED_EDGE('',*,*,#1124,.T.);
#1506=ORIENTED_EDGE('',*,*,#1125,.F.);
#1507=ORIENTED_EDGE('',*,*,#1126,.T.);
#1508=ORIENTED_EDGE('',*,*,#1127,.T.);
#1509=ORIENTED_EDGE('',*,*,#1128,.F.);
#1510=ORIENTED_EDGE('',*,*,#1129,.F.);
#1511=ORIENTED_EDGE('',*,*,#1130,.T.);
#1512=ORIENTED_EDGE('',*,*,#1131,.T.);
#1513=ORIENTED_EDGE('',*,*,#1132,.T.);
#1514=ORIENTED_EDGE('',*,*,#1133,.T.);
#1515=ORIENTED_EDGE('',*,*,#1134,.F.);
#1516=ORIENTED_EDGE('',*,*,#1135,.F.);
#1517=ORIENTED_EDGE('',*,*,#1126,.F.);
#1518=ORIENTED_EDGE('',*,*,#1136,.F.);
#1519=ORIENTED_EDGE('',*,*,#1133,.F.);
#1520=ORIENTED_EDGE('',*,*,#1137,.F.);
#1521=ORIENTED_EDGE('',*,*,#1123,.F.);
#1522=ORIENTED_EDGE('',*,*,#1138,.F.);
#1523=ORIENTED_EDGE('',*,*,#1131,.F.);
#1524=ORIENTED_EDGE('',*,*,#1139,.T.);
#1525=ORIENTED_EDGE('',*,*,#1140,.F.);
#1526=ORIENTED_EDGE('',*,*,#1132,.F.);
#1527=ORIENTED_EDGE('',*,*,#1140,.T.);
#1528=ORIENTED_EDGE('',*,*,#1141,.F.);
#1529=ORIENTED_EDGE('',*,*,#1134,.T.);
#1530=ORIENTED_EDGE('',*,*,#1136,.T.);
#1531=ORIENTED_EDGE('',*,*,#1127,.F.);
#1532=ORIENTED_EDGE('',*,*,#1135,.T.);
#1533=ORIENTED_EDGE('',*,*,#1141,.T.);
#1534=ORIENTED_EDGE('',*,*,#1142,.T.);
#1535=ORIENTED_EDGE('',*,*,#1129,.T.);
#1536=ORIENTED_EDGE('',*,*,#1143,.F.);
#1537=ORIENTED_EDGE('',*,*,#1128,.T.);
#1538=ORIENTED_EDGE('',*,*,#1143,.T.);
#1539=ORIENTED_EDGE('',*,*,#1139,.F.);
#1540=ORIENTED_EDGE('',*,*,#1130,.F.);
#1541=ORIENTED_EDGE('',*,*,#1142,.F.);
#1542=ORIENTED_EDGE('',*,*,#1124,.F.);
#1543=ORIENTED_EDGE('',*,*,#1137,.T.);
#1544=ORIENTED_EDGE('',*,*,#1144,.F.);
#1545=ORIENTED_EDGE('',*,*,#1122,.F.);
#1546=ORIENTED_EDGE('',*,*,#1118,.F.);
#1547=ORIENTED_EDGE('',*,*,#1125,.T.);
#1548=ORIENTED_EDGE('',*,*,#1144,.T.);
#1549=ORIENTED_EDGE('',*,*,#1138,.T.);
#1550=ORIENTED_EDGE('',*,*,#1121,.T.);
#1711=TOROIDAL_SURFACE('',#2050,1.99999999999999,0.25);
#1778=ADVANCED_FACE('',(#550),#1711,.T.);
#1779=ADVANCED_FACE('',(#551),#15,.F.);
#1780=ADVANCED_FACE('',(#552),#16,.T.);
#1781=ADVANCED_FACE('',(#553),#17,.T.);
#1782=ADVANCED_FACE('',(#554,#220),#257,.F.);
#1783=ADVANCED_FACE('',(#555),#258,.T.);
#1784=ADVANCED_FACE('',(#556),#18,.T.);
#1785=ADVANCED_FACE('',(#557),#19,.T.);
#1786=ADVANCED_FACE('',(#558),#259,.T.);
#1787=ADVANCED_FACE('',(#559),#260,.F.);
#1788=ADVANCED_FACE('',(#560),#261,.F.);
#1789=ADVANCED_FACE('',(#561),#20,.F.);
#1790=ADVANCED_FACE('',(#562),#262,.T.);
#1834=CLOSED_SHELL('',(#1778,#1779,#1780,#1781,#1782,#1783,#1784,#1785,
#1786,#1787,#1788,#1789,#1790));
#2049=AXIS2_PLACEMENT_3D('',#5272,#2398,#2399);
#2050=AXIS2_PLACEMENT_3D('',#5273,#2400,#2401);
#2051=AXIS2_PLACEMENT_3D('',#5276,#2402,#2403);
#2052=AXIS2_PLACEMENT_3D('',#5277,#2404,#2405);
#2053=AXIS2_PLACEMENT_3D('',#5279,#2406,#2407);
#2054=AXIS2_PLACEMENT_3D('',#5280,#2408,#2409);
#2055=AXIS2_PLACEMENT_3D('',#5379,#2410,#2411);
#2056=AXIS2_PLACEMENT_3D('',#5381,#2412,#2413);
#2057=AXIS2_PLACEMENT_3D('',#5748,#2414,#2415);
#2058=AXIS2_PLACEMENT_3D('',#5790,#2416,#2417);
#2059=AXIS2_PLACEMENT_3D('',#7722,#2418,#2419);
#2060=AXIS2_PLACEMENT_3D('',#7918,#2420,#2421);
#2061=AXIS2_PLACEMENT_3D('',#9934,#2422,#2423);
#2062=AXIS2_PLACEMENT_3D('',#9935,#2424,#2425);
#2063=AXIS2_PLACEMENT_3D('',#9936,#2426,#2427);
#2064=AXIS2_PLACEMENT_3D('',#9939,#2429,#2430);
#2065=AXIS2_PLACEMENT_3D('',#9940,#2431,#2432);
#2066=AXIS2_PLACEMENT_3D('',#9943,#2434,#2435);
#2067=AXIS2_PLACEMENT_3D('',#11587,#2436,#2437);
#2068=AXIS2_PLACEMENT_3D('',#11588,#2438,#2439);
#2069=AXIS2_PLACEMENT_3D('',#11589,#2440,#2441);
#2070=AXIS2_PLACEMENT_3D('',#11590,#2442,#2443);
#2071=AXIS2_PLACEMENT_3D('',#11591,#2444,#2445);
#2072=AXIS2_PLACEMENT_3D('',#11592,#2446,#2447);
#2073=AXIS2_PLACEMENT_3D('',#11677,#2448,#2449);
#2398=DIRECTION('axis',(0.,0.,1.));
#2399=DIRECTION('refdir',(1.,0.,0.));
#2400=DIRECTION('center_axis',(-1.,2.13070711535924E-14,1.04964664071668E-11));
#2401=DIRECTION('ref_axis',(1.04964925640161E-11,0.,1.));
#2402=DIRECTION('center_axis',(2.12533623997605E-14,1.,-2.83106871279414E-15));
#2403=DIRECTION('ref_axis',(8.97372454122798E-12,2.83106871260342E-15,1.));
#2404=DIRECTION('center_axis',(2.12533623997605E-14,1.,-2.83106871279414E-15));
#2405=DIRECTION('ref_axis',(8.97372454122798E-12,2.83106871260342E-15,1.));
#2406=DIRECTION('center_axis',(1.,-2.13070711535924E-14,-1.04964664071668E-11));
#2407=DIRECTION('ref_axis',(1.04964664071668E-11,1.23320016381195E-30,1.));
#2408=DIRECTION('center_axis',(-8.06361698590839E-12,0.638630771867137,
-0.769513311921493));
#2409=DIRECTION('ref_axis',(5.19723153402649E-12,0.769513311921493,0.638630771867137));
#2410=DIRECTION('center_axis',(4.51901948662213E-14,0.369697847569671,-0.929152033578118));
#2411=DIRECTION('ref_axis',(0.0324999339408396,0.928661197510084,0.369502550103484));
#2412=DIRECTION('center_axis',(-1.03853394700108E-11,0.143112919231812,
-0.989706366731542));
#2413=DIRECTION('ref_axis',(-7.02048013174369E-27,0.989706366731542,0.143112919231812));
#2414=DIRECTION('center_axis',(0.103812281246273,-0.983494881238285,0.148191864960724));
#2415=DIRECTION('ref_axis',(0.781565304323041,-0.0114833506200699,-0.623717730818172));
#2416=DIRECTION('center_axis',(0.220700126149881,0.458860340274016,0.860661746821038));
#2417=DIRECTION('ref_axis',(6.19011699821459E-17,-0.882420731745959,0.470461105921548));
#2418=DIRECTION('center_axis',(-9.28642086322632E-15,0.369697847569618,
-0.929152033578139));
#2419=DIRECTION('ref_axis',(-1.89840727556356E-30,0.929152033578139,0.369697847569618));
#2420=DIRECTION('center_axis',(1.22926249344571E-14,-0.369697847569616,
0.92915203357814));
#2421=DIRECTION('ref_axis',(-6.3986981584535E-29,0.92915203357814,0.369697847569616));
#2422=DIRECTION('center_axis',(0.0984311714245096,0.0472114241352603,0.994023332685465));
#2423=DIRECTION('ref_axis',(-0.324485630845978,-0.942758830796727,0.0769081421520186));
#2424=DIRECTION('center_axis',(1.22716376708482E-14,-0.369697847569616,
0.92915203357814));
#2425=DIRECTION('ref_axis',(-1.3530577912008E-26,-0.92915203357814,-0.369697847569616));
#2426=DIRECTION('center_axis',(1.22926249344571E-14,-0.369697847569616,
0.92915203357814));
#2427=DIRECTION('ref_axis',(-6.3986981584535E-29,0.92915203357814,0.369697847569616));
#2428=DIRECTION('',(1.,-4.13767374242821E-11,-1.64764880769037E-11));
#2429=DIRECTION('center_axis',(-1.43346686358312E-12,0.369697847570999,
-0.92915203357759));
#2430=DIRECTION('ref_axis',(-0.0324999455498311,0.928661197158793,0.369502549965296));
#2431=DIRECTION('center_axis',(9.26543359961297E-15,-0.369697847569618,
0.929152033578139));
#2432=DIRECTION('ref_axis',(-1.39344188711162E-26,-0.929152033578139,-0.369697847569618));
#2433=DIRECTION('',(-0.958764109698245,0.264067855465545,0.105069261272554));
#2434=DIRECTION('center_axis',(-9.28642086322632E-15,0.369697847569618,
-0.929152033578139));
#2435=DIRECTION('ref_axis',(-1.89840727556356E-30,0.929152033578139,0.369697847569618));
#2436=DIRECTION('center_axis',(0.220700126149881,0.458860340274016,0.860661746821038));
#2437=DIRECTION('ref_axis',(6.19011699821459E-17,-0.882420731745959,0.470461105921548));
#2438=DIRECTION('center_axis',(0.103812281246273,-0.983494881238285,0.148191864960724));
#2439=DIRECTION('ref_axis',(0.781565304323041,-0.0114833506200699,-0.623717730818172));
#2440=DIRECTION('center_axis',(0.103812281246273,-0.983494881238285,0.148191864960724));
#2441=DIRECTION('ref_axis',(0.781565304323041,-0.0114833506200699,-0.623717730818172));
#2442=DIRECTION('center_axis',(0.220700126149881,0.458860340274016,0.860661746821038));
#2443=DIRECTION('ref_axis',(1.21911388842755E-17,-0.882420731745959,0.470461105921548));
#2444=DIRECTION('center_axis',(-1.03853394700108E-11,0.143112919231812,
-0.989706366731542));
#2445=DIRECTION('ref_axis',(6.17299284843058E-27,0.989706366731542,0.143112919231812));
#2446=DIRECTION('center_axis',(-1.03853394700108E-11,0.143112919231812,
-0.989706366731542));
#2447=DIRECTION('ref_axis',(-7.02048013174369E-27,0.989706366731542,0.143112919231812));
#2448=DIRECTION('center_axis',(-8.06361698590839E-12,0.638630771867137,
-0.769513311921493));
#2449=DIRECTION('ref_axis',(5.196667977727E-12,0.769513311921493,0.638630771867137));
#5272=CARTESIAN_POINT('',(0.,0.,0.));
#5273=CARTESIAN_POINT('Origin',(-1.99999999999935,42.8890026416775,0.0554857494443409));
#5274=CARTESIAN_POINT('',(-2.00000000001811,42.8890026416775,-1.69451425055565));
#5275=CARTESIAN_POINT('',(-2.00000000002259,42.8890026416775,-2.19451425055565));
#5276=CARTESIAN_POINT('Origin',(-2.00000000002035,42.8890026416775,-1.94451425055565));
#5277=CARTESIAN_POINT('Origin',(-2.00000000002035,42.8890026416775,-1.94451425055565));
#5278=CARTESIAN_POINT('',(-2.00000000001111,41.5423543458149,-1.06211810132313));
#5279=CARTESIAN_POINT('Origin',(-1.99999999999935,42.8890026416775,0.0554857494443409));
#5280=CARTESIAN_POINT('Origin',(-2.0000000000128,41.3499760178345,-1.22177579428992));
#5281=CARTESIAN_POINT('Ctrl Pts',(-2.00000000001811,42.8890026416775,-1.69451425055562));
#5282=CARTESIAN_POINT('Ctrl Pts',(-2.00000000001811,42.7138340471106,-1.69451425055564));
#5283=CARTESIAN_POINT('Ctrl Pts',(-2.00000000001811,42.5195868694293,-1.69664685121079));
#5284=CARTESIAN_POINT('Ctrl Pts',(-2.00000000001818,42.1727041659024,-1.69763022720131));
#5285=CARTESIAN_POINT('Ctrl Pts',(-2.00000000001809,42.0075453806213,-1.69643582812033));
#5286=CARTESIAN_POINT('Ctrl Pts',(-2.000000000018,41.5447432182596,-1.67506238348623));
#5287=CARTESIAN_POINT('Ctrl Pts',(-2.00000000001759,41.2824586218001,-1.63529714422004));
#5288=CARTESIAN_POINT('Ctrl Pts',(-2.00000000001559,40.8726877368524,-1.45751662005935));
#5289=CARTESIAN_POINT('Ctrl Pts',(-2.00000000001428,40.7146168625301,-1.32576584773803));
#5290=CARTESIAN_POINT('Ctrl Pts',(-2.00000000000915,40.4347106414413,-0.836444527344903));
#5291=CARTESIAN_POINT('Ctrl Pts',(-2.00000000000487,40.3213171458309,-0.475216515464907));
#5292=CARTESIAN_POINT('Ctrl Pts',(-2.,40.247426591683,0.0357782298078951));
#5293=CARTESIAN_POINT('Ctrl Pts',(-1.50000000001812,42.8890026416775,-1.69451425056007));
#5294=CARTESIAN_POINT('Ctrl Pts',(-1.50000000001811,42.7138340471107,-1.6945142505601));
#5295=CARTESIAN_POINT('Ctrl Pts',(-1.50000000001814,42.5195868694296,-1.69664685121553));
#5296=CARTESIAN_POINT('Ctrl Pts',(-1.50000000001815,42.1727041659021,-1.69763022720547));
#5297=CARTESIAN_POINT('Ctrl Pts',(-1.50000000001812,42.0075453806213,-1.69643582812505));
#5298=CARTESIAN_POINT('Ctrl Pts',(-1.50000000001802,41.5447432182596,-1.6750623834901));
#5299=CARTESIAN_POINT('Ctrl Pts',(-1.50000000001758,41.2824586218004,-1.635297144225));
#5300=CARTESIAN_POINT('Ctrl Pts',(-1.50000000001562,40.8726877368527,-1.45751662006339));
#5301=CARTESIAN_POINT('Ctrl Pts',(-1.50000000001431,40.7146168625313,-1.32576584774273));
#5302=CARTESIAN_POINT('Ctrl Pts',(-1.50000000000914,40.4347106414414,-0.836444527349893));
#5303=CARTESIAN_POINT('Ctrl Pts',(-1.50000000000502,40.321317145827,-0.475216515469928));
#5304=CARTESIAN_POINT('Ctrl Pts',(-1.5,40.2474265916837,0.0357782298028141));
#5305=CARTESIAN_POINT('Ctrl Pts',(-1.50000000002261,42.8890026416775,-2.19451425056016));
#5306=CARTESIAN_POINT('Ctrl Pts',(-1.5000000000226,42.6924352393214,-2.19451425056018));
#5307=CARTESIAN_POINT('Ctrl Pts',(-1.50000000002262,42.5242279803483,-2.196635703513));
#5308=CARTESIAN_POINT('Ctrl Pts',(-1.50000000002264,42.1708979670303,-2.19763735653693));
#5309=CARTESIAN_POINT('Ctrl Pts',(-1.50000000002256,41.9983311272475,-2.19654321697105));
#5310=CARTESIAN_POINT('Ctrl Pts',(-1.50000000002256,41.4939715199041,-2.1732505327887));
#5311=CARTESIAN_POINT('Ctrl Pts',(-1.50000000002207,41.1721096008011,-2.1324514159462));
#5312=CARTESIAN_POINT('Ctrl Pts',(-1.50000000001927,40.5850276451855,-1.87774381002253));
#5313=CARTESIAN_POINT('Ctrl Pts',(-1.50000000001706,40.3267157332556,-1.65463617720806));
#5314=CARTESIAN_POINT('Ctrl Pts',(-1.50000000001012,39.9545934323558,-1.00410633608771));
#5315=CARTESIAN_POINT('Ctrl Pts',(-1.50000000000546,39.831903366932,-0.584389540167537));
#5316=CARTESIAN_POINT('Ctrl Pts',(-1.50000000000002,39.752573408318,-0.0357782298130924));
#5317=CARTESIAN_POINT('Ctrl Pts',(-2.00000000002259,42.8890026416775,-2.19451425055564));
#5318=CARTESIAN_POINT('Ctrl Pts',(-2.0000000000226,42.6924352393214,-2.19451425055565));
#5319=CARTESIAN_POINT('Ctrl Pts',(-2.00000000002263,42.5242279803487,-2.19663570350848));
#5320=CARTESIAN_POINT('Ctrl Pts',(-2.00000000002263,42.17089796703,-2.19763735653241));
#5321=CARTESIAN_POINT('Ctrl Pts',(-2.00000000002255,41.9983311272475,-2.19654321696658));
#5322=CARTESIAN_POINT('Ctrl Pts',(-2.00000000002255,41.4939715199041,-2.17325053278423));
#5323=CARTESIAN_POINT('Ctrl Pts',(-2.00000000002206,41.1721096008009,-2.13245141594075));
#5324=CARTESIAN_POINT('Ctrl Pts',(-2.00000000001923,40.5850276451852,-1.87774381001891));
#5325=CARTESIAN_POINT('Ctrl Pts',(-2.00000000001706,40.3267157332544,-1.65463617720347));
#5326=CARTESIAN_POINT('Ctrl Pts',(-2.00000000001007,39.9545934323557,-1.0041063360826));
#5327=CARTESIAN_POINT('Ctrl Pts',(-2.00000000000546,39.8319033669359,-0.58438954016253));
#5328=CARTESIAN_POINT('Ctrl Pts',(-2.,39.7525734083173,-0.03577822980802));
#5329=CARTESIAN_POINT('Ctrl Pts',(-2.50000000002261,42.8890026416775,-2.19451425055115));
#5330=CARTESIAN_POINT('Ctrl Pts',(-2.5000000000226,42.6924352393213,-2.19451425055115));
#5331=CARTESIAN_POINT('Ctrl Pts',(-2.50000000002264,42.524227980349,-2.19663570350397));
#5332=CARTESIAN_POINT('Ctrl Pts',(-2.50000000002262,42.1708979670296,-2.19763735652791));
#5333=CARTESIAN_POINT('Ctrl Pts',(-2.50000000002255,41.9983311272475,-2.19654321696204));
#5334=CARTESIAN_POINT('Ctrl Pts',(-2.50000000002259,41.493971519904,-2.17325053277969));
#5335=CARTESIAN_POINT('Ctrl Pts',(-2.5000000000221,41.1721096008005,-2.13245141593522));
#5336=CARTESIAN_POINT('Ctrl Pts',(-2.50000000001924,40.5850276451849,-1.87774381001523));
#5337=CARTESIAN_POINT('Ctrl Pts',(-2.50000000001709,40.3267157332532,-1.65463617719887));
#5338=CARTESIAN_POINT('Ctrl Pts',(-2.50000000001009,39.9545934323556,-1.00410633607742));
#5339=CARTESIAN_POINT('Ctrl Pts',(-2.50000000000545,39.8319033669398,-0.584389540157467));
#5340=CARTESIAN_POINT('Ctrl Pts',(-2.50000000000002,39.7525734083165,-0.0357782298028245));
#5341=CARTESIAN_POINT('Ctrl Pts',(-2.50000000001813,42.8890026416775,-1.69451425055113));
#5342=CARTESIAN_POINT('Ctrl Pts',(-2.50000000001811,42.7138340471106,-1.69451425055112));
#5343=CARTESIAN_POINT('Ctrl Pts',(-2.50000000001808,42.519586869429,-1.69664685120596));
#5344=CARTESIAN_POINT('Ctrl Pts',(-2.50000000001821,42.1727041659027,-1.6976302271971));
#5345=CARTESIAN_POINT('Ctrl Pts',(-2.50000000001814,42.0075453806212,-1.69643582811551));
#5346=CARTESIAN_POINT('Ctrl Pts',(-2.50000000001799,41.5447432182596,-1.67506238348225));
#5347=CARTESIAN_POINT('Ctrl Pts',(-2.50000000001761,41.2824586217998,-1.63529714421497));
#5348=CARTESIAN_POINT('Ctrl Pts',(-2.5000000000156,40.872687736852,-1.45751662005523));
#5349=CARTESIAN_POINT('Ctrl Pts',(-2.50000000001424,40.7146168625289,-1.32576584773326));
#5350=CARTESIAN_POINT('Ctrl Pts',(-2.50000000000921,40.4347106414412,-0.836444527339844));
#5351=CARTESIAN_POINT('Ctrl Pts',(-2.50000000000473,40.3213171458348,-0.475216515459863));
#5352=CARTESIAN_POINT('Ctrl Pts',(-2.5,40.2474265916822,0.0357782298130767));
#5353=CARTESIAN_POINT('Ctrl Pts',(-2.00000000001811,42.8890026416775,-1.69451425055562));
#5354=CARTESIAN_POINT('Ctrl Pts',(-2.00000000001811,42.7138340471106,-1.69451425055564));
#5355=CARTESIAN_POINT('Ctrl Pts',(-2.00000000001811,42.5195868694293,-1.69664685121079));
#5356=CARTESIAN_POINT('Ctrl Pts',(-2.00000000001818,42.1727041659024,-1.69763022720131));
#5357=CARTESIAN_POINT('Ctrl Pts',(-2.00000000001809,42.0075453806213,-1.69643582812033));
#5358=CARTESIAN_POINT('Ctrl Pts',(-2.000000000018,41.5447432182596,-1.67506238348623));
#5359=CARTESIAN_POINT('Ctrl Pts',(-2.00000000001759,41.2824586218001,-1.63529714422004));
#5360=CARTESIAN_POINT('Ctrl Pts',(-2.00000000001559,40.8726877368524,-1.45751662005935));
#5361=CARTESIAN_POINT('Ctrl Pts',(-2.00000000001428,40.7146168625301,-1.32576584773803));
#5362=CARTESIAN_POINT('Ctrl Pts',(-2.00000000000915,40.4347106414413,-0.836444527344903));
#5363=CARTESIAN_POINT('Ctrl Pts',(-2.00000000000487,40.3213171458309,-0.475216515464907));
#5364=CARTESIAN_POINT('Ctrl Pts',(-2.,40.247426591683,0.0357782298078951));
#5365=CARTESIAN_POINT('',(-1.99999999998774,39.7613743993598,-0.0949461097254665));
#5366=CARTESIAN_POINT('Ctrl Pts',(-2.00000000002259,42.8890026416775,-2.19451425055565));
#5367=CARTESIAN_POINT('Ctrl Pts',(-2.0000000000226,42.6924352393214,-2.19451425055565));
#5368=CARTESIAN_POINT('Ctrl Pts',(-2.00000000002263,42.5242279803487,-2.19663570350848));
#5369=CARTESIAN_POINT('Ctrl Pts',(-2.00000000002263,42.17089796703,-2.19763735653241));
#5370=CARTESIAN_POINT('Ctrl Pts',(-2.00000000002255,41.9983311272475,-2.19654321696658));
#5371=CARTESIAN_POINT('Ctrl Pts',(-2.00000000002255,41.4939715199041,-2.17325053278423));
#5372=CARTESIAN_POINT('Ctrl Pts',(-2.00000000002206,41.1721096008009,-2.13245141594075));
#5373=CARTESIAN_POINT('Ctrl Pts',(-2.00000000001923,40.5850276451852,-1.87774381001891));
#5374=CARTESIAN_POINT('Ctrl Pts',(-2.00000000001706,40.3267157332544,-1.65463617720347));
#5375=CARTESIAN_POINT('Ctrl Pts',(-2.0000000000102,39.9613396308944,-1.01589977993944));
#5376=CARTESIAN_POINT('Ctrl Pts',(-2.00000000000579,39.8408836611054,-0.61470152310314));
#5377=CARTESIAN_POINT('Ctrl Pts',(-1.99999999998774,39.7613743993598,-0.0949461097254665));
#5378=CARTESIAN_POINT('',(-2.24999999999999,40.0000000000105,4.08006961549745E-12));
#5379=CARTESIAN_POINT('Origin',(-1.99953720054553,40.0004045586706,0.000160968780395163));
#5380=CARTESIAN_POINT('',(-2.00000000002568,40.247426591683,0.0357782298078905));
#5381=CARTESIAN_POINT('Origin',(-1.99999999999999,40.0000000000001,-6.24500451351651E-14));
#5382=CARTESIAN_POINT('Ctrl Pts',(-2.00000000001811,42.8890026416775,-1.69451425055565));
#5383=CARTESIAN_POINT('Ctrl Pts',(-2.00000000001811,42.7138340471106,-1.69451425055564));
#5384=CARTESIAN_POINT('Ctrl Pts',(-2.00000000001811,42.5195868694293,-1.69664685121079));
#5385=CARTESIAN_POINT('Ctrl Pts',(-2.00000000001818,42.1727041659024,-1.69763022720131));
#5386=CARTESIAN_POINT('Ctrl Pts',(-2.00000000001809,42.0075453806213,-1.69643582812033));
#5387=CARTESIAN_POINT('Ctrl Pts',(-2.000000000018,41.5447432182596,-1.67506238348623));
#5388=CARTESIAN_POINT('Ctrl Pts',(-2.00000000001759,41.2824586218001,-1.63529714422004));
#5389=CARTESIAN_POINT('Ctrl Pts',(-2.00000000001559,40.8726877368524,-1.45751662005935));
#5390=CARTESIAN_POINT('Ctrl Pts',(-2.00000000001428,40.7146168625301,-1.32576584773803));
#5391=CARTESIAN_POINT('Ctrl Pts',(-2.00000000000915,40.4347106414413,-0.836444527344903));
#5392=CARTESIAN_POINT('Ctrl Pts',(-2.00000000000487,40.3213171458309,-0.475216515464907));
#5393=CARTESIAN_POINT('Ctrl Pts',(-2.00000000002568,40.247426591683,0.0357782298078905));
#5394=CARTESIAN_POINT('Ctrl Pts',(-2.,-0.264726219523816,0.141138331776411));
#5395=CARTESIAN_POINT('Ctrl Pts',(-1.93317897182823,-0.140204737359338,
0.374697162628536));
#5396=CARTESIAN_POINT('Ctrl Pts',(-1.89576248628645,-0.0714193310070166,
0.563392832565318));
#5397=CARTESIAN_POINT('Ctrl Pts',(-1.85828016234107,-0.0141476745355931,
0.845995304749381));
#5398=CARTESIAN_POINT('Ctrl Pts',(-1.85721582540971,-0.0237125088868792,
0.935184056400945));
#5399=CARTESIAN_POINT('Ctrl Pts',(-1.86061638209651,-0.0666740172427863,
1.06187361715673));
#5400=CARTESIAN_POINT('Ctrl Pts',(-1.86640738686477,-0.101672715288381,
1.11012925637074));
#5401=CARTESIAN_POINT('Ctrl Pts',(-1.88833554246329,-0.235746153313808,
1.21545234876845));
#5402=CARTESIAN_POINT('Ctrl Pts',(-1.9033753276643,-0.335251316849042,1.26604967753693));
#5403=CARTESIAN_POINT('Ctrl Pts',(-1.9189176957612,-0.518726439558199,1.34035163842065));
#5404=CARTESIAN_POINT('Ctrl Pts',(-1.92137116451861,-0.585485291115871,
1.36832017615168));
#5405=CARTESIAN_POINT('Ctrl Pts',(-1.93896943688162,-0.724455435049461,
1.40322870297494));
#5406=CARTESIAN_POINT('Ctrl Pts',(-1.95325668725115,-0.796545227124419,
1.40888781048668));
#5407=CARTESIAN_POINT('Ctrl Pts',(-1.99209925627655,-1.01599260874888,1.41219882843878));
#5408=CARTESIAN_POINT('Ctrl Pts',(-2.00898122237353,-1.16761549888469,1.40420126611032));
#5409=CARTESIAN_POINT('Ctrl Pts',(-2.01271588366055,-1.60175062040053,1.36576567629003));
#5410=CARTESIAN_POINT('Ctrl Pts',(-1.95046360827934,-1.85129221142242,1.32547580954877));
#5411=CARTESIAN_POINT('Ctrl Pts',(-1.69792570410908,-2.14007513561928,1.27973035876422));
#5412=CARTESIAN_POINT('Ctrl Pts',(-1.50788517190343,-2.24578075342313,1.26508664601861));
#5413=CARTESIAN_POINT('Ctrl Pts',(-1.03351721040672,-2.37409803162741,1.24662061906772));
#5414=CARTESIAN_POINT('Ctrl Pts',(-0.753928362614793,-2.39679255199907,
1.24243205928811));
#5415=CARTESIAN_POINT('Ctrl Pts',(-0.218845999430284,-2.35785399723118,
1.24055602083421));
#5416=CARTESIAN_POINT('Ctrl Pts',(0.0368662467341799,-2.29519092886669,
1.24322556456469));
#5417=CARTESIAN_POINT('Ctrl Pts',(0.411239882065782,-2.11406967659605,1.2495991139221));
#5418=CARTESIAN_POINT('Ctrl Pts',(0.518384719875618,-2.00298884738698,1.25072899682664));
#5419=CARTESIAN_POINT('Ctrl Pts',(0.571801954928687,-1.83523605217566,1.25334679757698));
#5420=CARTESIAN_POINT('Ctrl Pts',(0.569023344394799,-1.74044478899434,1.25599881503435));
#5421=CARTESIAN_POINT('Ctrl Pts',(0.494126240428662,-1.50788563057796,1.25886663470126));
#5422=CARTESIAN_POINT('Ctrl Pts',(0.421606239831573,-1.37485017740085,1.26041038383949));
#5423=CARTESIAN_POINT('Ctrl Pts',(0.127609128452456,-0.989034614321357,
1.26907008807672));
#5424=CARTESIAN_POINT('Ctrl Pts',(-0.170570542490676,-0.751894328558357,
1.28023791867232));
#5425=CARTESIAN_POINT('Ctrl Pts',(-0.569600762546571,-0.586703644418381,
1.30640573381989));
#5426=CARTESIAN_POINT('Ctrl Pts',(-0.692371618949951,-0.563856396440986,
1.31685387723007));
#5427=CARTESIAN_POINT('Ctrl Pts',(-0.882581236630141,-0.577499841895708,
1.33968897633028));
#5428=CARTESIAN_POINT('Ctrl Pts',(-0.949730803773584,-0.6053755874494,1.35084566027416));
#5429=CARTESIAN_POINT('Ctrl Pts',(-1.08267031338154,-0.742643707380371,
1.38530535019886));
#5430=CARTESIAN_POINT('Ctrl Pts',(-1.14980571385887,-0.863823663666268,
1.41045379245241));
#5431=CARTESIAN_POINT('Ctrl Pts',(-1.22863752459304,-1.27359538565792,1.48274964800499));
#5432=CARTESIAN_POINT('Ctrl Pts',(-1.23841278692706,-1.55826711159036,1.52914339518866));
#5433=CARTESIAN_POINT('Ctrl Pts',(-1.19858468901873,-1.92998306793573,1.58589472341859));
#5434=CARTESIAN_POINT('Ctrl Pts',(-1.41479497306135,-0.327024714779108,
0.0242881116882445));
#5435=CARTESIAN_POINT('Ctrl Pts',(-1.34348834763361,-0.181249481177505,
0.268980137453439));
#5436=CARTESIAN_POINT('Ctrl Pts',(-1.3008279414714,-0.0880635038225108,
0.476394018094572));
#5437=CARTESIAN_POINT('Ctrl Pts',(-1.25754057161045,0.0123013660558204,
0.831666797361881));
#5438=CARTESIAN_POINT('Ctrl Pts',(-1.25687388480527,0.0194522591100595,
0.979479411006855));
#5439=CARTESIAN_POINT('Ctrl Pts',(-1.2830830371466,-0.0336379080354797,
1.23391882276437));
#5440=CARTESIAN_POINT('Ctrl Pts',(-1.30959041125068,-0.0938600720654208,
1.34021747917579));
#5441=CARTESIAN_POINT('Ctrl Pts',(-1.38041341547889,-0.261824969553754,
1.53853407301497));
#5442=CARTESIAN_POINT('Ctrl Pts',(-1.42362766577653,-0.369411940643664,
1.63197959161429));
#5443=CARTESIAN_POINT('Ctrl Pts',(-1.51482462448403,-0.553055900414141,
1.7840154902546));
#5444=CARTESIAN_POINT('Ctrl Pts',(-1.55452145207106,-0.616871235334267,
1.84288502733572));
#5445=CARTESIAN_POINT('Ctrl Pts',(-1.61769237293684,-0.76088554847919,1.90941994885935));
#5446=CARTESIAN_POINT('Ctrl Pts',(-1.63741652204799,-0.839819060706829,
1.91721278463516));
#5447=CARTESIAN_POINT('Ctrl Pts',(-1.67857813189676,-1.07311708366726,1.92065626175757));
#5448=CARTESIAN_POINT('Ctrl Pts',(-1.69450638574114,-1.22468485755413,1.91207917479615));
#5449=CARTESIAN_POINT('Ctrl Pts',(-1.69776273723848,-1.63025676912522,1.87601769283407));
#5450=CARTESIAN_POINT('Ctrl Pts',(-1.63558587031057,-1.8094473554909,1.8484014728917));
#5451=CARTESIAN_POINT('Ctrl Pts',(-1.51744170723058,-1.93391724344097,1.82161070104937));
#5452=CARTESIAN_POINT('Ctrl Pts',(-1.38720614355509,-2.01215777720118,1.80651658245784));
#5453=CARTESIAN_POINT('Ctrl Pts',(-0.999318445532683,-2.1000372109959,1.78142022672165));
#5454=CARTESIAN_POINT('Ctrl Pts',(-0.75320228279494,-2.109345485096,1.77049841986191));
#5455=CARTESIAN_POINT('Ctrl Pts',(-0.291144343481196,-2.05182844476988,
1.75300283223748));
#5456=CARTESIAN_POINT('Ctrl Pts',(-0.0746276920240247,-1.98390441220646,
1.74716065612451));
#5457=CARTESIAN_POINT('Ctrl Pts',(0.192072445804306,-1.83915272276575,1.73915712563726));
#5458=CARTESIAN_POINT('Ctrl Pts',(0.210347585325089,-1.77773490581458,1.73080489996179));
#5459=CARTESIAN_POINT('Ctrl Pts',(0.198976982175155,-1.81462152515841,1.73113541660097));
#5460=CARTESIAN_POINT('Ctrl Pts',(0.213011996067426,-1.79205629656322,1.73877515384333));
#5461=CARTESIAN_POINT('Ctrl Pts',(0.177186567758258,-1.65070903664641,1.7504269870299));
#5462=CARTESIAN_POINT('Ctrl Pts',(0.129908624188708,-1.54404411523484,1.75773877200305));
#5463=CARTESIAN_POINT('Ctrl Pts',(-0.0876107518951426,-1.21505608778235,
1.78559033317587));
#5464=CARTESIAN_POINT('Ctrl Pts',(-0.337497876869364,-0.989695956702306,
1.81129298511067));
#5465=CARTESIAN_POINT('Ctrl Pts',(-0.619417429815987,-0.851281642971048,
1.84410939565886));
#5466=CARTESIAN_POINT('Ctrl Pts',(-0.691821618472955,-0.839216119419207,
1.85456575460658));
#5467=CARTESIAN_POINT('Ctrl Pts',(-0.742506322151624,-0.836948971076064,
1.86696729841403));
#5468=CARTESIAN_POINT('Ctrl Pts',(-0.720038690828119,-0.826234748910869,
1.86596691745099));
#5469=CARTESIAN_POINT('Ctrl Pts',(-0.741001371120147,-0.843622783703197,
1.87515508429125));
#5470=CARTESIAN_POINT('Ctrl Pts',(-0.787635764756597,-0.899635885793011,
1.88970955146323));
#5471=CARTESIAN_POINT('Ctrl Pts',(-0.852118294742336,-1.21903207139812,
1.94900258458685));
#5472=CARTESIAN_POINT('Ctrl Pts',(-0.865431353370241,-1.47313529513962,
1.99195746223939));
#5473=CARTESIAN_POINT('Ctrl Pts',(-0.829509728173782,-1.82164035961998,
2.04637874141716));
#5474=CARTESIAN_POINT('Ctrl Pts',(-1.41479497306136,0.202427724268475,-0.257988551864688));
#5475=CARTESIAN_POINT('Ctrl Pts',(-1.34782648899619,0.367997360937599,0.023830846800561));
#5476=CARTESIAN_POINT('Ctrl Pts',(-1.30808707499932,0.484781686762276,0.280931411872746));
#5477=CARTESIAN_POINT('Ctrl Pts',(-1.27980253042162,0.615948260124595,0.792619532033457));
#5478=CARTESIAN_POINT('Ctrl Pts',(-1.29321476237305,0.626404567290167,1.05659684088554));
#5479=CARTESIAN_POINT('Ctrl Pts',(-1.38946357811,0.488938846353634,1.53600410055517));
#5480=CARTESIAN_POINT('Ctrl Pts',(-1.46927966447622,0.34423952699714,1.72959611556546));
#5481=CARTESIAN_POINT('Ctrl Pts',(-1.64804633832672,0.0351654638783543,
1.99593663738672));
#5482=CARTESIAN_POINT('Ctrl Pts',(-1.74809047347069,-0.128192913728382,
2.08305283586927));
#5483=CARTESIAN_POINT('Ctrl Pts',(-1.93188952347472,-0.373532157725284,
2.17842710957436));
#5484=CARTESIAN_POINT('Ctrl Pts',(-2.00679552031709,-0.454457191434216,
2.20361434518665));
#5485=CARTESIAN_POINT('Ctrl Pts',(-2.10891108326887,-0.632484078259461,
2.2307813240385));
#5486=CARTESIAN_POINT('Ctrl Pts',(-2.13408587854556,-0.728563548890991,
2.23545023463704));
#5487=CARTESIAN_POINT('Ctrl Pts',(-2.18470343784499,-1.01580120595979,2.23985105426332));
#5488=CARTESIAN_POINT('Ctrl Pts',(-2.20504953495422,-1.20449005728727,2.22965055680831));
#5489=CARTESIAN_POINT('Ctrl Pts',(-2.20926209776938,-1.74080899784122,2.18228791128134));
#5490=CARTESIAN_POINT('Ctrl Pts',(-2.13571406139752,-2.05748394873335,2.12938063388729));
#5491=CARTESIAN_POINT('Ctrl Pts',(-1.80914039490605,-2.4116424454986,2.07707686166329));
#5492=CARTESIAN_POINT('Ctrl Pts',(-1.58558544675306,-2.52101501223511,2.06437413078064));
#5493=CARTESIAN_POINT('Ctrl Pts',(-1.06274917012361,-2.63535508293751,2.05380211046861));
#5494=CARTESIAN_POINT('Ctrl Pts',(-0.765526424774163,-2.63982623851908,
2.05574575179177));
#5495=CARTESIAN_POINT('Ctrl Pts',(-0.201198256641021,-2.55922793898205,
2.06506565863797));
#5496=CARTESIAN_POINT('Ctrl Pts',(0.0660448366282887,-2.47511972447648,
2.07245950804548));
#5497=CARTESIAN_POINT('Ctrl Pts',(0.475148760175511,-2.24745677674094,2.08564829134537));
#5498=CARTESIAN_POINT('Ctrl Pts',(0.608134614732898,-2.10455710556735,2.09040062351607));
#5499=CARTESIAN_POINT('Ctrl Pts',(0.692807377742016,-1.84294516771091,2.09414100985965));
#5500=CARTESIAN_POINT('Ctrl Pts',(0.695288539321058,-1.71667259554446,2.09510414856687));
#5501=CARTESIAN_POINT('Ctrl Pts',(0.624899286559479,-1.43522068083482,2.09446462416269));
#5502=CARTESIAN_POINT('Ctrl Pts',(0.555414215357652,-1.2826933626758,2.0935057350151));
#5503=CARTESIAN_POINT('Ctrl Pts',(0.273957080557801,-0.835699802377016,
2.09178023085904));
#5504=CARTESIAN_POINT('Ctrl Pts',(-0.0144466890476935,-0.553079604701429,
2.09136454656141));
#5505=CARTESIAN_POINT('Ctrl Pts',(-0.45094860176887,-0.336574440271572,
2.10878602648762));
#5506=CARTESIAN_POINT('Ctrl Pts',(-0.595413630263608,-0.298852315146673,
2.11776209928019));
#5507=CARTESIAN_POINT('Ctrl Pts',(-0.85098489192329,-0.305627887932605,
2.14353553496541));
#5508=CARTESIAN_POINT('Ctrl Pts',(-0.96192160586922,-0.346842648185032,
2.15984784684465));
#5509=CARTESIAN_POINT('Ctrl Pts',(-1.15250413694999,-0.533505951798014,
2.20558401172234));
#5510=CARTESIAN_POINT('Ctrl Pts',(-1.23266332711506,-0.683289971881234,
2.23568288668276));
#5511=CARTESIAN_POINT('Ctrl Pts',(-1.32515666438693,-1.13327359192835,2.31428720538256));
#5512=CARTESIAN_POINT('Ctrl Pts',(-1.33679811649895,-1.43203332580916,2.36251628262105));
#5513=CARTESIAN_POINT('Ctrl Pts',(-1.29844891076763,-1.81475034924797,2.42060937990806));
#5514=CARTESIAN_POINT('Ctrl Pts',(-1.99999999999999,0.264726219523767,-0.14113833177655));
#5515=CARTESIAN_POINT('Ctrl Pts',(-1.93751711319081,0.409042104755758,0.129547871975604));
#5516=CARTESIAN_POINT('Ctrl Pts',(-1.9030216198144,0.501425859577798,0.367930226343516));
#5517=CARTESIAN_POINT('Ctrl Pts',(-1.88054212115223,0.589499219533149,0.806948039420934));
#5518=CARTESIAN_POINT('Ctrl Pts',(-1.89355670297749,0.583239799293228,1.01230148627963));
#5519=CARTESIAN_POINT('Ctrl Pts',(-1.96699692305992,0.455902737146338,1.36395889494755));
#5520=CARTESIAN_POINT('Ctrl Pts',(-2.02609664009031,0.336426883774145,1.4995078927604));
#5521=CARTESIAN_POINT('Ctrl Pts',(-2.15596846531113,0.0612442801182847,
1.67285491314019));
#5522=CARTESIAN_POINT('Ctrl Pts',(-2.22783813535845,-0.0940322899337931,
1.71712292179187));
#5523=CARTESIAN_POINT('Ctrl Pts',(-2.33598259475191,-0.33920269686933,1.73476325774032));
#5524=CARTESIAN_POINT('Ctrl Pts',(-2.37364523276466,-0.423071247215849,
1.72904949400271));
#5525=CARTESIAN_POINT('Ctrl Pts',(-2.43018814721365,-0.596053964829743,
1.72459007815411));
#5526=CARTESIAN_POINT('Ctrl Pts',(-2.44992604374876,-0.685289715308575,
1.72712526048845));
#5527=CARTESIAN_POINT('Ctrl Pts',(-2.49822456222477,-0.958676731041413,
1.73139362094456));
#5528=CARTESIAN_POINT('Ctrl Pts',(-2.51952437158661,-1.14742069861778,1.72177264812241));
#5529=CARTESIAN_POINT('Ctrl Pts',(-2.52421524419146,-1.71230284911647,1.67203589473725));
#5530=CARTESIAN_POINT('Ctrl Pts',(-2.45059179936626,-2.09932880466486,1.60645497054434));
#5531=CARTESIAN_POINT('Ctrl Pts',(-1.98962439178456,-2.61780033767695,1.53519651937827));
#5532=CARTESIAN_POINT('Ctrl Pts',(-1.70626447510137,-2.75463798845714,1.52294419434135));
#5533=CARTESIAN_POINT('Ctrl Pts',(-1.09694793499771,-2.90941590356896,1.5190025028147));
#5534=CARTESIAN_POINT('Ctrl Pts',(-0.766252504594009,-2.92727330542218,
1.52767939121794));
#5535=CARTESIAN_POINT('Ctrl Pts',(-0.128899912590116,-2.86525349144335,
1.55261884723468));
#5536=CARTESIAN_POINT('Ctrl Pts',(0.177538775386479,-2.78640624113666,1.56852441648561));
#5537=CARTESIAN_POINT('Ctrl Pts',(0.694316196436971,-2.52237373057128,1.59609027963019));
#5538=CARTESIAN_POINT('Ctrl Pts',(0.916171749283459,-2.32981104713974,1.610324720381));
#5539=CARTESIAN_POINT('Ctrl Pts',(1.06563235049552,-1.86355969472816,1.61635239083565));
#5540=CARTESIAN_POINT('Ctrl Pts',(1.05129988764842,-1.66506108797555,1.61232780975798));
#5541=CARTESIAN_POINT('Ctrl Pts',(0.941838959229918,-1.29239727476634,1.60290427183405));
#5542=CARTESIAN_POINT('Ctrl Pts',(0.847111831000521,-1.11349942484178,1.59617734685152));
#5543=CARTESIAN_POINT('Ctrl Pts',(0.48917696090542,-0.609678328916015,1.57525998575984));
#5544=CARTESIAN_POINT('Ctrl Pts',(0.152480645331013,-0.315277976557456,
1.560309480123));
#5545=CARTESIAN_POINT('Ctrl Pts',(-0.401131934499451,-0.0719964417188537,
1.57108236464872));
#5546=CARTESIAN_POINT('Ctrl Pts',(-0.595963630740598,-0.0234925921684045,
1.58005022190368));
#5547=CARTESIAN_POINT('Ctrl Pts',(-0.99105980640179,-0.0461787587522702,
1.61625721288154));
#5548=CARTESIAN_POINT('Ctrl Pts',(-1.19161371881466,-0.12598348672354,1.64472658966789));
#5549=CARTESIAN_POINT('Ctrl Pts',(-1.49417307921139,-0.432526875475132,
1.71573427762991));
#5550=CARTESIAN_POINT('Ctrl Pts',(-1.5948332762173,-0.647477749754412,1.75642712767188));
#5551=CARTESIAN_POINT('Ctrl Pts',(-1.70167589423767,-1.18783690618816,1.84803426880073));
#5552=CARTESIAN_POINT('Ctrl Pts',(-1.70977955005583,-1.51716514225989,1.89970221556995));
#5553=CARTESIAN_POINT('Ctrl Pts',(-1.66752387161256,-1.92309305756368,1.96012536190953));
#5554=CARTESIAN_POINT('Ctrl Pts',(-2.58520502693868,0.327024714779061,-0.0242881116882809));
#5555=CARTESIAN_POINT('Ctrl Pts',(-2.52720773738545,0.450086848573887,0.235264897150667));
#5556=CARTESIAN_POINT('Ctrl Pts',(-2.49795616462949,0.518070032393306,0.45492904081419));
#5557=CARTESIAN_POINT('Ctrl Pts',(-2.48128171188284,0.563050178941749,0.821276546808376));
#5558=CARTESIAN_POINT('Ctrl Pts',(-2.49389864358196,0.540075031296315,0.968006131673827));
#5559=CARTESIAN_POINT('Ctrl Pts',(-2.54453026800985,0.422866627938986,1.19191368933997));
#5560=CARTESIAN_POINT('Ctrl Pts',(-2.58291361570442,0.32861424055116,1.26941966995528));
#5561=CARTESIAN_POINT('Ctrl Pts',(-2.66389059229556,0.0873230963582133,
1.34977318889387));
#5562=CARTESIAN_POINT('Ctrl Pts',(-2.70758579724625,-0.0598716661391885,
1.35119300771448));
#5563=CARTESIAN_POINT('Ctrl Pts',(-2.74007566602911,-0.304873236013411,
1.29109940590619));
#5564=CARTESIAN_POINT('Ctrl Pts',(-2.74049494521224,-0.391685302997432,
1.25448464281861));
#5565=CARTESIAN_POINT('Ctrl Pts',(-2.75146521115844,-0.559623851400008,
1.21839883226965));
#5566=CARTESIAN_POINT('Ctrl Pts',(-2.76576620895198,-0.642015881726228,
1.21880028633987));
#5567=CARTESIAN_POINT('Ctrl Pts',(-2.81174568660457,-0.901552256123071,
1.22293618762564));
#5568=CARTESIAN_POINT('Ctrl Pts',(-2.83399920821904,-1.09035133994834,1.21389473943648));
#5569=CARTESIAN_POINT('Ctrl Pts',(-2.83916839061358,-1.68379670039174,1.16178387819315));
#5570=CARTESIAN_POINT('Ctrl Pts',(-2.76546953733502,-2.14117366059643,1.08352930720148));
#5571=CARTESIAN_POINT('Ctrl Pts',(-2.17010838866312,-2.82395822985523,0.99331617709322));
#5572=CARTESIAN_POINT('Ctrl Pts',(-1.8269435034497,-2.98826096467916,0.981514257902072));
#5573=CARTESIAN_POINT('Ctrl Pts',(-1.13114669987181,-3.18347672420042,0.984202895160761));
#5574=CARTESIAN_POINT('Ctrl Pts',(-0.766978584413879,-3.21472037232524,
0.99961303064418));
#5575=CARTESIAN_POINT('Ctrl Pts',(-0.0566015685392616,-3.1712790439046,
1.04017203583152));
#5576=CARTESIAN_POINT('Ctrl Pts',(0.289032714144647,-3.09769275779683,1.0645893249258));
#5577=CARTESIAN_POINT('Ctrl Pts',(0.913483632698393,-2.79729068440162,1.10653226791493));
#5578=CARTESIAN_POINT('Ctrl Pts',(1.22420888383399,-2.55506498871208,1.13024881724595));
#5579=CARTESIAN_POINT('Ctrl Pts',(1.43845732324901,-1.88417422174541,1.13856377181168));
#5580=CARTESIAN_POINT('Ctrl Pts',(1.40731123597572,-1.61344958040663,1.12955147094911));
#5581=CARTESIAN_POINT('Ctrl Pts',(1.25877863190032,-1.14957386869789,1.11134391950535));
#5582=CARTESIAN_POINT('Ctrl Pts',(1.13880944664334,-0.944305487007855,1.09884895868796));
#5583=CARTESIAN_POINT('Ctrl Pts',(0.704396841252997,-0.383656855455022,
1.05873974066059));
#5584=CARTESIAN_POINT('Ctrl Pts',(0.3194079797097,-0.0774763484135167,1.02925441368461));
#5585=CARTESIAN_POINT('Ctrl Pts',(-0.351315267230051,0.19258155683384,1.03337870280986));
#5586=CARTESIAN_POINT('Ctrl Pts',(-0.596513631217612,0.251867130809852,
1.0423383445272));
#5587=CARTESIAN_POINT('Ctrl Pts',(-1.13113472088033,0.213270370428087,1.08897889079772));
#5588=CARTESIAN_POINT('Ctrl Pts',(-1.42130583176012,0.0948756747378918,
1.12960533249102));
#5589=CARTESIAN_POINT('Ctrl Pts',(-1.83584202147282,-0.331547799152291,
1.22588454353743));
#5590=CARTESIAN_POINT('Ctrl Pts',(-1.95700322531958,-0.611665527627663,
1.277171368661));
#5591=CARTESIAN_POINT('Ctrl Pts',(-2.07819512408842,-1.242400220448,1.38178133221873));
#5592=CARTESIAN_POINT('Ctrl Pts',(-2.08276098361269,-1.6022969587106,1.43688814851895));
#5593=CARTESIAN_POINT('Ctrl Pts',(-2.03659883245755,-2.03143576587941,1.49964134391094));
#5594=CARTESIAN_POINT('Ctrl Pts',(-2.58520502693868,-0.202427724268506,
0.257988551864641));
#5595=CARTESIAN_POINT('Ctrl Pts',(-2.52286959602286,-0.0991599935411917,
0.480414187803598));
#5596=CARTESIAN_POINT('Ctrl Pts',(-2.49069703110151,-0.0547751581915275,
0.650391647036053));
#5597=CARTESIAN_POINT('Ctrl Pts',(-2.45901975307171,-0.0405967151270361,
0.860323812136826));
#5598=CARTESIAN_POINT('Ctrl Pts',(-2.45755776601418,-0.0668772768837554,
0.890888701795052));
#5599=CARTESIAN_POINT('Ctrl Pts',(-2.43814972704647,-0.0997101264501223,
0.889828411549012));
#5600=CARTESIAN_POINT('Ctrl Pts',(-2.42322436247891,-0.109485358511338,
0.880041033565627));
#5601=CARTESIAN_POINT('Ctrl Pts',(-2.39625766944769,-0.209667337073921,
0.892370624522099));
#5602=CARTESIAN_POINT('Ctrl Pts',(-2.38312298955208,-0.301090693054413,
0.900119763459602));
#5603=CARTESIAN_POINT('Ctrl Pts',(-2.32301076703839,-0.484396978702216,
0.896687786586603));
#5604=CARTESIAN_POINT('Ctrl Pts',(-2.2882208769662,-0.554099346897494,0.893755324967696));
#5605=CARTESIAN_POINT('Ctrl Pts',(-2.26024650082642,-0.688025321619785,
0.897037457090494));
#5606=CARTESIAN_POINT('Ctrl Pts',(-2.26909685245436,-0.753271393542086,
0.90056283633815));
#5607=CARTESIAN_POINT('Ctrl Pts',(-2.30562038065636,-0.958868133830514,
0.903741395119929));
#5608=CARTESIAN_POINT('Ctrl Pts',(-2.32345605900597,-1.11054614021518,0.896323357424417));
#5609=CARTESIAN_POINT('Ctrl Pts',(-2.32766903008263,-1.57324447167574,0.855513659745901));
#5610=CARTESIAN_POINT('Ctrl Pts',(-2.26534134624811,-1.89313706735396,0.802550146205944));
#5611=CARTESIAN_POINT('Ctrl Pts',(-1.8784097009876,-2.34623302779759,0.737850016479276));
#5612=CARTESIAN_POINT('Ctrl Pts',(-1.62856420025181,-2.47940372964513,0.723656709579273));
#5613=CARTESIAN_POINT('Ctrl Pts',(-1.0677159752808,-2.64815885225886,0.711821011413811));
#5614=CARTESIAN_POINT('Ctrl Pts',(-0.754654442434687,-2.68423961890214,
0.7143656987144));
#5615=CARTESIAN_POINT('Ctrl Pts',(-0.146547655379389,-2.66387954969245,
0.728109209430922));
#5616=CARTESIAN_POINT('Ctrl Pts',(0.148360185492318,-2.60647744552693,0.739290473004851));
#5617=CARTESIAN_POINT('Ctrl Pts',(0.630407318327205,-2.38898663042632,0.760041102206871));
#5618=CARTESIAN_POINT('Ctrl Pts',(0.826421854426146,-2.22824278895934,0.770653093691493));
#5619=CARTESIAN_POINT('Ctrl Pts',(0.944626927682175,-1.85585057919288,0.775558178553095));
#5620=CARTESIAN_POINT('Ctrl Pts',(0.925034692722124,-1.68883328142547,0.773222476225436));
#5621=CARTESIAN_POINT('Ctrl Pts',(0.811065913099062,-1.36506222450943,0.767306282372666));
#5622=CARTESIAN_POINT('Ctrl Pts',(0.713303855474414,-1.20565623956688,0.763081995675995));
#5623=CARTESIAN_POINT('Ctrl Pts',(0.34282900880003,-0.763013140860391,0.752549842977497));
#5624=CARTESIAN_POINT('Ctrl Pts',(-0.00364320811200702,-0.51409270041443,
0.749182852233819));
#5625=CARTESIAN_POINT('Ctrl Pts',(-0.51978409527715,-0.322125645865647,
0.768702071980997));
#5626=CARTESIAN_POINT('Ctrl Pts',(-0.692921619426966,-0.288496673462745,
0.779141999853542));
#5627=CARTESIAN_POINT('Ctrl Pts',(-1.02265615110868,-0.318050712715351,
0.812410654246396));
#5628=CARTESIAN_POINT('Ctrl Pts',(-1.17942291671907,-0.38451642598792,0.835724403097336));
#5629=CARTESIAN_POINT('Ctrl Pts',(-1.42433925564296,-0.641664631057489,
0.895455616106331));
#5630=CARTESIAN_POINT('Ctrl Pts',(-1.51197566296117,-0.828011441539482,
0.931198033441523));
#5631=CARTESIAN_POINT('Ctrl Pts',(-1.60515675444377,-1.32815869991775,1.016496711423));
#5632=CARTESIAN_POINT('Ctrl Pts',(-1.61139422048387,-1.6433989280412,1.06632932813794));
#5633=CARTESIAN_POINT('Ctrl Pts',(-1.5676596498637,-2.03832577625143,1.12541070542012));
#5634=CARTESIAN_POINT('Ctrl Pts',(-2.,-0.264726219523816,0.141138331776411));
#5635=CARTESIAN_POINT('Ctrl Pts',(-1.93317897182823,-0.140204737359338,
0.374697162628536));
#5636=CARTESIAN_POINT('Ctrl Pts',(-1.89576248628645,-0.0714193310070166,
0.563392832565318));
#5637=CARTESIAN_POINT('Ctrl Pts',(-1.85828016234107,-0.0141476745355931,
0.845995304749381));
#5638=CARTESIAN_POINT('Ctrl Pts',(-1.85721582540971,-0.0237125088868792,
0.935184056400945));
#5639=CARTESIAN_POINT('Ctrl Pts',(-1.86061638209651,-0.0666740172427863,
1.06187361715673));
#5640=CARTESIAN_POINT('Ctrl Pts',(-1.86640738686477,-0.101672715288381,
1.11012925637074));
#5641=CARTESIAN_POINT('Ctrl Pts',(-1.88833554246329,-0.235746153313808,
1.21545234876845));
#5642=CARTESIAN_POINT('Ctrl Pts',(-1.9033753276643,-0.335251316849042,1.26604967753693));
#5643=CARTESIAN_POINT('Ctrl Pts',(-1.9189176957612,-0.518726439558199,1.34035163842065));
#5644=CARTESIAN_POINT('Ctrl Pts',(-1.92137116451861,-0.585485291115871,
1.36832017615168));
#5645=CARTESIAN_POINT('Ctrl Pts',(-1.93896943688162,-0.724455435049461,
1.40322870297494));
#5646=CARTESIAN_POINT('Ctrl Pts',(-1.95325668725115,-0.796545227124419,
1.40888781048668));
#5647=CARTESIAN_POINT('Ctrl Pts',(-1.99209925627655,-1.01599260874888,1.41219882843878));
#5648=CARTESIAN_POINT('Ctrl Pts',(-2.00898122237353,-1.16761549888469,1.40420126611032));
#5649=CARTESIAN_POINT('Ctrl Pts',(-2.01271588366055,-1.60175062040053,1.36576567629003));
#5650=CARTESIAN_POINT('Ctrl Pts',(-1.95046360827934,-1.85129221142242,1.32547580954877));
#5651=CARTESIAN_POINT('Ctrl Pts',(-1.69792570410908,-2.14007513561928,1.27973035876422));
#5652=CARTESIAN_POINT('Ctrl Pts',(-1.50788517190343,-2.24578075342313,1.26508664601861));
#5653=CARTESIAN_POINT('Ctrl Pts',(-1.03351721040672,-2.37409803162741,1.24662061906772));
#5654=CARTESIAN_POINT('Ctrl Pts',(-0.753928362614793,-2.39679255199907,
1.24243205928811));
#5655=CARTESIAN_POINT('Ctrl Pts',(-0.218845999430284,-2.35785399723118,
1.24055602083421));
#5656=CARTESIAN_POINT('Ctrl Pts',(0.0368662467341799,-2.29519092886669,
1.24322556456469));
#5657=CARTESIAN_POINT('Ctrl Pts',(0.411239882065782,-2.11406967659605,1.2495991139221));
#5658=CARTESIAN_POINT('Ctrl Pts',(0.518384719875618,-2.00298884738698,1.25072899682664));
#5659=CARTESIAN_POINT('Ctrl Pts',(0.571801954928687,-1.83523605217566,1.25334679757698));
#5660=CARTESIAN_POINT('Ctrl Pts',(0.569023344394799,-1.74044478899434,1.25599881503435));
#5661=CARTESIAN_POINT('Ctrl Pts',(0.494126240428662,-1.50788563057796,1.25886663470126));
#5662=CARTESIAN_POINT('Ctrl Pts',(0.421606239831573,-1.37485017740085,1.26041038383949));
#5663=CARTESIAN_POINT('Ctrl Pts',(0.127609128452456,-0.989034614321357,
1.26907008807672));
#5664=CARTESIAN_POINT('Ctrl Pts',(-0.170570542490676,-0.751894328558357,
1.28023791867232));
#5665=CARTESIAN_POINT('Ctrl Pts',(-0.569600762546571,-0.586703644418381,
1.30640573381989));
#5666=CARTESIAN_POINT('Ctrl Pts',(-0.692371618949951,-0.563856396440986,
1.31685387723007));
#5667=CARTESIAN_POINT('Ctrl Pts',(-0.882581236630141,-0.577499841895708,
1.33968897633028));
#5668=CARTESIAN_POINT('Ctrl Pts',(-0.949730803773584,-0.6053755874494,1.35084566027416));
#5669=CARTESIAN_POINT('Ctrl Pts',(-1.08267031338154,-0.742643707380371,
1.38530535019886));
#5670=CARTESIAN_POINT('Ctrl Pts',(-1.14980571385887,-0.863823663666268,
1.41045379245241));
#5671=CARTESIAN_POINT('Ctrl Pts',(-1.22863752459304,-1.27359538565792,1.48274964800499));
#5672=CARTESIAN_POINT('Ctrl Pts',(-1.23841278692706,-1.55826711159036,1.52914339518866));
#5673=CARTESIAN_POINT('Ctrl Pts',(-1.19858468901873,-1.92998306793573,1.58589472341859));
#5674=CARTESIAN_POINT('',(-1.7123707667093,-0.0792203553185641,-0.0315207782236257));
#5675=CARTESIAN_POINT('',(-1.97217110131402,0.328135292296241,-0.0174867429177148));
#5676=CARTESIAN_POINT('Ctrl Pts',(-1.71237076670932,-0.0792203554440619,
-0.0315207779082008));
#5677=CARTESIAN_POINT('Ctrl Pts',(-1.71225680255821,-0.0788631339014023,
-0.0313786429465269));
#5678=CARTESIAN_POINT('Ctrl Pts',(-1.71208823782772,-0.0782706097349225,
-0.0313418726165944));
#5679=CARTESIAN_POINT('Ctrl Pts',(-1.71157335911718,-0.0763326226625869,
-0.0314050208455891));
#5680=CARTESIAN_POINT('Ctrl Pts',(-1.71136778606381,-0.0755433059720559,
-0.0314456176241967));
#5681=CARTESIAN_POINT('Ctrl Pts',(-1.71086177270017,-0.0735744218851083,
-0.0315527227334411));
#5682=CARTESIAN_POINT('Ctrl Pts',(-1.71050659837137,-0.0721571984421657,
-0.0316391398449165));
#5683=CARTESIAN_POINT('Ctrl Pts',(-1.70947628057217,-0.0679313170811708,
-0.0318967502239478));
#5684=CARTESIAN_POINT('Ctrl Pts',(-1.70882852767769,-0.0651327994730381,
-0.0320693383888488));
#5685=CARTESIAN_POINT('Ctrl Pts',(-1.7069794858788,-0.0566966787293398,
-0.0325751880937715));
#5686=CARTESIAN_POINT('Ctrl Pts',(-1.70587853876313,-0.0510502238207176,
-0.0328976980002992));
#5687=CARTESIAN_POINT('Ctrl Pts',(-1.70296990262491,-0.0340398585560832,
-0.0338106570223856));
#5688=CARTESIAN_POINT('Ctrl Pts',(-1.70155701975247,-0.0226075766793059,
-0.0343482598789538));
#5689=CARTESIAN_POINT('Ctrl Pts',(-1.69895448923435,0.0115451283008395,
-0.0357337044930367));
#5690=CARTESIAN_POINT('Ctrl Pts',(-1.69932902938613,0.034374979625958,-0.0363725220507445));
#5691=CARTESIAN_POINT('Ctrl Pts',(-1.70678458981123,0.100203388283196,-0.0374512675022018));
#5692=CARTESIAN_POINT('Ctrl Pts',(-1.71963219235882,0.142271280888972,-0.0371798099524647));
#5693=CARTESIAN_POINT('Ctrl Pts',(-1.75844045789029,0.212695496528277,-0.0350857448847548));
#5694=CARTESIAN_POINT('Ctrl Pts',(-1.78187136755302,0.241571788518346,-0.0335185403772877));
#5695=CARTESIAN_POINT('Ctrl Pts',(-1.8355021662325,0.286103340279215,-0.0295180509329332));
#5696=CARTESIAN_POINT('Ctrl Pts',(-1.86409005060045,0.30238404614985,-0.0272408755264394));
#5697=CARTESIAN_POINT('Ctrl Pts',(-1.91989972762967,0.321892907016035,-0.0224470229788942));
#5698=CARTESIAN_POINT('Ctrl Pts',(-1.94585998817096,0.326883504438017,-0.0200983562132771));
#5699=CARTESIAN_POINT('Ctrl Pts',(-1.97217850583874,0.328104890351764,-0.0175485997260151));
#5700=CARTESIAN_POINT('',(-1.66752387161258,-1.92309305756372,1.96012536190956));
#5701=CARTESIAN_POINT('Ctrl Pts',(-1.9721636967893,0.328165694240719,-0.0174248861094145));
#5702=CARTESIAN_POINT('Ctrl Pts',(-1.96047851223817,0.356633337001664,0.0404871888707593));
#5703=CARTESIAN_POINT('Ctrl Pts',(-1.95013077049801,0.382355896985405,0.0964727267131344));
#5704=CARTESIAN_POINT('Ctrl Pts',(-1.93177358498602,0.429073484290914,0.206103730203931));
#5705=CARTESIAN_POINT('Ctrl Pts',(-1.92380662254987,0.449981339228045,0.259693515327892));
#5706=CARTESIAN_POINT('Ctrl Pts',(-1.91012545460458,0.487292465067314,0.365429133263016));
#5707=CARTESIAN_POINT('Ctrl Pts',(-1.90447531620791,0.503564356399332,0.417500925391009));
#5708=CARTESIAN_POINT('Ctrl Pts',(-1.89652758858992,0.528274529448912,0.508776271663394));
#5709=CARTESIAN_POINT('Ctrl Pts',(-1.89377973603894,0.537635019250509,0.54842142255703));
#5710=CARTESIAN_POINT('Ctrl Pts',(-1.88054212115223,0.589499219533149,0.806948039420934));
#5711=CARTESIAN_POINT('Ctrl Pts',(-1.89355670297749,0.583239799293228,1.01230148627963));
#5712=CARTESIAN_POINT('Ctrl Pts',(-1.96699692305992,0.455902737146338,1.36395889494755));
#5713=CARTESIAN_POINT('Ctrl Pts',(-2.0260966400903,0.336426883774145,1.4995078927604));
#5714=CARTESIAN_POINT('Ctrl Pts',(-2.15596846531112,0.0612442801182847,
1.67285491314019));
#5715=CARTESIAN_POINT('Ctrl Pts',(-2.22783813535845,-0.0940322899337932,
1.71712292179187));
#5716=CARTESIAN_POINT('Ctrl Pts',(-2.33598259475191,-0.33920269686933,1.73476325774032));
#5717=CARTESIAN_POINT('Ctrl Pts',(-2.37364523276466,-0.423071247215849,
1.72904949400271));
#5718=CARTESIAN_POINT('Ctrl Pts',(-2.43018814721365,-0.596053964829743,
1.72459007815411));
#5719=CARTESIAN_POINT('Ctrl Pts',(-2.44992604374876,-0.685289715308575,
1.72712526048845));
#5720=CARTESIAN_POINT('Ctrl Pts',(-2.49822456222477,-0.958676731041413,
1.73139362094456));
#5721=CARTESIAN_POINT('Ctrl Pts',(-2.51952437158661,-1.14742069861778,1.72177264812241));
#5722=CARTESIAN_POINT('Ctrl Pts',(-2.52421524419146,-1.71230284911647,1.67203589473725));
#5723=CARTESIAN_POINT('Ctrl Pts',(-2.45059179936626,-2.09932880466486,1.60645497054434));
#5724=CARTESIAN_POINT('Ctrl Pts',(-1.98962439178456,-2.61780033767695,1.53519651937827));
#5725=CARTESIAN_POINT('Ctrl Pts',(-1.70626447510137,-2.75463798845714,1.52294419434135));
#5726=CARTESIAN_POINT('Ctrl Pts',(-1.09694793499771,-2.90941590356896,1.51900250281471));
#5727=CARTESIAN_POINT('Ctrl Pts',(-0.766252504594009,-2.92727330542218,
1.52767939121794));
#5728=CARTESIAN_POINT('Ctrl Pts',(-0.128899912590115,-2.86525349144335,
1.55261884723468));
#5729=CARTESIAN_POINT('Ctrl Pts',(0.177538775386479,-2.78640624113666,1.56852441648561));
#5730=CARTESIAN_POINT('Ctrl Pts',(0.694316196436972,-2.52237373057128,1.59609027963019));
#5731=CARTESIAN_POINT('Ctrl Pts',(0.916171749283459,-2.32981104713974,1.610324720381));
#5732=CARTESIAN_POINT('Ctrl Pts',(1.06563235049552,-1.86355969472817,1.61635239083565));
#5733=CARTESIAN_POINT('Ctrl Pts',(1.05129988764842,-1.66506108797555,1.61232780975798));
#5734=CARTESIAN_POINT('Ctrl Pts',(0.941838959229918,-1.29239727476634,1.60290427183405));
#5735=CARTESIAN_POINT('Ctrl Pts',(0.847111831000521,-1.11349942484178,1.59617734685152));
#5736=CARTESIAN_POINT('Ctrl Pts',(0.48917696090542,-0.609678328916015,1.57525998575985));
#5737=CARTESIAN_POINT('Ctrl Pts',(0.152480645331013,-0.315277976557456,
1.560309480123));
#5738=CARTESIAN_POINT('Ctrl Pts',(-0.401131934499452,-0.0719964417188535,
1.57108236464872));
#5739=CARTESIAN_POINT('Ctrl Pts',(-0.5959636307406,-0.0234925921684045,
1.58005022190368));
#5740=CARTESIAN_POINT('Ctrl Pts',(-0.99105980640179,-0.0461787587522702,
1.61625721288154));
#5741=CARTESIAN_POINT('Ctrl Pts',(-1.19161371881466,-0.12598348672354,1.64472658966789));
#5742=CARTESIAN_POINT('Ctrl Pts',(-1.49417307921139,-0.432526875475132,
1.71573427762991));
#5743=CARTESIAN_POINT('Ctrl Pts',(-1.5948332762173,-0.647477749754412,1.75642712767188));
#5744=CARTESIAN_POINT('Ctrl Pts',(-1.70167589423767,-1.18783690618816,1.84803426880073));
#5745=CARTESIAN_POINT('Ctrl Pts',(-1.70977955005582,-1.5171651422599,1.89970221556995));
#5746=CARTESIAN_POINT('Ctrl Pts',(-1.66752387161256,-1.92309305756368,1.96012536190953));
#5747=CARTESIAN_POINT('',(-1.19858468901873,-1.92998306793576,1.58589472341869));
#5748=CARTESIAN_POINT('Origin',(-1.43305428031565,-1.92653806274973,1.77301004266414));
#5749=CARTESIAN_POINT('',(-2.,-0.264726219523809,0.141138331776429));
#5750=CARTESIAN_POINT('Ctrl Pts',(-2.,-0.264726219523809,0.141138331776429));
#5751=CARTESIAN_POINT('Ctrl Pts',(-1.93317897182823,-0.140204737359338,
0.374697162628536));
#5752=CARTESIAN_POINT('Ctrl Pts',(-1.89576248628645,-0.0714193310070166,
0.563392832565318));
#5753=CARTESIAN_POINT('Ctrl Pts',(-1.85828016234107,-0.0141476745355931,
0.845995304749381));
#5754=CARTESIAN_POINT('Ctrl Pts',(-1.85721582540971,-0.0237125088868792,
0.935184056400945));
#5755=CARTESIAN_POINT('Ctrl Pts',(-1.86061638209651,-0.0666740172427863,
1.06187361715673));
#5756=CARTESIAN_POINT('Ctrl Pts',(-1.86640738686477,-0.101672715288381,
1.11012925637074));
#5757=CARTESIAN_POINT('Ctrl Pts',(-1.88833554246329,-0.235746153313808,
1.21545234876845));
#5758=CARTESIAN_POINT('Ctrl Pts',(-1.9033753276643,-0.335251316849042,1.26604967753693));
#5759=CARTESIAN_POINT('Ctrl Pts',(-1.9189176957612,-0.518726439558199,1.34035163842065));
#5760=CARTESIAN_POINT('Ctrl Pts',(-1.92137116451861,-0.585485291115871,
1.36832017615168));
#5761=CARTESIAN_POINT('Ctrl Pts',(-1.93896943688162,-0.724455435049461,
1.40322870297494));
#5762=CARTESIAN_POINT('Ctrl Pts',(-1.95325668725115,-0.796545227124419,
1.40888781048668));
#5763=CARTESIAN_POINT('Ctrl Pts',(-1.99209925627655,-1.01599260874888,1.41219882843878));
#5764=CARTESIAN_POINT('Ctrl Pts',(-2.00898122237353,-1.16761549888469,1.40420126611032));
#5765=CARTESIAN_POINT('Ctrl Pts',(-2.01271588366055,-1.60175062040053,1.36576567629003));
#5766=CARTESIAN_POINT('Ctrl Pts',(-1.95046360827934,-1.85129221142242,1.32547580954877));
#5767=CARTESIAN_POINT('Ctrl Pts',(-1.69792570410908,-2.14007513561928,1.27973035876422));
#5768=CARTESIAN_POINT('Ctrl Pts',(-1.50788517190343,-2.24578075342313,1.26508664601861));
#5769=CARTESIAN_POINT('Ctrl Pts',(-1.03351721040672,-2.37409803162741,1.24662061906772));
#5770=CARTESIAN_POINT('Ctrl Pts',(-0.753928362614793,-2.39679255199907,
1.24243205928811));
#5771=CARTESIAN_POINT('Ctrl Pts',(-0.218845999430284,-2.35785399723118,
1.24055602083421));
#5772=CARTESIAN_POINT('Ctrl Pts',(0.0368662467341799,-2.29519092886669,
1.24322556456469));
#5773=CARTESIAN_POINT('Ctrl Pts',(0.411239882065782,-2.11406967659605,1.2495991139221));
#5774=CARTESIAN_POINT('Ctrl Pts',(0.518384719875618,-2.00298884738698,1.25072899682664));
#5775=CARTESIAN_POINT('Ctrl Pts',(0.571801954928687,-1.83523605217566,1.25334679757698));
#5776=CARTESIAN_POINT('Ctrl Pts',(0.569023344394799,-1.74044478899434,1.25599881503435));
#5777=CARTESIAN_POINT('Ctrl Pts',(0.494126240428662,-1.50788563057796,1.25886663470126));
#5778=CARTESIAN_POINT('Ctrl Pts',(0.421606239831573,-1.37485017740085,1.26041038383949));
#5779=CARTESIAN_POINT('Ctrl Pts',(0.127609128452456,-0.989034614321357,
1.26907008807672));
#5780=CARTESIAN_POINT('Ctrl Pts',(-0.170570542490676,-0.751894328558357,
1.28023791867232));
#5781=CARTESIAN_POINT('Ctrl Pts',(-0.569600762546571,-0.586703644418381,
1.30640573381989));
#5782=CARTESIAN_POINT('Ctrl Pts',(-0.692371618949951,-0.563856396440986,
1.31685387723007));
#5783=CARTESIAN_POINT('Ctrl Pts',(-0.882581236630141,-0.577499841895708,
1.33968897633028));
#5784=CARTESIAN_POINT('Ctrl Pts',(-0.949730803773584,-0.6053755874494,1.35084566027416));
#5785=CARTESIAN_POINT('Ctrl Pts',(-1.08267031338154,-0.742643707380371,
1.38530535019886));
#5786=CARTESIAN_POINT('Ctrl Pts',(-1.14980571385887,-0.863823663666268,
1.41045379245241));
#5787=CARTESIAN_POINT('Ctrl Pts',(-1.22863752459304,-1.27359538565792,1.48274964800499));
#5788=CARTESIAN_POINT('Ctrl Pts',(-1.23841278692706,-1.55826711159036,1.52914339518866));
#5789=CARTESIAN_POINT('Ctrl Pts',(-1.19858468901873,-1.92998306793576,1.58589472341869));
#5790=CARTESIAN_POINT('Origin',(-2.,-2.08166817117217E-14,-3.46944695195361E-14));
#5791=CARTESIAN_POINT('Ctrl Pts',(-2.00006370137914,0.278745603789511,0.110909351770506));
#5792=CARTESIAN_POINT('Ctrl Pts',(-2.02978177261913,0.487078937122742,-0.425006101824765));
#5793=CARTESIAN_POINT('Ctrl Pts',(-1.78756065046676,0.695412270456132,-0.903981534539017));
#5794=CARTESIAN_POINT('Ctrl Pts',(-1.5453395283144,0.903745603789377,-1.38295696725319));
#5795=CARTESIAN_POINT('Ctrl Pts',(-1.09608216684017,1.11207893712281,-1.67665129869622));
#5796=CARTESIAN_POINT('Ctrl Pts',(-0.646824805365941,1.32041227045615,-1.97034563013915));
#5797=CARTESIAN_POINT('Ctrl Pts',(-0.110909351770586,1.52874560378948,-2.00006370137914));
#5798=CARTESIAN_POINT('Ctrl Pts',(0.425006101824744,1.73707893712275,-2.02978177261916));
#5799=CARTESIAN_POINT('Ctrl Pts',(0.903981534538964,1.94541227045615,-1.78756065046677));
#5800=CARTESIAN_POINT('Ctrl Pts',(1.38295696725319,2.15374560378948,-1.5453395283144));
#5801=CARTESIAN_POINT('Ctrl Pts',(1.67665129869617,2.36207893712281,-1.09608216684018));
#5802=CARTESIAN_POINT('Ctrl Pts',(1.97034563013914,2.57041227045613,-0.646824805365955));
#5803=CARTESIAN_POINT('Ctrl Pts',(2.00006370137916,2.77874560378949,-0.110909351770603));
#5804=CARTESIAN_POINT('Ctrl Pts',(2.02978177261913,2.98707893712281,0.425006101824722));
#5805=CARTESIAN_POINT('Ctrl Pts',(1.78756065046677,3.19541227045615,0.903981534538913));
#5806=CARTESIAN_POINT('Ctrl Pts',(1.5453395283144,3.40374560378943,1.38295696725317));
#5807=CARTESIAN_POINT('Ctrl Pts',(1.09608216684017,3.61207893712282,1.67665129869616));
#5808=CARTESIAN_POINT('Ctrl Pts',(0.646824805365943,3.8204122704561,1.97034563013913));
#5809=CARTESIAN_POINT('Ctrl Pts',(0.1109093517706,4.02874560378949,2.00006370137908));
#5810=CARTESIAN_POINT('Ctrl Pts',(-0.425006101824727,4.23707893712277,2.02978177261911));
#5811=CARTESIAN_POINT('Ctrl Pts',(-0.903981534538964,4.44541227045615,1.78756065046676));
#5812=CARTESIAN_POINT('Ctrl Pts',(-1.38295696725319,4.65374560378948,1.54533952831435));
#5813=CARTESIAN_POINT('Ctrl Pts',(-1.67665129869618,4.86207893712285,1.09608216684011));
#5814=CARTESIAN_POINT('Ctrl Pts',(-1.97034563013914,5.07041227045609,0.646824805365927));
#5815=CARTESIAN_POINT('Ctrl Pts',(-2.00006370137914,5.27874560378947,0.110909351770506));
#5816=CARTESIAN_POINT('Ctrl Pts',(-2.02978177261913,5.48707893712276,-0.425006101824808));
#5817=CARTESIAN_POINT('Ctrl Pts',(-1.78756065046676,5.69541227045614,-0.903981534539017));
#5818=CARTESIAN_POINT('Ctrl Pts',(-1.5453395283144,5.90374560378943,-1.38295696725317));
#5819=CARTESIAN_POINT('Ctrl Pts',(-1.09608216684016,6.11207893712282,-1.67665129869616));
#5820=CARTESIAN_POINT('Ctrl Pts',(-0.646824805365928,6.32041227045614,-1.97034563013915));
#5821=CARTESIAN_POINT('Ctrl Pts',(-0.110909351770598,6.52874560378952,-2.00006370137919));
#5822=CARTESIAN_POINT('Ctrl Pts',(0.425006101824742,6.73707893712276,-2.02978177261914));
#5823=CARTESIAN_POINT('Ctrl Pts',(0.903981534538965,6.94541227045619,-1.78756065046677));
#5824=CARTESIAN_POINT('Ctrl Pts',(1.3829569672532,7.15374560378946,-1.54533952831446));
#5825=CARTESIAN_POINT('Ctrl Pts',(1.67665129869614,7.36207893712281,-1.09608216684023));
#5826=CARTESIAN_POINT('Ctrl Pts',(1.97034563013915,7.57041227045615,-0.646824805365941));
#5827=CARTESIAN_POINT('Ctrl Pts',(2.00006370137914,7.77874560378953,-0.11090935177061));
#5828=CARTESIAN_POINT('Ctrl Pts',(2.02978177261913,7.98707893712276,0.425006101824722));
#5829=CARTESIAN_POINT('Ctrl Pts',(1.78756065046677,8.19541227045616,0.903981534538955));
#5830=CARTESIAN_POINT('Ctrl Pts',(1.54533952831442,8.40374560378946,1.38295696725319));
#5831=CARTESIAN_POINT('Ctrl Pts',(1.09608216684017,8.61207893712284,1.67665129869611));
#5832=CARTESIAN_POINT('Ctrl Pts',(0.646824805365943,8.82041227045615,1.97034563013914));
#5833=CARTESIAN_POINT('Ctrl Pts',(0.110909351770597,9.0287456037895,2.00006370137908));
#5834=CARTESIAN_POINT('Ctrl Pts',(-0.42500610182474,9.23707893712282,2.02978177261913));
#5835=CARTESIAN_POINT('Ctrl Pts',(-0.903981534538962,9.44541227045615,1.78756065046671));
#5836=CARTESIAN_POINT('Ctrl Pts',(-1.38295696725319,9.65374560378948,1.5453395283144));
#5837=CARTESIAN_POINT('Ctrl Pts',(-1.67665129869616,9.86207893712282,1.09608216684017));
#5838=CARTESIAN_POINT('Ctrl Pts',(-1.97034563013914,10.0704122704562,0.646824805365941));
#5839=CARTESIAN_POINT('Ctrl Pts',(-2.00006370137912,10.2787456037895,0.110909351770534));
#5840=CARTESIAN_POINT('Ctrl Pts',(-2.02978177261913,10.4870789371228,-0.425006101824744));
#5841=CARTESIAN_POINT('Ctrl Pts',(-1.78756065046676,10.6954122704562,-0.903981534539066));
#5842=CARTESIAN_POINT('Ctrl Pts',(-1.5453395283144,10.9037456037894,-1.3829569672532));
#5843=CARTESIAN_POINT('Ctrl Pts',(-1.09608216684017,11.1120789371228,-1.67665129869622));
#5844=CARTESIAN_POINT('Ctrl Pts',(-0.646824805365941,11.3204122704561,-1.97034563013915));
#5845=CARTESIAN_POINT('Ctrl Pts',(-0.1109093517706,11.5287456037895,-2.00006370137916));
#5846=CARTESIAN_POINT('Ctrl Pts',(0.425006101824742,11.7370789371228,-2.02978177261915));
#5847=CARTESIAN_POINT('Ctrl Pts',(0.903981534538964,11.9454122704562,-1.78756065046677));
#5848=CARTESIAN_POINT('Ctrl Pts',(1.38295696725319,12.1537456037895,-1.54533952831446));
#5849=CARTESIAN_POINT('Ctrl Pts',(1.67665129869616,12.3620789371228,-1.09608216684018));
#5850=CARTESIAN_POINT('Ctrl Pts',(1.97034563013917,12.5704122704561,-0.646824805365955));
#5851=CARTESIAN_POINT('Ctrl Pts',(2.00006370137914,12.7787456037895,-0.110909351770652));
#5852=CARTESIAN_POINT('Ctrl Pts',(2.02978177261913,12.9870789371228,0.425006101824744));
#5853=CARTESIAN_POINT('Ctrl Pts',(1.78756065046676,13.1954122704562,0.903981534538906));
#5854=CARTESIAN_POINT('Ctrl Pts',(1.5453395283144,13.4037456037895,1.38295696725318));
#5855=CARTESIAN_POINT('Ctrl Pts',(1.09608216684017,13.6120789371228,1.67665129869616));
#5856=CARTESIAN_POINT('Ctrl Pts',(0.646824805365943,13.8204122704562,1.97034563013915));
#5857=CARTESIAN_POINT('Ctrl Pts',(0.1109093517706,14.0287456037895,2.0000637013791));
#5858=CARTESIAN_POINT('Ctrl Pts',(-0.425006101824742,14.2370789371228,2.02978177261913));
#5859=CARTESIAN_POINT('Ctrl Pts',(-0.903981534538964,14.4454122704562,1.78756065046667));
#5860=CARTESIAN_POINT('Ctrl Pts',(-1.38295696725319,14.6537456037895,1.54533952831435));
#5861=CARTESIAN_POINT('Ctrl Pts',(-1.67665129869616,14.8620789371229,1.09608216684011));
#5862=CARTESIAN_POINT('Ctrl Pts',(-1.97034563013913,15.0704122704562,0.646824805365955));
#5863=CARTESIAN_POINT('Ctrl Pts',(-2.00006370137914,15.2787456037895,0.110909351770541));
#5864=CARTESIAN_POINT('Ctrl Pts',(-2.02978177261913,15.4870789371228,-0.425006101824851));
#5865=CARTESIAN_POINT('Ctrl Pts',(-1.78756065046676,15.6954122704562,-0.903981534538976));
#5866=CARTESIAN_POINT('Ctrl Pts',(-1.5453395283144,15.9037456037895,-1.38295696725319));
#5867=CARTESIAN_POINT('Ctrl Pts',(-1.09608216684016,16.1120789371229,-1.6766512986962));
#5868=CARTESIAN_POINT('Ctrl Pts',(-0.646824805365941,16.3204122704561,-1.9703456301392));
#5869=CARTESIAN_POINT('Ctrl Pts',(-0.1109093517706,16.5287456037895,-2.00006370137919));
#5870=CARTESIAN_POINT('Ctrl Pts',(0.425006101824744,16.7370789371228,-2.02978177261913));
#5871=CARTESIAN_POINT('Ctrl Pts',(0.903981534538977,16.9454122704562,-1.78756065046677));
#5872=CARTESIAN_POINT('Ctrl Pts',(1.38295696725319,17.1537456037895,-1.5453395283144));
#5873=CARTESIAN_POINT('Ctrl Pts',(1.67665129869616,17.3620789371229,-1.09608216684022));
#5874=CARTESIAN_POINT('Ctrl Pts',(1.97034563013914,17.5704122704561,-0.646824805365941));
#5875=CARTESIAN_POINT('Ctrl Pts',(2.00006370137914,17.7787456037895,-0.11090935177061));
#5876=CARTESIAN_POINT('Ctrl Pts',(2.02978177261913,17.9870789371228,0.425006101824686));
#5877=CARTESIAN_POINT('Ctrl Pts',(1.78756065046677,18.1954122704562,0.903981534538948));
#5878=CARTESIAN_POINT('Ctrl Pts',(1.54533952831442,18.4037456037895,1.38295696725319));
#5879=CARTESIAN_POINT('Ctrl Pts',(1.09608216684017,18.6120789371228,1.67665129869611));
#5880=CARTESIAN_POINT('Ctrl Pts',(0.646824805365943,18.8204122704562,1.97034563013914));
#5881=CARTESIAN_POINT('Ctrl Pts',(0.110909351770598,19.0287456037895,2.00006370137909));
#5882=CARTESIAN_POINT('Ctrl Pts',(-0.425006101824742,19.2370789371228,2.02978177261913));
#5883=CARTESIAN_POINT('Ctrl Pts',(-0.903981534538962,19.4454122704562,1.78756065046669));
#5884=CARTESIAN_POINT('Ctrl Pts',(-1.38295696725319,19.6537456037895,1.5453395283144));
#5885=CARTESIAN_POINT('Ctrl Pts',(-1.67665129869616,19.8620789371228,1.09608216684013));
#5886=CARTESIAN_POINT('Ctrl Pts',(-1.97034563013915,20.0704122704561,0.646824805365941));
#5887=CARTESIAN_POINT('Ctrl Pts',(-2.00006370137912,20.2787456037895,0.110909351770513));
#5888=CARTESIAN_POINT('Ctrl Pts',(-2.02978177261911,20.4870789371228,-0.425006101824801));
#5889=CARTESIAN_POINT('Ctrl Pts',(-1.78756065046676,20.6954122704562,-0.903981534539024));
#5890=CARTESIAN_POINT('Ctrl Pts',(-1.54533952831439,20.9037456037895,-1.38295696725322));
#5891=CARTESIAN_POINT('Ctrl Pts',(-1.09608216684018,21.1120789371229,-1.67665129869622));
#5892=CARTESIAN_POINT('Ctrl Pts',(-0.646824805365943,21.3204122704561,-1.97034563013915));
#5893=CARTESIAN_POINT('Ctrl Pts',(-0.1109093517706,21.5287456037895,-2.00006370137914));
#5894=CARTESIAN_POINT('Ctrl Pts',(0.425006101824742,21.7370789371228,-2.02978177261912));
#5895=CARTESIAN_POINT('Ctrl Pts',(0.903981534538964,21.9454122704562,-1.7875606504668));
#5896=CARTESIAN_POINT('Ctrl Pts',(1.38295696725319,22.1537456037895,-1.54533952831446));
#5897=CARTESIAN_POINT('Ctrl Pts',(1.67665129869617,22.3620789371229,-1.09608216684019));
#5898=CARTESIAN_POINT('Ctrl Pts',(1.97034563013912,22.5704122704561,-0.646824805365941));
#5899=CARTESIAN_POINT('Ctrl Pts',(2.00006370137914,22.7787456037895,-0.110909351770638));
#5900=CARTESIAN_POINT('Ctrl Pts',(2.02978177261915,22.9870789371228,0.425006101824744));
#5901=CARTESIAN_POINT('Ctrl Pts',(1.78756065046677,23.1954122704562,0.903981534538906));
#5902=CARTESIAN_POINT('Ctrl Pts',(1.5453395283144,23.4037456037895,1.38295696725318));
#5903=CARTESIAN_POINT('Ctrl Pts',(1.09608216684017,23.6120789371229,1.67665129869614));
#5904=CARTESIAN_POINT('Ctrl Pts',(0.646824805365957,23.8204122704561,1.97034563013915));
#5905=CARTESIAN_POINT('Ctrl Pts',(0.1109093517706,24.0287456037895,2.00006370137905));
#5906=CARTESIAN_POINT('Ctrl Pts',(-0.425006101824742,24.2370789371228,2.02978177261914));
#5907=CARTESIAN_POINT('Ctrl Pts',(-0.903981534538964,24.4454122704562,1.78756065046667));
#5908=CARTESIAN_POINT('Ctrl Pts',(-1.38295696725317,24.6537456037895,1.54533952831433));
#5909=CARTESIAN_POINT('Ctrl Pts',(-1.67665129869615,24.8620789371229,1.09608216684012));
#5910=CARTESIAN_POINT('Ctrl Pts',(-1.97034563013914,25.0704122704562,0.646824805365955));
#5911=CARTESIAN_POINT('Ctrl Pts',(-2.00006370137914,25.2787456037895,0.110909351770548));
#5912=CARTESIAN_POINT('Ctrl Pts',(-2.02978177261913,25.4870789371228,-0.425006101824772));
#5913=CARTESIAN_POINT('Ctrl Pts',(-1.78756065046676,25.6954122704562,-0.903981534538976));
#5914=CARTESIAN_POINT('Ctrl Pts',(-1.5453395283144,25.9037456037895,-1.38295696725319));
#5915=CARTESIAN_POINT('Ctrl Pts',(-1.09608216684017,26.1120789371229,-1.67665129869619));
#5916=CARTESIAN_POINT('Ctrl Pts',(-0.646824805365941,26.3204122704561,-1.9703456301392));
#5917=CARTESIAN_POINT('Ctrl Pts',(-0.1109093517706,26.5287456037895,-2.00006370137917));
#5918=CARTESIAN_POINT('Ctrl Pts',(0.425006101824756,26.7370789371228,-2.02978177261913));
#5919=CARTESIAN_POINT('Ctrl Pts',(0.903981534538977,26.9454122704562,-1.78756065046682));
#5920=CARTESIAN_POINT('Ctrl Pts',(1.38295696725319,27.1537456037895,-1.5453395283144));
#5921=CARTESIAN_POINT('Ctrl Pts',(1.67665129869614,27.3620789371229,-1.09608216684021));
#5922=CARTESIAN_POINT('Ctrl Pts',(1.97034563013914,27.5704122704562,-0.646824805365969));
#5923=CARTESIAN_POINT('Ctrl Pts',(2.00006370137911,27.7787456037896,-0.110909351770603));
#5924=CARTESIAN_POINT('Ctrl Pts',(2.02978177261913,27.9870789371228,0.425006101824736));
#5925=CARTESIAN_POINT('Ctrl Pts',(1.78756065046677,28.1954122704562,0.903981534538934));
#5926=CARTESIAN_POINT('Ctrl Pts',(1.54533952831439,28.4037456037895,1.38295696725318));
#5927=CARTESIAN_POINT('Ctrl Pts',(1.09608216684017,28.6120789371229,1.67665129869612));
#5928=CARTESIAN_POINT('Ctrl Pts',(0.646824805365943,28.8204122704562,1.97034563013911));
#5929=CARTESIAN_POINT('Ctrl Pts',(0.110909351770614,29.0287456037896,2.0000637013791));
#5930=CARTESIAN_POINT('Ctrl Pts',(-0.425006101824742,29.2370789371228,2.02978177261913));
#5931=CARTESIAN_POINT('Ctrl Pts',(-0.903981534538962,29.4454122704562,1.78756065046671));
#5932=CARTESIAN_POINT('Ctrl Pts',(-1.38295696725319,29.6537456037896,1.54533952831437));
#5933=CARTESIAN_POINT('Ctrl Pts',(-1.67665129869616,29.8620789371229,1.0960821668401));
#5934=CARTESIAN_POINT('Ctrl Pts',(-1.97034563013914,30.0704122704562,0.646824805365912));
#5935=CARTESIAN_POINT('Ctrl Pts',(-2.00006370137914,30.2787456037896,0.110909351770527));
#5936=CARTESIAN_POINT('Ctrl Pts',(-2.02978177261913,30.4870789371228,-0.425006101824801));
#5937=CARTESIAN_POINT('Ctrl Pts',(-1.78756065046675,30.6954122704562,-0.90398153453901));
#5938=CARTESIAN_POINT('Ctrl Pts',(-1.5453395283144,30.9037456037895,-1.38295696725315));
#5939=CARTESIAN_POINT('Ctrl Pts',(-1.09608216684017,31.1120789371229,-1.67665129869622));
#5940=CARTESIAN_POINT('Ctrl Pts',(-0.646824805365941,31.3204122704562,-1.97034563013915));
#5941=CARTESIAN_POINT('Ctrl Pts',(-0.110909351770598,31.5287456037896,-2.00006370137914));
#5942=CARTESIAN_POINT('Ctrl Pts',(0.425006101824744,31.7370789371229,-2.02978177261914));
#5943=CARTESIAN_POINT('Ctrl Pts',(0.903981534538951,31.9454122704562,-1.78756065046679));
#5944=CARTESIAN_POINT('Ctrl Pts',(1.38295696725319,32.1537456037895,-1.54533952831446));
#5945=CARTESIAN_POINT('Ctrl Pts',(1.67665129869616,32.3620789371229,-1.09608216684022));
#5946=CARTESIAN_POINT('Ctrl Pts',(1.97034563013914,32.5704122704561,-0.646824805365941));
#5947=CARTESIAN_POINT('Ctrl Pts',(2.00006370137914,32.7787456037896,-0.11090935177061));
#5948=CARTESIAN_POINT('Ctrl Pts',(2.02978177261913,32.9870789371229,0.425006101824715));
#5949=CARTESIAN_POINT('Ctrl Pts',(1.78756065046676,33.1954122704563,0.903981534538906));
#5950=CARTESIAN_POINT('Ctrl Pts',(1.5453395283144,33.4037456037895,1.3829569672532));
#5951=CARTESIAN_POINT('Ctrl Pts',(1.09608216684017,33.6120789371229,1.67665129869615));
#5952=CARTESIAN_POINT('Ctrl Pts',(0.646824805365943,33.8204122704562,1.97034563013915));
#5953=CARTESIAN_POINT('Ctrl Pts',(0.1109093517706,34.0287456037896,2.00006370137906));
#5954=CARTESIAN_POINT('Ctrl Pts',(-0.425006101824742,34.2370789371229,2.02978177261912));
#5955=CARTESIAN_POINT('Ctrl Pts',(-0.903981534538964,34.4454122704562,1.7875606504667));
#5956=CARTESIAN_POINT('Ctrl Pts',(-1.3829569672532,34.6537456037895,1.54533952831438));
#5957=CARTESIAN_POINT('Ctrl Pts',(-1.67665129869615,34.8620789371228,1.09608216684013));
#5958=CARTESIAN_POINT('Ctrl Pts',(-1.97034563013914,35.0704122704562,0.646824805365955));
#5959=CARTESIAN_POINT('Ctrl Pts',(-2.00006370137914,35.2787456037896,0.110909351770548));
#5960=CARTESIAN_POINT('Ctrl Pts',(-2.02978177261913,35.4870789371229,-0.425006101824787));
#5961=CARTESIAN_POINT('Ctrl Pts',(-1.78756065046676,35.6954122704562,-0.903981534538996));
#5962=CARTESIAN_POINT('Ctrl Pts',(-1.5453395283144,35.9037456037895,-1.3829569672532));
#5963=CARTESIAN_POINT('Ctrl Pts',(-1.09608216684017,36.1120789371229,-1.67665129869619));
#5964=CARTESIAN_POINT('Ctrl Pts',(-0.646824805365928,36.3204122704562,-1.97034563013915));
#5965=CARTESIAN_POINT('Ctrl Pts',(-0.1109093517706,36.5287456037896,-2.00006370137918));
#5966=CARTESIAN_POINT('Ctrl Pts',(0.425006101824742,36.7370789371229,-2.02978177261914));
#5967=CARTESIAN_POINT('Ctrl Pts',(0.903981534538964,36.9454122704562,-1.78756065046682));
#5968=CARTESIAN_POINT('Ctrl Pts',(1.38295696725319,37.1537456037895,-1.5453395283144));
#5969=CARTESIAN_POINT('Ctrl Pts',(1.67665129869617,37.3620789371229,-1.09608216684022));
#5970=CARTESIAN_POINT('Ctrl Pts',(1.97034563013915,37.5704122704562,-0.646824805365941));
#5971=CARTESIAN_POINT('Ctrl Pts',(2.00006370137914,37.7787456037895,-0.110909351770645));
#5972=CARTESIAN_POINT('Ctrl Pts',(2.02978177261915,37.9870789371229,0.425006101824736));
#5973=CARTESIAN_POINT('Ctrl Pts',(1.78756065046677,38.1954122704563,0.90398153453892));
#5974=CARTESIAN_POINT('Ctrl Pts',(1.5453395283144,38.4037456037895,1.38295696725319));
#5975=CARTESIAN_POINT('Ctrl Pts',(1.09608216684019,38.6120789371229,1.67665129869612));
#5976=CARTESIAN_POINT('Ctrl Pts',(0.646824805365943,38.8204122704562,1.97034563013916));
#5977=CARTESIAN_POINT('Ctrl Pts',(0.110909351770614,39.0287456037896,2.0000637013791));
#5978=CARTESIAN_POINT('Ctrl Pts',(-0.425006101824727,39.2370789371229,2.02978177261914));
#5979=CARTESIAN_POINT('Ctrl Pts',(-0.90398153453895,39.4454122704563,1.78756065046672));
#5980=CARTESIAN_POINT('Ctrl Pts',(-1.38295696725319,39.6537456037896,1.54533952831436));
#5981=CARTESIAN_POINT('Ctrl Pts',(-1.67665129869616,39.8620789371229,1.09608216684011));
#5982=CARTESIAN_POINT('Ctrl Pts',(-1.97034563013914,40.0704122704562,0.646824805365955));
#5983=CARTESIAN_POINT('Ctrl Pts',(-2.00006370137914,40.2787456037896,0.110909351770527));
#5984=CARTESIAN_POINT('Ctrl Pts',(-2.00004246683501,0.278745607978964,0.110909353437437));
#5985=CARTESIAN_POINT('Ctrl Pts',(-2.02976053852165,0.487078941312195,-0.425000410378884));
#5986=CARTESIAN_POINT('Ctrl Pts',(-1.78754226164558,0.695412274645584,-0.903970915823348));
#5987=CARTESIAN_POINT('Ctrl Pts',(-1.5453239847695,0.903745607978829,-1.38294142126773));
#5988=CARTESIAN_POINT('Ctrl Pts',(-1.09607155101171,1.11207894131226,-1.6766329082081));
#5989=CARTESIAN_POINT('Ctrl Pts',(-0.64681911725392,1.32041227464561,-1.97032439514837));
#5990=CARTESIAN_POINT('Ctrl Pts',(-0.110909353437516,1.52874560797894,-2.00004246683502));
#5991=CARTESIAN_POINT('Ctrl Pts',(0.425000410378862,1.7370789413122,-2.02976053852169));
#5992=CARTESIAN_POINT('Ctrl Pts',(0.903970915823295,1.94541227464561,-1.78754226164558));
#5993=CARTESIAN_POINT('Ctrl Pts',(1.38294142126773,2.15374560797893,-1.5453239847695));
#5994=CARTESIAN_POINT('Ctrl Pts',(1.67663290820805,2.36207894131226,-1.09607155101172));
#5995=CARTESIAN_POINT('Ctrl Pts',(1.97032439514836,2.57041227464558,-0.646819117253935));
#5996=CARTESIAN_POINT('Ctrl Pts',(2.00004246683503,2.77874560797894,-0.110909353437534));
#5997=CARTESIAN_POINT('Ctrl Pts',(2.02976053852165,2.98707894131226,0.42500041037884));
#5998=CARTESIAN_POINT('Ctrl Pts',(1.78754226164558,3.1954122746456,0.903970915823244));
#5999=CARTESIAN_POINT('Ctrl Pts',(1.5453239847695,3.40374560797888,1.38294142126772));
#6000=CARTESIAN_POINT('Ctrl Pts',(1.09607155101171,3.61207894131227,1.67663290820804));
#6001=CARTESIAN_POINT('Ctrl Pts',(0.646819117253922,3.82041227464555,1.97032439514834));
#6002=CARTESIAN_POINT('Ctrl Pts',(0.11090935343753,4.02874560797894,2.00004246683495));
#6003=CARTESIAN_POINT('Ctrl Pts',(-0.425000410378846,4.23707894131222,2.02976053852163));
#6004=CARTESIAN_POINT('Ctrl Pts',(-0.903970915823295,4.4454122746456,1.78754226164557));
#6005=CARTESIAN_POINT('Ctrl Pts',(-1.38294142126773,4.65374560797893,1.54532398476945));
#6006=CARTESIAN_POINT('Ctrl Pts',(-1.67663290820806,4.8620789413123,1.09607155101165));
#6007=CARTESIAN_POINT('Ctrl Pts',(-1.97032439514836,5.07041227464555,0.646819117253906));
#6008=CARTESIAN_POINT('Ctrl Pts',(-2.00004246683501,5.27874560797892,0.110909353437437));
#6009=CARTESIAN_POINT('Ctrl Pts',(-2.02976053852165,5.48707894131221,-0.425000410378927));
#6010=CARTESIAN_POINT('Ctrl Pts',(-1.78754226164558,5.6954122746456,-0.903970915823348));
#6011=CARTESIAN_POINT('Ctrl Pts',(-1.5453239847695,5.90374560797888,-1.38294142126772));
#6012=CARTESIAN_POINT('Ctrl Pts',(-1.0960715510117,6.11207894131227,-1.67663290820805));
#6013=CARTESIAN_POINT('Ctrl Pts',(-0.646819117253907,6.3204122746456,-1.97032439514837));
#6014=CARTESIAN_POINT('Ctrl Pts',(-0.110909353437529,6.52874560797897,-2.00004246683506));
#6015=CARTESIAN_POINT('Ctrl Pts',(0.42500041037886,6.73707894131221,-2.02976053852166));
#6016=CARTESIAN_POINT('Ctrl Pts',(0.903970915823297,6.94541227464564,-1.78754226164558));
#6017=CARTESIAN_POINT('Ctrl Pts',(1.38294142126774,7.15374560797891,-1.54532398476956));
#6018=CARTESIAN_POINT('Ctrl Pts',(1.67663290820802,7.36207894131227,-1.09607155101177));
#6019=CARTESIAN_POINT('Ctrl Pts',(1.97032439514836,7.5704122746456,-0.64681911725392));
#6020=CARTESIAN_POINT('Ctrl Pts',(2.00004246683501,7.77874560797898,-0.110909353437541));
#6021=CARTESIAN_POINT('Ctrl Pts',(2.02976053852165,7.98707894131222,0.42500041037884));
#6022=CARTESIAN_POINT('Ctrl Pts',(1.78754226164558,8.19541227464561,0.903970915823286));
#6023=CARTESIAN_POINT('Ctrl Pts',(1.54532398476952,8.40374560797891,1.38294142126773));
#6024=CARTESIAN_POINT('Ctrl Pts',(1.09607155101171,8.6120789413123,1.67663290820799));
#6025=CARTESIAN_POINT('Ctrl Pts',(0.646819117253922,8.8204122746456,1.97032439514836));
#6026=CARTESIAN_POINT('Ctrl Pts',(0.110909353437527,9.02874560797896,2.00004246683495));
#6027=CARTESIAN_POINT('Ctrl Pts',(-0.425000410378858,9.23707894131227,2.02976053852165));
#6028=CARTESIAN_POINT('Ctrl Pts',(-0.903970915823293,9.44541227464561,1.78754226164552));
#6029=CARTESIAN_POINT('Ctrl Pts',(-1.38294142126773,9.65374560797894,1.5453239847695));
#6030=CARTESIAN_POINT('Ctrl Pts',(-1.67663290820805,9.86207894131228,1.09607155101171));
#6031=CARTESIAN_POINT('Ctrl Pts',(-1.97032439514836,10.0704122746456,0.64681911725392));
#6032=CARTESIAN_POINT('Ctrl Pts',(-2.00004246683499,10.278745607979,0.110909353437464));
#6033=CARTESIAN_POINT('Ctrl Pts',(-2.02976053852165,10.4870789413123,-0.425000410378862));
#6034=CARTESIAN_POINT('Ctrl Pts',(-1.78754226164558,10.6954122746456,-0.903970915823397));
#6035=CARTESIAN_POINT('Ctrl Pts',(-1.5453239847695,10.9037456079789,-1.38294142126775));
#6036=CARTESIAN_POINT('Ctrl Pts',(-1.09607155101171,11.1120789413123,-1.6766329082081));
#6037=CARTESIAN_POINT('Ctrl Pts',(-0.64681911725392,11.3204122746456,-1.97032439514837));
#6038=CARTESIAN_POINT('Ctrl Pts',(-0.11090935343753,11.528745607979,-2.00004246683503));
#6039=CARTESIAN_POINT('Ctrl Pts',(0.42500041037886,11.7370789413123,-2.02976053852167));
#6040=CARTESIAN_POINT('Ctrl Pts',(0.903970915823295,11.9454122746456,-1.78754226164558));
#6041=CARTESIAN_POINT('Ctrl Pts',(1.38294142126773,12.1537456079789,-1.54532398476955));
#6042=CARTESIAN_POINT('Ctrl Pts',(1.67663290820804,12.3620789413123,-1.09607155101172));
#6043=CARTESIAN_POINT('Ctrl Pts',(1.97032439514839,12.5704122746456,-0.646819117253935));
#6044=CARTESIAN_POINT('Ctrl Pts',(2.00004246683501,12.778745607979,-0.110909353437582));
#6045=CARTESIAN_POINT('Ctrl Pts',(2.02976053852165,12.9870789413123,0.425000410378862));
#6046=CARTESIAN_POINT('Ctrl Pts',(1.78754226164557,13.1954122746456,0.903970915823237));
#6047=CARTESIAN_POINT('Ctrl Pts',(1.5453239847695,13.4037456079789,1.38294142126772));
#6048=CARTESIAN_POINT('Ctrl Pts',(1.09607155101171,13.6120789413123,1.67663290820805));
#6049=CARTESIAN_POINT('Ctrl Pts',(0.646819117253922,13.8204122746456,1.97032439514837));
#6050=CARTESIAN_POINT('Ctrl Pts',(0.11090935343753,14.0287456079789,2.00004246683497));
#6051=CARTESIAN_POINT('Ctrl Pts',(-0.42500041037886,14.2370789413123,2.02976053852165));
#6052=CARTESIAN_POINT('Ctrl Pts',(-0.903970915823295,14.4454122746456,1.78754226164548));
#6053=CARTESIAN_POINT('Ctrl Pts',(-1.38294142126773,14.6537456079789,1.54532398476945));
#6054=CARTESIAN_POINT('Ctrl Pts',(-1.67663290820804,14.8620789413123,1.09607155101165));
#6055=CARTESIAN_POINT('Ctrl Pts',(-1.97032439514835,15.0704122746456,0.646819117253935));
#6056=CARTESIAN_POINT('Ctrl Pts',(-2.00004246683501,15.278745607979,0.110909353437471));
#6057=CARTESIAN_POINT('Ctrl Pts',(-2.02976053852165,15.4870789413123,-0.42500041037897));
#6058=CARTESIAN_POINT('Ctrl Pts',(-1.78754226164558,15.6954122746456,-0.903970915823307));
#6059=CARTESIAN_POINT('Ctrl Pts',(-1.5453239847695,15.9037456079789,-1.38294142126773));
#6060=CARTESIAN_POINT('Ctrl Pts',(-1.0960715510117,16.1120789413123,-1.67663290820808));
#6061=CARTESIAN_POINT('Ctrl Pts',(-0.64681911725392,16.3204122746456,-1.97032439514842));
#6062=CARTESIAN_POINT('Ctrl Pts',(-0.11090935343753,16.528745607979,-2.00004246683506));
#6063=CARTESIAN_POINT('Ctrl Pts',(0.425000410378862,16.7370789413123,-2.02976053852165));
#6064=CARTESIAN_POINT('Ctrl Pts',(0.903970915823309,16.9454122746456,-1.78754226164558));
#6065=CARTESIAN_POINT('Ctrl Pts',(1.38294142126773,17.1537456079789,-1.5453239847695));
#6066=CARTESIAN_POINT('Ctrl Pts',(1.67663290820804,17.3620789413123,-1.09607155101176));
#6067=CARTESIAN_POINT('Ctrl Pts',(1.97032439514836,17.5704122746456,-0.64681911725392));
#6068=CARTESIAN_POINT('Ctrl Pts',(2.00004246683501,17.778745607979,-0.110909353437541));
#6069=CARTESIAN_POINT('Ctrl Pts',(2.02976053852165,17.9870789413123,0.425000410378805));
#6070=CARTESIAN_POINT('Ctrl Pts',(1.78754226164558,18.1954122746456,0.903970915823279));
#6071=CARTESIAN_POINT('Ctrl Pts',(1.54532398476952,18.4037456079789,1.38294142126773));
#6072=CARTESIAN_POINT('Ctrl Pts',(1.09607155101171,18.6120789413123,1.67663290820799));
#6073=CARTESIAN_POINT('Ctrl Pts',(0.646819117253922,18.8204122746456,1.97032439514836));
#6074=CARTESIAN_POINT('Ctrl Pts',(0.110909353437529,19.028745607979,2.00004246683496));
#6075=CARTESIAN_POINT('Ctrl Pts',(-0.42500041037886,19.2370789413123,2.02976053852165));
#6076=CARTESIAN_POINT('Ctrl Pts',(-0.903970915823293,19.4454122746457,1.7875422616455));
#6077=CARTESIAN_POINT('Ctrl Pts',(-1.38294142126773,19.6537456079789,1.5453239847695));
#6078=CARTESIAN_POINT('Ctrl Pts',(-1.67663290820805,19.8620789413123,1.09607155101167));
#6079=CARTESIAN_POINT('Ctrl Pts',(-1.97032439514836,20.0704122746456,0.64681911725392));
#6080=CARTESIAN_POINT('Ctrl Pts',(-2.00004246683499,20.278745607979,0.110909353437444));
#6081=CARTESIAN_POINT('Ctrl Pts',(-2.02976053852164,20.4870789413123,-0.42500041037892));
#6082=CARTESIAN_POINT('Ctrl Pts',(-1.78754226164558,20.6954122746456,-0.903970915823355));
#6083=CARTESIAN_POINT('Ctrl Pts',(-1.54532398476949,20.903745607979,-1.38294142126777));
#6084=CARTESIAN_POINT('Ctrl Pts',(-1.09607155101172,21.1120789413123,-1.6766329082081));
#6085=CARTESIAN_POINT('Ctrl Pts',(-0.646819117253922,21.3204122746456,-1.97032439514837));
#6086=CARTESIAN_POINT('Ctrl Pts',(-0.11090935343753,21.528745607979,-2.00004246683501));
#6087=CARTESIAN_POINT('Ctrl Pts',(0.42500041037886,21.7370789413123,-2.02976053852164));
#6088=CARTESIAN_POINT('Ctrl Pts',(0.903970915823295,21.9454122746457,-1.78754226164561));
#6089=CARTESIAN_POINT('Ctrl Pts',(1.38294142126773,22.1537456079789,-1.54532398476955));
#6090=CARTESIAN_POINT('Ctrl Pts',(1.67663290820805,22.3620789413123,-1.09607155101173));
#6091=CARTESIAN_POINT('Ctrl Pts',(1.97032439514834,22.5704122746456,-0.64681911725392));
#6092=CARTESIAN_POINT('Ctrl Pts',(2.00004246683501,22.778745607979,-0.110909353437569));
#6093=CARTESIAN_POINT('Ctrl Pts',(2.02976053852168,22.9870789413123,0.425000410378862));
#6094=CARTESIAN_POINT('Ctrl Pts',(1.78754226164558,23.1954122746457,0.903970915823237));
#6095=CARTESIAN_POINT('Ctrl Pts',(1.5453239847695,23.4037456079789,1.38294142126772));
#6096=CARTESIAN_POINT('Ctrl Pts',(1.09607155101171,23.6120789413123,1.67663290820802));
#6097=CARTESIAN_POINT('Ctrl Pts',(0.646819117253936,23.8204122746456,1.97032439514837));
#6098=CARTESIAN_POINT('Ctrl Pts',(0.11090935343753,24.028745607979,2.00004246683493));
#6099=CARTESIAN_POINT('Ctrl Pts',(-0.42500041037886,24.2370789413123,2.02976053852166));
#6100=CARTESIAN_POINT('Ctrl Pts',(-0.903970915823295,24.4454122746457,1.78754226164548));
#6101=CARTESIAN_POINT('Ctrl Pts',(-1.38294142126772,24.653745607979,1.54532398476942));
#6102=CARTESIAN_POINT('Ctrl Pts',(-1.67663290820803,24.8620789413123,1.09607155101166));
#6103=CARTESIAN_POINT('Ctrl Pts',(-1.97032439514836,25.0704122746456,0.646819117253935));
#6104=CARTESIAN_POINT('Ctrl Pts',(-2.00004246683501,25.278745607979,0.110909353437478));
#6105=CARTESIAN_POINT('Ctrl Pts',(-2.02976053852165,25.4870789413123,-0.425000410378891));
#6106=CARTESIAN_POINT('Ctrl Pts',(-1.78754226164558,25.6954122746456,-0.903970915823307));
#6107=CARTESIAN_POINT('Ctrl Pts',(-1.5453239847695,25.903745607979,-1.38294142126773));
#6108=CARTESIAN_POINT('Ctrl Pts',(-1.09607155101171,26.1120789413123,-1.67663290820807));
#6109=CARTESIAN_POINT('Ctrl Pts',(-0.64681911725392,26.3204122746456,-1.97032439514842));
#6110=CARTESIAN_POINT('Ctrl Pts',(-0.11090935343753,26.528745607979,-2.00004246683504));
#6111=CARTESIAN_POINT('Ctrl Pts',(0.425000410378875,26.7370789413123,-2.02976053852165));
#6112=CARTESIAN_POINT('Ctrl Pts',(0.903970915823309,26.9454122746457,-1.78754226164563));
#6113=CARTESIAN_POINT('Ctrl Pts',(1.38294142126773,27.1537456079789,-1.5453239847695));
#6114=CARTESIAN_POINT('Ctrl Pts',(1.67663290820802,27.3620789413123,-1.09607155101175));
#6115=CARTESIAN_POINT('Ctrl Pts',(1.97032439514836,27.5704122746456,-0.646819117253949));
#6116=CARTESIAN_POINT('Ctrl Pts',(2.00004246683498,27.778745607979,-0.110909353437534));
#6117=CARTESIAN_POINT('Ctrl Pts',(2.02976053852165,27.9870789413123,0.425000410378855));
#6118=CARTESIAN_POINT('Ctrl Pts',(1.78754226164558,28.1954122746457,0.903970915823265));
#6119=CARTESIAN_POINT('Ctrl Pts',(1.54532398476949,28.403745607979,1.38294142126772));
#6120=CARTESIAN_POINT('Ctrl Pts',(1.09607155101171,28.6120789413123,1.676632908208));
#6121=CARTESIAN_POINT('Ctrl Pts',(0.646819117253922,28.8204122746456,1.97032439514833));
#6122=CARTESIAN_POINT('Ctrl Pts',(0.110909353437544,29.028745607979,2.00004246683497));
#6123=CARTESIAN_POINT('Ctrl Pts',(-0.42500041037886,29.2370789413123,2.02976053852165));
#6124=CARTESIAN_POINT('Ctrl Pts',(-0.903970915823293,29.4454122746457,1.78754226164552));
#6125=CARTESIAN_POINT('Ctrl Pts',(-1.38294142126773,29.653745607979,1.54532398476947));
#6126=CARTESIAN_POINT('Ctrl Pts',(-1.67663290820805,29.8620789413123,1.09607155101164));
#6127=CARTESIAN_POINT('Ctrl Pts',(-1.97032439514836,30.0704122746456,0.646819117253891));
#6128=CARTESIAN_POINT('Ctrl Pts',(-2.00004246683501,30.278745607979,0.110909353437458));
#6129=CARTESIAN_POINT('Ctrl Pts',(-2.02976053852165,30.4870789413123,-0.42500041037892));
#6130=CARTESIAN_POINT('Ctrl Pts',(-1.78754226164556,30.6954122746457,-0.903970915823342));
#6131=CARTESIAN_POINT('Ctrl Pts',(-1.5453239847695,30.903745607979,-1.3829414212677));
#6132=CARTESIAN_POINT('Ctrl Pts',(-1.09607155101171,31.1120789413123,-1.6766329082081));
#6133=CARTESIAN_POINT('Ctrl Pts',(-0.64681911725392,31.3204122746456,-1.97032439514837));
#6134=CARTESIAN_POINT('Ctrl Pts',(-0.110909353437529,31.528745607979,-2.00004246683501));
#6135=CARTESIAN_POINT('Ctrl Pts',(0.425000410378862,31.7370789413123,-2.02976053852167));
#6136=CARTESIAN_POINT('Ctrl Pts',(0.903970915823283,31.9454122746457,-1.7875422616456));
#6137=CARTESIAN_POINT('Ctrl Pts',(1.38294142126773,32.153745607979,-1.54532398476955));
#6138=CARTESIAN_POINT('Ctrl Pts',(1.67663290820804,32.3620789413124,-1.09607155101176));
#6139=CARTESIAN_POINT('Ctrl Pts',(1.97032439514836,32.5704122746456,-0.64681911725392));
#6140=CARTESIAN_POINT('Ctrl Pts',(2.00004246683501,32.778745607979,-0.110909353437541));
#6141=CARTESIAN_POINT('Ctrl Pts',(2.02976053852165,32.9870789413124,0.425000410378833));
#6142=CARTESIAN_POINT('Ctrl Pts',(1.78754226164557,33.1954122746457,0.903970915823237));
#6143=CARTESIAN_POINT('Ctrl Pts',(1.5453239847695,33.4037456079789,1.38294142126775));
#6144=CARTESIAN_POINT('Ctrl Pts',(1.09607155101171,33.6120789413123,1.67663290820803));
#6145=CARTESIAN_POINT('Ctrl Pts',(0.646819117253922,33.8204122746456,1.97032439514837));
#6146=CARTESIAN_POINT('Ctrl Pts',(0.11090935343753,34.028745607979,2.00004246683493));
#6147=CARTESIAN_POINT('Ctrl Pts',(-0.42500041037886,34.2370789413123,2.02976053852164));
#6148=CARTESIAN_POINT('Ctrl Pts',(-0.903970915823295,34.4454122746457,1.78754226164551));
#6149=CARTESIAN_POINT('Ctrl Pts',(-1.38294142126774,34.653745607979,1.54532398476948));
#6150=CARTESIAN_POINT('Ctrl Pts',(-1.67663290820803,34.8620789413123,1.09607155101167));
#6151=CARTESIAN_POINT('Ctrl Pts',(-1.97032439514836,35.0704122746456,0.646819117253935));
#6152=CARTESIAN_POINT('Ctrl Pts',(-2.00004246683501,35.2787456079791,0.110909353437478));
#6153=CARTESIAN_POINT('Ctrl Pts',(-2.02976053852165,35.4870789413123,-0.425000410378905));
#6154=CARTESIAN_POINT('Ctrl Pts',(-1.78754226164558,35.6954122746457,-0.903970915823328));
#6155=CARTESIAN_POINT('Ctrl Pts',(-1.5453239847695,35.903745607979,-1.38294142126775));
#6156=CARTESIAN_POINT('Ctrl Pts',(-1.09607155101171,36.1120789413124,-1.67663290820807));
#6157=CARTESIAN_POINT('Ctrl Pts',(-0.646819117253907,36.3204122746457,-1.97032439514837));
#6158=CARTESIAN_POINT('Ctrl Pts',(-0.11090935343753,36.528745607979,-2.00004246683505));
#6159=CARTESIAN_POINT('Ctrl Pts',(0.42500041037886,36.7370789413123,-2.02976053852166));
#6160=CARTESIAN_POINT('Ctrl Pts',(0.903970915823295,36.9454122746457,-1.78754226164563));
#6161=CARTESIAN_POINT('Ctrl Pts',(1.38294142126773,37.1537456079789,-1.5453239847695));
#6162=CARTESIAN_POINT('Ctrl Pts',(1.67663290820805,37.3620789413124,-1.09607155101176));
#6163=CARTESIAN_POINT('Ctrl Pts',(1.97032439514836,37.5704122746456,-0.64681911725392));
#6164=CARTESIAN_POINT('Ctrl Pts',(2.00004246683501,37.778745607979,-0.110909353437575));
#6165=CARTESIAN_POINT('Ctrl Pts',(2.02976053852168,37.9870789413124,0.425000410378855));
#6166=CARTESIAN_POINT('Ctrl Pts',(1.78754226164558,38.1954122746457,0.903970915823252));
#6167=CARTESIAN_POINT('Ctrl Pts',(1.5453239847695,38.4037456079789,1.38294142126773));
#6168=CARTESIAN_POINT('Ctrl Pts',(1.09607155101173,38.6120789413124,1.676632908208));
#6169=CARTESIAN_POINT('Ctrl Pts',(0.646819117253922,38.8204122746457,1.97032439514837));
#6170=CARTESIAN_POINT('Ctrl Pts',(0.110909353437544,39.028745607979,2.00004246683497));
#6171=CARTESIAN_POINT('Ctrl Pts',(-0.425000410378846,39.2370789413124,2.02976053852167));
#6172=CARTESIAN_POINT('Ctrl Pts',(-0.903970915823281,39.4454122746457,1.78754226164553));
#6173=CARTESIAN_POINT('Ctrl Pts',(-1.38294142126773,39.653745607979,1.54532398476946));
#6174=CARTESIAN_POINT('Ctrl Pts',(-1.67663290820805,39.8620789413124,1.09607155101165));
#6175=CARTESIAN_POINT('Ctrl Pts',(-1.97032439514836,40.0704122746457,0.646819117253935));
#6176=CARTESIAN_POINT('Ctrl Pts',(-2.00004246683501,40.278745607979,0.110909353437458));
#6177=CARTESIAN_POINT('Ctrl Pts',(-2.00002123304185,0.278745610073468,0.110909354270813));
#6178=CARTESIAN_POINT('Ctrl Pts',(-2.0297393049518,0.487078943406699,-0.42499471996778));
#6179=CARTESIAN_POINT('Ctrl Pts',(-1.78752387305798,0.695412276740089,-0.903960298205047));
#6180=CARTESIAN_POINT('Ctrl Pts',(-1.54530844116415,0.903745610073333,-1.38292587644223));
#6181=CARTESIAN_POINT('Ctrl Pts',(-1.09606093483686,1.11207894340676,-1.67661451878712));
#6182=CARTESIAN_POINT('Ctrl Pts',(-0.646813428509569,1.32041227674011,-1.97030316113191));
#6183=CARTESIAN_POINT('Ctrl Pts',(-0.110909354270893,1.52874561007344,-2.00002123304186));
#6184=CARTESIAN_POINT('Ctrl Pts',(0.424994719967758,1.7370789434067,-2.02973930495184));
#6185=CARTESIAN_POINT('Ctrl Pts',(0.903960298204994,1.94541227674011,-1.78752387305798));
#6186=CARTESIAN_POINT('Ctrl Pts',(1.38292587644223,2.15374561007344,-1.54530844116415));
#6187=CARTESIAN_POINT('Ctrl Pts',(1.67661451878707,2.36207894340677,-1.09606093483686));
#6188=CARTESIAN_POINT('Ctrl Pts',(1.97030316113191,2.57041227674009,-0.646813428509584));
#6189=CARTESIAN_POINT('Ctrl Pts',(2.00002123304188,2.77874561007344,-0.110909354270911));
#6190=CARTESIAN_POINT('Ctrl Pts',(2.0297393049518,2.98707894340676,0.424994719967736));
#6191=CARTESIAN_POINT('Ctrl Pts',(1.78752387305798,3.1954122767401,0.903960298204943));
#6192=CARTESIAN_POINT('Ctrl Pts',(1.54530844116415,3.40374561007338,1.38292587644222));
#6193=CARTESIAN_POINT('Ctrl Pts',(1.09606093483686,3.61207894340677,1.67661451878706));
#6194=CARTESIAN_POINT('Ctrl Pts',(0.646813428509572,3.82041227674006,1.97030316113189));
#6195=CARTESIAN_POINT('Ctrl Pts',(0.110909354270907,4.02874561007344,2.0000212330418));
#6196=CARTESIAN_POINT('Ctrl Pts',(-0.424994719967742,4.23707894340673,2.02973930495178));
#6197=CARTESIAN_POINT('Ctrl Pts',(-0.903960298204994,4.44541227674011,1.78752387305797));
#6198=CARTESIAN_POINT('Ctrl Pts',(-1.38292587644223,4.65374561007344,1.5453084411641));
#6199=CARTESIAN_POINT('Ctrl Pts',(-1.67661451878708,4.8620789434068,1.0960609348368));
#6200=CARTESIAN_POINT('Ctrl Pts',(-1.9703031611319,5.07041227674005,0.646813428509555));
#6201=CARTESIAN_POINT('Ctrl Pts',(-2.00002123304185,5.27874561007342,0.110909354270813));
#6202=CARTESIAN_POINT('Ctrl Pts',(-2.0297393049518,5.48707894340671,-0.424994719967823));
#6203=CARTESIAN_POINT('Ctrl Pts',(-1.78752387305798,5.6954122767401,-0.903960298205047));
#6204=CARTESIAN_POINT('Ctrl Pts',(-1.54530844116415,5.90374561007338,-1.38292587644222));
#6205=CARTESIAN_POINT('Ctrl Pts',(-1.09606093483685,6.11207894340678,-1.67661451878707));
#6206=CARTESIAN_POINT('Ctrl Pts',(-0.646813428509557,6.3204122767401,-1.97030316113191));
#6207=CARTESIAN_POINT('Ctrl Pts',(-0.110909354270905,6.52874561007347,-2.00002123304191));
#6208=CARTESIAN_POINT('Ctrl Pts',(0.424994719967756,6.73707894340672,-2.02973930495181));
#6209=CARTESIAN_POINT('Ctrl Pts',(0.903960298204995,6.94541227674014,-1.78752387305798));
#6210=CARTESIAN_POINT('Ctrl Pts',(1.38292587644225,7.15374561007342,-1.54530844116421));
#6211=CARTESIAN_POINT('Ctrl Pts',(1.67661451878704,7.36207894340677,-1.09606093483692));
#6212=CARTESIAN_POINT('Ctrl Pts',(1.97030316113191,7.57041227674011,-0.646813428509569));
#6213=CARTESIAN_POINT('Ctrl Pts',(2.00002123304185,7.77874561007349,-0.110909354270917));
#6214=CARTESIAN_POINT('Ctrl Pts',(2.0297393049518,7.98707894340672,0.424994719967736));
#6215=CARTESIAN_POINT('Ctrl Pts',(1.78752387305798,8.19541227674012,0.903960298204985));
#6216=CARTESIAN_POINT('Ctrl Pts',(1.54530844116417,8.40374561007341,1.38292587644223));
#6217=CARTESIAN_POINT('Ctrl Pts',(1.09606093483686,8.6120789434068,1.67661451878701));
#6218=CARTESIAN_POINT('Ctrl Pts',(0.646813428509572,8.82041227674011,1.9703031611319));
#6219=CARTESIAN_POINT('Ctrl Pts',(0.110909354270904,9.02874561007346,2.00002123304179));
#6220=CARTESIAN_POINT('Ctrl Pts',(-0.424994719967754,9.23707894340678,2.0297393049518));
#6221=CARTESIAN_POINT('Ctrl Pts',(-0.903960298204992,9.44541227674011,1.78752387305792));
#6222=CARTESIAN_POINT('Ctrl Pts',(-1.38292587644223,9.65374561007344,1.54530844116415));
#6223=CARTESIAN_POINT('Ctrl Pts',(-1.67661451878707,9.86207894340678,1.09606093483686));
#6224=CARTESIAN_POINT('Ctrl Pts',(-1.97030316113191,10.0704122767401,0.646813428509569));
#6225=CARTESIAN_POINT('Ctrl Pts',(-2.00002123304184,10.2787456100735,0.110909354270841));
#6226=CARTESIAN_POINT('Ctrl Pts',(-2.0297393049518,10.4870789434068,-0.424994719967758));
#6227=CARTESIAN_POINT('Ctrl Pts',(-1.78752387305798,10.6954122767401,-0.903960298205096));
#6228=CARTESIAN_POINT('Ctrl Pts',(-1.54530844116415,10.9037456100734,-1.38292587644225));
#6229=CARTESIAN_POINT('Ctrl Pts',(-1.09606093483686,11.1120789434068,-1.67661451878712));
#6230=CARTESIAN_POINT('Ctrl Pts',(-0.646813428509569,11.3204122767401,-1.97030316113191));
#6231=CARTESIAN_POINT('Ctrl Pts',(-0.110909354270907,11.5287456100735,-2.00002123304188));
#6232=CARTESIAN_POINT('Ctrl Pts',(0.424994719967756,11.7370789434068,-2.02973930495182));
#6233=CARTESIAN_POINT('Ctrl Pts',(0.903960298204994,11.9454122767401,-1.78752387305798));
#6234=CARTESIAN_POINT('Ctrl Pts',(1.38292587644223,12.1537456100734,-1.5453084411642));
#6235=CARTESIAN_POINT('Ctrl Pts',(1.67661451878707,12.3620789434068,-1.09606093483686));
#6236=CARTESIAN_POINT('Ctrl Pts',(1.97030316113194,12.5704122767401,-0.646813428509584));
#6237=CARTESIAN_POINT('Ctrl Pts',(2.00002123304185,12.7787456100735,-0.110909354270959));
#6238=CARTESIAN_POINT('Ctrl Pts',(2.0297393049518,12.9870789434068,0.424994719967758));
#6239=CARTESIAN_POINT('Ctrl Pts',(1.78752387305797,13.1954122767401,0.903960298204936));
#6240=CARTESIAN_POINT('Ctrl Pts',(1.54530844116415,13.4037456100734,1.38292587644223));
#6241=CARTESIAN_POINT('Ctrl Pts',(1.09606093483686,13.6120789434068,1.67661451878707));
#6242=CARTESIAN_POINT('Ctrl Pts',(0.646813428509572,13.8204122767401,1.97030316113191));
#6243=CARTESIAN_POINT('Ctrl Pts',(0.110909354270907,14.0287456100735,2.00002123304182));
#6244=CARTESIAN_POINT('Ctrl Pts',(-0.424994719967756,14.2370789434068,2.0297393049518));
#6245=CARTESIAN_POINT('Ctrl Pts',(-0.903960298204994,14.4454122767402,1.78752387305788));
#6246=CARTESIAN_POINT('Ctrl Pts',(-1.38292587644223,14.6537456100734,1.5453084411641));
#6247=CARTESIAN_POINT('Ctrl Pts',(-1.67661451878707,14.8620789434068,1.0960609348368));
#6248=CARTESIAN_POINT('Ctrl Pts',(-1.97030316113189,15.0704122767401,0.646813428509584));
#6249=CARTESIAN_POINT('Ctrl Pts',(-2.00002123304185,15.2787456100735,0.110909354270848));
#6250=CARTESIAN_POINT('Ctrl Pts',(-2.0297393049518,15.4870789434068,-0.424994719967866));
#6251=CARTESIAN_POINT('Ctrl Pts',(-1.78752387305798,15.6954122767401,-0.903960298205006));
#6252=CARTESIAN_POINT('Ctrl Pts',(-1.54530844116415,15.9037456100734,-1.38292587644223));
#6253=CARTESIAN_POINT('Ctrl Pts',(-1.09606093483685,16.1120789434068,-1.6766145187871));
#6254=CARTESIAN_POINT('Ctrl Pts',(-0.646813428509569,16.3204122767401,-1.97030316113196));
#6255=CARTESIAN_POINT('Ctrl Pts',(-0.110909354270907,16.5287456100735,-2.0000212330419));
#6256=CARTESIAN_POINT('Ctrl Pts',(0.424994719967758,16.7370789434068,-2.0297393049518));
#6257=CARTESIAN_POINT('Ctrl Pts',(0.903960298205007,16.9454122767401,-1.78752387305798));
#6258=CARTESIAN_POINT('Ctrl Pts',(1.38292587644223,17.1537456100734,-1.54530844116415));
#6259=CARTESIAN_POINT('Ctrl Pts',(1.67661451878707,17.3620789434068,-1.09606093483691));
#6260=CARTESIAN_POINT('Ctrl Pts',(1.97030316113191,17.5704122767401,-0.646813428509569));
#6261=CARTESIAN_POINT('Ctrl Pts',(2.00002123304185,17.7787456100735,-0.110909354270917));
#6262=CARTESIAN_POINT('Ctrl Pts',(2.0297393049518,17.9870789434068,0.424994719967701));
#6263=CARTESIAN_POINT('Ctrl Pts',(1.78752387305798,18.1954122767401,0.903960298204978));
#6264=CARTESIAN_POINT('Ctrl Pts',(1.54530844116417,18.4037456100734,1.38292587644223));
#6265=CARTESIAN_POINT('Ctrl Pts',(1.09606093483686,18.6120789434068,1.67661451878701));
#6266=CARTESIAN_POINT('Ctrl Pts',(0.646813428509572,18.8204122767401,1.9703031611319));
#6267=CARTESIAN_POINT('Ctrl Pts',(0.110909354270905,19.0287456100735,2.00002123304181));
#6268=CARTESIAN_POINT('Ctrl Pts',(-0.424994719967756,19.2370789434068,2.0297393049518));
#6269=CARTESIAN_POINT('Ctrl Pts',(-0.903960298204992,19.4454122767402,1.7875238730579));
#6270=CARTESIAN_POINT('Ctrl Pts',(-1.38292587644223,19.6537456100734,1.54530844116415));
#6271=CARTESIAN_POINT('Ctrl Pts',(-1.67661451878707,19.8620789434068,1.09606093483682));
#6272=CARTESIAN_POINT('Ctrl Pts',(-1.97030316113191,20.0704122767401,0.646813428509569));
#6273=CARTESIAN_POINT('Ctrl Pts',(-2.00002123304184,20.2787456100735,0.11090935427082));
#6274=CARTESIAN_POINT('Ctrl Pts',(-2.02973930495179,20.4870789434068,-0.424994719967816));
#6275=CARTESIAN_POINT('Ctrl Pts',(-1.78752387305798,20.6954122767402,-0.903960298205054));
#6276=CARTESIAN_POINT('Ctrl Pts',(-1.54530844116414,20.9037456100735,-1.38292587644227));
#6277=CARTESIAN_POINT('Ctrl Pts',(-1.09606093483687,21.1120789434068,-1.67661451878712));
#6278=CARTESIAN_POINT('Ctrl Pts',(-0.646813428509572,21.3204122767401,-1.97030316113191));
#6279=CARTESIAN_POINT('Ctrl Pts',(-0.110909354270907,21.5287456100735,-2.00002123304186));
#6280=CARTESIAN_POINT('Ctrl Pts',(0.424994719967756,21.7370789434068,-2.0297393049518));
#6281=CARTESIAN_POINT('Ctrl Pts',(0.903960298204994,21.9454122767402,-1.78752387305801));
#6282=CARTESIAN_POINT('Ctrl Pts',(1.38292587644223,22.1537456100734,-1.5453084411642));
#6283=CARTESIAN_POINT('Ctrl Pts',(1.67661451878707,22.3620789434069,-1.09606093483688));
#6284=CARTESIAN_POINT('Ctrl Pts',(1.97030316113188,22.5704122767401,-0.646813428509569));
#6285=CARTESIAN_POINT('Ctrl Pts',(2.00002123304185,22.7787456100735,-0.110909354270945));
#6286=CARTESIAN_POINT('Ctrl Pts',(2.02973930495183,22.9870789434068,0.424994719967758));
#6287=CARTESIAN_POINT('Ctrl Pts',(1.78752387305798,23.1954122767402,0.903960298204936));
#6288=CARTESIAN_POINT('Ctrl Pts',(1.54530844116415,23.4037456100734,1.38292587644223));
#6289=CARTESIAN_POINT('Ctrl Pts',(1.09606093483686,23.6120789434068,1.67661451878704));
#6290=CARTESIAN_POINT('Ctrl Pts',(0.646813428509586,23.8204122767401,1.97030316113191));
#6291=CARTESIAN_POINT('Ctrl Pts',(0.110909354270907,24.0287456100735,2.00002123304177));
#6292=CARTESIAN_POINT('Ctrl Pts',(-0.424994719967756,24.2370789434068,2.02973930495181));
#6293=CARTESIAN_POINT('Ctrl Pts',(-0.903960298204994,24.4454122767402,1.78752387305788));
#6294=CARTESIAN_POINT('Ctrl Pts',(-1.38292587644222,24.6537456100735,1.54530844116407));
#6295=CARTESIAN_POINT('Ctrl Pts',(-1.67661451878706,24.8620789434068,1.09606093483681));
#6296=CARTESIAN_POINT('Ctrl Pts',(-1.97030316113191,25.0704122767401,0.646813428509584));
#6297=CARTESIAN_POINT('Ctrl Pts',(-2.00002123304185,25.2787456100735,0.110909354270855));
#6298=CARTESIAN_POINT('Ctrl Pts',(-2.0297393049518,25.4870789434068,-0.424994719967787));
#6299=CARTESIAN_POINT('Ctrl Pts',(-1.78752387305798,25.6954122767401,-0.903960298205006));
#6300=CARTESIAN_POINT('Ctrl Pts',(-1.54530844116415,25.9037456100735,-1.38292587644223));
#6301=CARTESIAN_POINT('Ctrl Pts',(-1.09606093483686,26.1120789434068,-1.6766145187871));
#6302=CARTESIAN_POINT('Ctrl Pts',(-0.646813428509569,26.3204122767401,-1.97030316113196));
#6303=CARTESIAN_POINT('Ctrl Pts',(-0.110909354270907,26.5287456100735,-2.00002123304189));
#6304=CARTESIAN_POINT('Ctrl Pts',(0.424994719967771,26.7370789434068,-2.0297393049518));
#6305=CARTESIAN_POINT('Ctrl Pts',(0.903960298205007,26.9454122767402,-1.78752387305803));
#6306=CARTESIAN_POINT('Ctrl Pts',(1.38292587644223,27.1537456100734,-1.54530844116415));
#6307=CARTESIAN_POINT('Ctrl Pts',(1.67661451878704,27.3620789434068,-1.0960609348369));
#6308=CARTESIAN_POINT('Ctrl Pts',(1.97030316113191,27.5704122767401,-0.646813428509598));
#6309=CARTESIAN_POINT('Ctrl Pts',(2.00002123304183,27.7787456100735,-0.110909354270911));
#6310=CARTESIAN_POINT('Ctrl Pts',(2.0297393049518,27.9870789434068,0.424994719967751));
#6311=CARTESIAN_POINT('Ctrl Pts',(1.78752387305798,28.1954122767402,0.903960298204964));
#6312=CARTESIAN_POINT('Ctrl Pts',(1.54530844116414,28.4037456100735,1.38292587644223));
#6313=CARTESIAN_POINT('Ctrl Pts',(1.09606093483686,28.6120789434068,1.67661451878702));
#6314=CARTESIAN_POINT('Ctrl Pts',(0.646813428509572,28.8204122767401,1.97030316113188));
#6315=CARTESIAN_POINT('Ctrl Pts',(0.110909354270921,29.0287456100735,2.00002123304182));
#6316=CARTESIAN_POINT('Ctrl Pts',(-0.424994719967756,29.2370789434068,2.0297393049518));
#6317=CARTESIAN_POINT('Ctrl Pts',(-0.903960298204992,29.4454122767402,1.78752387305792));
#6318=CARTESIAN_POINT('Ctrl Pts',(-1.38292587644223,29.6537456100735,1.54530844116412));
#6319=CARTESIAN_POINT('Ctrl Pts',(-1.67661451878707,29.8620789434068,1.09606093483679));
#6320=CARTESIAN_POINT('Ctrl Pts',(-1.97030316113191,30.0704122767401,0.646813428509541));
#6321=CARTESIAN_POINT('Ctrl Pts',(-2.00002123304185,30.2787456100735,0.110909354270834));
#6322=CARTESIAN_POINT('Ctrl Pts',(-2.0297393049518,30.4870789434068,-0.424994719967816));
#6323=CARTESIAN_POINT('Ctrl Pts',(-1.78752387305796,30.6954122767402,-0.90396029820504));
#6324=CARTESIAN_POINT('Ctrl Pts',(-1.54530844116415,30.9037456100735,-1.3829258764422));
#6325=CARTESIAN_POINT('Ctrl Pts',(-1.09606093483686,31.1120789434068,-1.67661451878712));
#6326=CARTESIAN_POINT('Ctrl Pts',(-0.646813428509569,31.3204122767401,-1.97030316113191));
#6327=CARTESIAN_POINT('Ctrl Pts',(-0.110909354270905,31.5287456100735,-2.00002123304186));
#6328=CARTESIAN_POINT('Ctrl Pts',(0.424994719967758,31.7370789434068,-2.02973930495182));
#6329=CARTESIAN_POINT('Ctrl Pts',(0.903960298204981,31.9454122767402,-1.787523873058));
#6330=CARTESIAN_POINT('Ctrl Pts',(1.38292587644223,32.1537456100735,-1.5453084411642));
#6331=CARTESIAN_POINT('Ctrl Pts',(1.67661451878707,32.3620789434069,-1.09606093483691));
#6332=CARTESIAN_POINT('Ctrl Pts',(1.97030316113191,32.5704122767401,-0.646813428509569));
#6333=CARTESIAN_POINT('Ctrl Pts',(2.00002123304185,32.7787456100735,-0.110909354270917));
#6334=CARTESIAN_POINT('Ctrl Pts',(2.0297393049518,32.9870789434069,0.424994719967729));
#6335=CARTESIAN_POINT('Ctrl Pts',(1.78752387305797,33.1954122767402,0.903960298204936));
#6336=CARTESIAN_POINT('Ctrl Pts',(1.54530844116415,33.4037456100734,1.38292587644225));
#6337=CARTESIAN_POINT('Ctrl Pts',(1.09606093483686,33.6120789434068,1.67661451878706));
#6338=CARTESIAN_POINT('Ctrl Pts',(0.646813428509572,33.8204122767401,1.97030316113191));
#6339=CARTESIAN_POINT('Ctrl Pts',(0.110909354270907,34.0287456100735,2.00002123304178));
#6340=CARTESIAN_POINT('Ctrl Pts',(-0.424994719967756,34.2370789434068,2.0297393049518));
#6341=CARTESIAN_POINT('Ctrl Pts',(-0.903960298204994,34.4454122767402,1.78752387305791));
#6342=CARTESIAN_POINT('Ctrl Pts',(-1.38292587644225,34.6537456100735,1.54530844116413));
#6343=CARTESIAN_POINT('Ctrl Pts',(-1.67661451878706,34.8620789434068,1.09606093483682));
#6344=CARTESIAN_POINT('Ctrl Pts',(-1.9703031611319,35.0704122767402,0.646813428509584));
#6345=CARTESIAN_POINT('Ctrl Pts',(-2.00002123304185,35.2787456100736,0.110909354270855));
#6346=CARTESIAN_POINT('Ctrl Pts',(-2.0297393049518,35.4870789434068,-0.424994719967801));
#6347=CARTESIAN_POINT('Ctrl Pts',(-1.78752387305798,35.6954122767402,-0.903960298205026));
#6348=CARTESIAN_POINT('Ctrl Pts',(-1.54530844116415,35.9037456100735,-1.38292587644225));
#6349=CARTESIAN_POINT('Ctrl Pts',(-1.09606093483686,36.1120789434069,-1.67661451878709));
#6350=CARTESIAN_POINT('Ctrl Pts',(-0.646813428509557,36.3204122767402,-1.97030316113191));
#6351=CARTESIAN_POINT('Ctrl Pts',(-0.110909354270907,36.5287456100735,-2.0000212330419));
#6352=CARTESIAN_POINT('Ctrl Pts',(0.424994719967756,36.7370789434068,-2.02973930495181));
#6353=CARTESIAN_POINT('Ctrl Pts',(0.903960298204994,36.9454122767402,-1.78752387305804));
#6354=CARTESIAN_POINT('Ctrl Pts',(1.38292587644223,37.1537456100734,-1.54530844116415));
#6355=CARTESIAN_POINT('Ctrl Pts',(1.67661451878707,37.3620789434069,-1.09606093483691));
#6356=CARTESIAN_POINT('Ctrl Pts',(1.97030316113191,37.5704122767401,-0.646813428509569));
#6357=CARTESIAN_POINT('Ctrl Pts',(2.00002123304185,37.7787456100735,-0.110909354270952));
#6358=CARTESIAN_POINT('Ctrl Pts',(2.02973930495183,37.9870789434069,0.424994719967751));
#6359=CARTESIAN_POINT('Ctrl Pts',(1.78752387305798,38.1954122767402,0.90396029820495));
#6360=CARTESIAN_POINT('Ctrl Pts',(1.54530844116415,38.4037456100734,1.38292587644223));
#6361=CARTESIAN_POINT('Ctrl Pts',(1.09606093483688,38.6120789434069,1.67661451878703));
#6362=CARTESIAN_POINT('Ctrl Pts',(0.646813428509572,38.8204122767402,1.97030316113192));
#6363=CARTESIAN_POINT('Ctrl Pts',(0.110909354270921,39.0287456100735,2.00002123304182));
#6364=CARTESIAN_POINT('Ctrl Pts',(-0.424994719967742,39.2370789434069,2.02973930495182));
#6365=CARTESIAN_POINT('Ctrl Pts',(-0.90396029820498,39.4454122767402,1.78752387305793));
#6366=CARTESIAN_POINT('Ctrl Pts',(-1.38292587644223,39.6537456100735,1.54530844116411));
#6367=CARTESIAN_POINT('Ctrl Pts',(-1.67661451878707,39.8620789434069,1.0960609348368));
#6368=CARTESIAN_POINT('Ctrl Pts',(-1.97030316113191,40.0704122767402,0.646813428509584));
#6369=CARTESIAN_POINT('Ctrl Pts',(-2.00002123304185,40.2787456100735,0.110909354270834));
#6370=CARTESIAN_POINT('Ctrl Pts',(-2.,0.278745610073468,0.110909354270813));
#6371=CARTESIAN_POINT('Ctrl Pts',(-2.02971807190995,0.487078943406699,-0.424989030591362));
#6372=CARTESIAN_POINT('Ctrl Pts',(-1.78750548470433,0.695412276740089,-0.90394968168412));
#6373=CARTESIAN_POINT('Ctrl Pts',(-1.54529289749872,0.903745610073333,-1.3829103327768));
#6374=CARTESIAN_POINT('Ctrl Pts',(-1.09605031831593,1.11207894340676,-1.67659613043348));
#6375=CARTESIAN_POINT('Ctrl Pts',(-0.646807739133152,1.32041227674011,-1.97028192809006));
#6376=CARTESIAN_POINT('Ctrl Pts',(-0.110909354270893,1.52874561007344,-2.00000000000001));
#6377=CARTESIAN_POINT('Ctrl Pts',(0.42498903059134,1.7370789434067,-2.02971807190998));
#6378=CARTESIAN_POINT('Ctrl Pts',(0.903949681684066,1.94541227674011,-1.78750548470433));
#6379=CARTESIAN_POINT('Ctrl Pts',(1.38291033277679,2.15374561007344,-1.54529289749872));
#6380=CARTESIAN_POINT('Ctrl Pts',(1.67659613043343,2.36207894340677,-1.09605031831594));
#6381=CARTESIAN_POINT('Ctrl Pts',(1.97028192809005,2.57041227674009,-0.646807739133166));
#6382=CARTESIAN_POINT('Ctrl Pts',(2.00000000000003,2.77874561007344,-0.110909354270911));
#6383=CARTESIAN_POINT('Ctrl Pts',(2.02971807190995,2.98707894340676,0.424989030591319));
#6384=CARTESIAN_POINT('Ctrl Pts',(1.78750548470433,3.1954122767401,0.903949681684016));
#6385=CARTESIAN_POINT('Ctrl Pts',(1.54529289749872,3.40374561007338,1.38291033277678));
#6386=CARTESIAN_POINT('Ctrl Pts',(1.09605031831593,3.61207894340677,1.67659613043342));
#6387=CARTESIAN_POINT('Ctrl Pts',(0.646807739133154,3.82041227674006,1.97028192809004));
#6388=CARTESIAN_POINT('Ctrl Pts',(0.110909354270907,4.02874561007344,1.99999999999995));
#6389=CARTESIAN_POINT('Ctrl Pts',(-0.424989030591324,4.23707894340672,2.02971807190993));
#6390=CARTESIAN_POINT('Ctrl Pts',(-0.903949681684066,4.44541227674011,1.78750548470433));
#6391=CARTESIAN_POINT('Ctrl Pts',(-1.38291033277679,4.65374561007344,1.54529289749866));
#6392=CARTESIAN_POINT('Ctrl Pts',(-1.67659613043344,4.8620789434068,1.09605031831587));
#6393=CARTESIAN_POINT('Ctrl Pts',(-1.97028192809005,5.07041227674005,0.646807739133138));
#6394=CARTESIAN_POINT('Ctrl Pts',(-2.,5.27874561007342,0.110909354270813));
#6395=CARTESIAN_POINT('Ctrl Pts',(-2.02971807190995,5.48707894340671,-0.424989030591405));
#6396=CARTESIAN_POINT('Ctrl Pts',(-1.78750548470433,5.6954122767401,-0.90394968168412));
#6397=CARTESIAN_POINT('Ctrl Pts',(-1.54529289749872,5.90374561007338,-1.38291033277678));
#6398=CARTESIAN_POINT('Ctrl Pts',(-1.09605031831592,6.11207894340678,-1.67659613043342));
#6399=CARTESIAN_POINT('Ctrl Pts',(-0.646807739133139,6.3204122767401,-1.97028192809006));
#6400=CARTESIAN_POINT('Ctrl Pts',(-0.110909354270905,6.52874561007347,-2.00000000000006));
#6401=CARTESIAN_POINT('Ctrl Pts',(0.424989030591338,6.73707894340672,-2.02971807190996));
#6402=CARTESIAN_POINT('Ctrl Pts',(0.903949681684068,6.94541227674014,-1.78750548470433));
#6403=CARTESIAN_POINT('Ctrl Pts',(1.38291033277681,7.15374561007342,-1.54529289749877));
#6404=CARTESIAN_POINT('Ctrl Pts',(1.6765961304334,7.36207894340677,-1.09605031831599));
#6405=CARTESIAN_POINT('Ctrl Pts',(1.97028192809006,7.57041227674011,-0.646807739133152));
#6406=CARTESIAN_POINT('Ctrl Pts',(2.,7.77874561007349,-0.110909354270917));
#6407=CARTESIAN_POINT('Ctrl Pts',(2.02971807190995,7.98707894340672,0.424989030591319));
#6408=CARTESIAN_POINT('Ctrl Pts',(1.78750548470433,8.19541227674012,0.903949681684058));
#6409=CARTESIAN_POINT('Ctrl Pts',(1.54529289749873,8.40374561007341,1.3829103327768));
#6410=CARTESIAN_POINT('Ctrl Pts',(1.09605031831593,8.6120789434068,1.67659613043337));
#6411=CARTESIAN_POINT('Ctrl Pts',(0.646807739133154,8.82041227674011,1.97028192809005));
#6412=CARTESIAN_POINT('Ctrl Pts',(0.110909354270904,9.02874561007346,1.99999999999994));
#6413=CARTESIAN_POINT('Ctrl Pts',(-0.424989030591337,9.23707894340678,2.02971807190995));
#6414=CARTESIAN_POINT('Ctrl Pts',(-0.903949681684064,9.44541227674011,1.78750548470427));
#6415=CARTESIAN_POINT('Ctrl Pts',(-1.38291033277679,9.65374561007344,1.54529289749871));
#6416=CARTESIAN_POINT('Ctrl Pts',(-1.67659613043342,9.86207894340678,1.09605031831593));
#6417=CARTESIAN_POINT('Ctrl Pts',(-1.97028192809005,10.0704122767401,0.646807739133152));
#6418=CARTESIAN_POINT('Ctrl Pts',(-1.99999999999999,10.2787456100735,0.110909354270841));
#6419=CARTESIAN_POINT('Ctrl Pts',(-2.02971807190994,10.4870789434068,-0.42498903059134));
#6420=CARTESIAN_POINT('Ctrl Pts',(-1.78750548470433,10.6954122767401,-0.903949681684169));
#6421=CARTESIAN_POINT('Ctrl Pts',(-1.54529289749871,10.9037456100734,-1.38291033277681));
#6422=CARTESIAN_POINT('Ctrl Pts',(-1.09605031831593,11.1120789434068,-1.67659613043348));
#6423=CARTESIAN_POINT('Ctrl Pts',(-0.646807739133152,11.3204122767401,-1.97028192809006));
#6424=CARTESIAN_POINT('Ctrl Pts',(-0.110909354270907,11.5287456100735,-2.00000000000002));
#6425=CARTESIAN_POINT('Ctrl Pts',(0.424989030591338,11.7370789434068,-2.02971807190997));
#6426=CARTESIAN_POINT('Ctrl Pts',(0.903949681684066,11.9454122767401,-1.78750548470433));
#6427=CARTESIAN_POINT('Ctrl Pts',(1.3829103327768,12.1537456100734,-1.54529289749877));
#6428=CARTESIAN_POINT('Ctrl Pts',(1.67659613043342,12.3620789434068,-1.09605031831594));
#6429=CARTESIAN_POINT('Ctrl Pts',(1.97028192809008,12.5704122767401,-0.646807739133166));
#6430=CARTESIAN_POINT('Ctrl Pts',(2.,12.7787456100735,-0.110909354270959));
#6431=CARTESIAN_POINT('Ctrl Pts',(2.02971807190995,12.9870789434068,0.42498903059134));
#6432=CARTESIAN_POINT('Ctrl Pts',(1.78750548470433,13.1954122767401,0.903949681684009));
#6433=CARTESIAN_POINT('Ctrl Pts',(1.54529289749872,13.4037456100734,1.38291033277679));
#6434=CARTESIAN_POINT('Ctrl Pts',(1.09605031831593,13.6120789434068,1.67659613043342));
#6435=CARTESIAN_POINT('Ctrl Pts',(0.646807739133154,13.8204122767401,1.97028192809006));
#6436=CARTESIAN_POINT('Ctrl Pts',(0.110909354270907,14.0287456100735,1.99999999999997));
#6437=CARTESIAN_POINT('Ctrl Pts',(-0.424989030591338,14.2370789434068,2.02971807190995));
#6438=CARTESIAN_POINT('Ctrl Pts',(-0.903949681684066,14.4454122767402,1.78750548470424));
#6439=CARTESIAN_POINT('Ctrl Pts',(-1.38291033277679,14.6537456100734,1.54529289749866));
#6440=CARTESIAN_POINT('Ctrl Pts',(-1.67659613043342,14.8620789434068,1.09605031831587));
#6441=CARTESIAN_POINT('Ctrl Pts',(-1.97028192809004,15.0704122767401,0.646807739133166));
#6442=CARTESIAN_POINT('Ctrl Pts',(-2.,15.2787456100735,0.110909354270848));
#6443=CARTESIAN_POINT('Ctrl Pts',(-2.02971807190995,15.4870789434068,-0.424989030591448));
#6444=CARTESIAN_POINT('Ctrl Pts',(-1.78750548470433,15.6954122767401,-0.903949681684079));
#6445=CARTESIAN_POINT('Ctrl Pts',(-1.54529289749872,15.9037456100734,-1.3829103327768));
#6446=CARTESIAN_POINT('Ctrl Pts',(-1.09605031831592,16.1120789434068,-1.67659613043346));
#6447=CARTESIAN_POINT('Ctrl Pts',(-0.646807739133152,16.3204122767401,-1.97028192809011));
#6448=CARTESIAN_POINT('Ctrl Pts',(-0.110909354270907,16.5287456100735,-2.00000000000005));
#6449=CARTESIAN_POINT('Ctrl Pts',(0.42498903059134,16.7370789434068,-2.02971807190995));
#6450=CARTESIAN_POINT('Ctrl Pts',(0.90394968168408,16.9454122767401,-1.78750548470433));
#6451=CARTESIAN_POINT('Ctrl Pts',(1.38291033277679,17.1537456100734,-1.54529289749872));
#6452=CARTESIAN_POINT('Ctrl Pts',(1.67659613043342,17.3620789434068,-1.09605031831599));
#6453=CARTESIAN_POINT('Ctrl Pts',(1.97028192809005,17.5704122767401,-0.646807739133152));
#6454=CARTESIAN_POINT('Ctrl Pts',(2.,17.7787456100735,-0.110909354270917));
#6455=CARTESIAN_POINT('Ctrl Pts',(2.02971807190995,17.9870789434068,0.424989030591283));
#6456=CARTESIAN_POINT('Ctrl Pts',(1.78750548470433,18.1954122767401,0.903949681684051));
#6457=CARTESIAN_POINT('Ctrl Pts',(1.54529289749873,18.4037456100734,1.3829103327768));
#6458=CARTESIAN_POINT('Ctrl Pts',(1.09605031831593,18.6120789434068,1.67659613043337));
#6459=CARTESIAN_POINT('Ctrl Pts',(0.646807739133154,18.8204122767401,1.97028192809005));
#6460=CARTESIAN_POINT('Ctrl Pts',(0.110909354270905,19.0287456100735,1.99999999999995));
#6461=CARTESIAN_POINT('Ctrl Pts',(-0.424989030591338,19.2370789434068,2.02971807190995));
#6462=CARTESIAN_POINT('Ctrl Pts',(-0.903949681684064,19.4454122767402,1.78750548470426));
#6463=CARTESIAN_POINT('Ctrl Pts',(-1.38291033277679,19.6537456100734,1.54529289749871));
#6464=CARTESIAN_POINT('Ctrl Pts',(-1.67659613043342,19.8620789434068,1.0960503183159));
#6465=CARTESIAN_POINT('Ctrl Pts',(-1.97028192809006,20.0704122767401,0.646807739133152));
#6466=CARTESIAN_POINT('Ctrl Pts',(-1.99999999999999,20.2787456100735,0.11090935427082));
#6467=CARTESIAN_POINT('Ctrl Pts',(-2.02971807190993,20.4870789434068,-0.424989030591398));
#6468=CARTESIAN_POINT('Ctrl Pts',(-1.78750548470433,20.6954122767402,-0.903949681684127));
#6469=CARTESIAN_POINT('Ctrl Pts',(-1.5452928974987,20.9037456100735,-1.38291033277683));
#6470=CARTESIAN_POINT('Ctrl Pts',(-1.09605031831595,21.1120789434068,-1.67659613043348));
#6471=CARTESIAN_POINT('Ctrl Pts',(-0.646807739133154,21.3204122767401,-1.97028192809006));
#6472=CARTESIAN_POINT('Ctrl Pts',(-0.110909354270907,21.5287456100735,-2.));
#6473=CARTESIAN_POINT('Ctrl Pts',(0.424989030591338,21.7370789434068,-2.02971807190994));
#6474=CARTESIAN_POINT('Ctrl Pts',(0.903949681684066,21.9454122767402,-1.78750548470436));
#6475=CARTESIAN_POINT('Ctrl Pts',(1.38291033277679,22.1537456100734,-1.54529289749877));
#6476=CARTESIAN_POINT('Ctrl Pts',(1.67659613043343,22.3620789434069,-1.09605031831595));
#6477=CARTESIAN_POINT('Ctrl Pts',(1.97028192809003,22.5704122767401,-0.646807739133152));
#6478=CARTESIAN_POINT('Ctrl Pts',(2.,22.7787456100735,-0.110909354270945));
#6479=CARTESIAN_POINT('Ctrl Pts',(2.02971807190997,22.9870789434068,0.42498903059134));
#6480=CARTESIAN_POINT('Ctrl Pts',(1.78750548470433,23.1954122767402,0.903949681684009));
#6481=CARTESIAN_POINT('Ctrl Pts',(1.54529289749872,23.4037456100734,1.38291033277679));
#6482=CARTESIAN_POINT('Ctrl Pts',(1.09605031831593,23.6120789434068,1.6765961304334));
#6483=CARTESIAN_POINT('Ctrl Pts',(0.646807739133168,23.8204122767401,1.97028192809006));
#6484=CARTESIAN_POINT('Ctrl Pts',(0.110909354270907,24.0287456100735,1.99999999999992));
#6485=CARTESIAN_POINT('Ctrl Pts',(-0.424989030591338,24.2370789434068,2.02971807190996));
#6486=CARTESIAN_POINT('Ctrl Pts',(-0.903949681684066,24.4454122767402,1.78750548470424));
#6487=CARTESIAN_POINT('Ctrl Pts',(-1.38291033277678,24.6537456100735,1.54529289749864));
#6488=CARTESIAN_POINT('Ctrl Pts',(-1.67659613043341,24.8620789434068,1.09605031831588));
#6489=CARTESIAN_POINT('Ctrl Pts',(-1.97028192809005,25.0704122767401,0.646807739133166));
#6490=CARTESIAN_POINT('Ctrl Pts',(-2.,25.2787456100735,0.110909354270855));
#6491=CARTESIAN_POINT('Ctrl Pts',(-2.02971807190995,25.4870789434068,-0.424989030591369));
#6492=CARTESIAN_POINT('Ctrl Pts',(-1.78750548470433,25.6954122767401,-0.903949681684079));
#6493=CARTESIAN_POINT('Ctrl Pts',(-1.54529289749871,25.9037456100735,-1.3829103327768));
#6494=CARTESIAN_POINT('Ctrl Pts',(-1.09605031831593,26.1120789434068,-1.67659613043345));
#6495=CARTESIAN_POINT('Ctrl Pts',(-0.646807739133152,26.3204122767401,-1.97028192809011));
#6496=CARTESIAN_POINT('Ctrl Pts',(-0.110909354270907,26.5287456100735,-2.00000000000004));
#6497=CARTESIAN_POINT('Ctrl Pts',(0.424989030591353,26.7370789434068,-2.02971807190995));
#6498=CARTESIAN_POINT('Ctrl Pts',(0.90394968168408,26.9454122767402,-1.78750548470438));
#6499=CARTESIAN_POINT('Ctrl Pts',(1.38291033277679,27.1537456100734,-1.54529289749872));
#6500=CARTESIAN_POINT('Ctrl Pts',(1.6765961304334,27.3620789434068,-1.09605031831597));
#6501=CARTESIAN_POINT('Ctrl Pts',(1.97028192809005,27.5704122767401,-0.64680773913318));
#6502=CARTESIAN_POINT('Ctrl Pts',(1.99999999999997,27.7787456100735,-0.110909354270911));
#6503=CARTESIAN_POINT('Ctrl Pts',(2.02971807190995,27.9870789434068,0.424989030591333));
#6504=CARTESIAN_POINT('Ctrl Pts',(1.78750548470433,28.1954122767402,0.903949681684037));
#6505=CARTESIAN_POINT('Ctrl Pts',(1.5452928974987,28.4037456100735,1.38291033277679));
#6506=CARTESIAN_POINT('Ctrl Pts',(1.09605031831593,28.6120789434068,1.67659613043337));
#6507=CARTESIAN_POINT('Ctrl Pts',(0.646807739133154,28.8204122767401,1.97028192809002));
#6508=CARTESIAN_POINT('Ctrl Pts',(0.110909354270921,29.0287456100735,1.99999999999997));
#6509=CARTESIAN_POINT('Ctrl Pts',(-0.424989030591338,29.2370789434068,2.02971807190995));
#6510=CARTESIAN_POINT('Ctrl Pts',(-0.903949681684064,29.4454122767402,1.78750548470427));
#6511=CARTESIAN_POINT('Ctrl Pts',(-1.38291033277679,29.6537456100735,1.54529289749868));
#6512=CARTESIAN_POINT('Ctrl Pts',(-1.67659613043342,29.8620789434068,1.09605031831586));
#6513=CARTESIAN_POINT('Ctrl Pts',(-1.97028192809005,30.0704122767401,0.646807739133123));
#6514=CARTESIAN_POINT('Ctrl Pts',(-2.,30.2787456100735,0.110909354270834));
#6515=CARTESIAN_POINT('Ctrl Pts',(-2.02971807190995,30.4870789434068,-0.424989030591398));
#6516=CARTESIAN_POINT('Ctrl Pts',(-1.78750548470432,30.6954122767402,-0.903949681684113));
#6517=CARTESIAN_POINT('Ctrl Pts',(-1.54529289749872,30.9037456100735,-1.38291033277676));
#6518=CARTESIAN_POINT('Ctrl Pts',(-1.09605031831593,31.1120789434068,-1.67659613043348));
#6519=CARTESIAN_POINT('Ctrl Pts',(-0.646807739133152,31.3204122767401,-1.97028192809006));
#6520=CARTESIAN_POINT('Ctrl Pts',(-0.110909354270905,31.5287456100735,-2.));
#6521=CARTESIAN_POINT('Ctrl Pts',(0.42498903059134,31.7370789434068,-2.02971807190996));
#6522=CARTESIAN_POINT('Ctrl Pts',(0.903949681684054,31.9454122767402,-1.78750548470435));
#6523=CARTESIAN_POINT('Ctrl Pts',(1.38291033277679,32.1537456100735,-1.54529289749877));
#6524=CARTESIAN_POINT('Ctrl Pts',(1.67659613043342,32.3620789434069,-1.09605031831598));
#6525=CARTESIAN_POINT('Ctrl Pts',(1.97028192809005,32.5704122767401,-0.646807739133152));
#6526=CARTESIAN_POINT('Ctrl Pts',(2.,32.7787456100735,-0.110909354270917));
#6527=CARTESIAN_POINT('Ctrl Pts',(2.02971807190995,32.9870789434069,0.424989030591311));
#6528=CARTESIAN_POINT('Ctrl Pts',(1.78750548470433,33.1954122767402,0.903949681684009));
#6529=CARTESIAN_POINT('Ctrl Pts',(1.54529289749872,33.4037456100734,1.38291033277681));
#6530=CARTESIAN_POINT('Ctrl Pts',(1.09605031831593,33.6120789434068,1.67659613043341));
#6531=CARTESIAN_POINT('Ctrl Pts',(0.646807739133154,33.8204122767401,1.97028192809006));
#6532=CARTESIAN_POINT('Ctrl Pts',(0.110909354270907,34.0287456100735,1.99999999999993));
#6533=CARTESIAN_POINT('Ctrl Pts',(-0.424989030591338,34.2370789434068,2.02971807190994));
#6534=CARTESIAN_POINT('Ctrl Pts',(-0.903949681684066,34.4454122767402,1.78750548470426));
#6535=CARTESIAN_POINT('Ctrl Pts',(-1.38291033277681,34.6537456100735,1.54529289749869));
#6536=CARTESIAN_POINT('Ctrl Pts',(-1.67659613043341,34.8620789434068,1.0960503183159));
#6537=CARTESIAN_POINT('Ctrl Pts',(-1.97028192809005,35.0704122767402,0.646807739133166));
#6538=CARTESIAN_POINT('Ctrl Pts',(-2.,35.2787456100736,0.110909354270855));
#6539=CARTESIAN_POINT('Ctrl Pts',(-2.02971807190995,35.4870789434068,-0.424989030591383));
#6540=CARTESIAN_POINT('Ctrl Pts',(-1.78750548470433,35.6954122767402,-0.903949681684099));
#6541=CARTESIAN_POINT('Ctrl Pts',(-1.54529289749872,35.9037456100735,-1.38291033277681));
#6542=CARTESIAN_POINT('Ctrl Pts',(-1.09605031831593,36.1120789434069,-1.67659613043344));
#6543=CARTESIAN_POINT('Ctrl Pts',(-0.646807739133139,36.3204122767402,-1.97028192809006));
#6544=CARTESIAN_POINT('Ctrl Pts',(-0.110909354270907,36.5287456100735,-2.00000000000004));
#6545=CARTESIAN_POINT('Ctrl Pts',(0.424989030591338,36.7370789434068,-2.02971807190996));
#6546=CARTESIAN_POINT('Ctrl Pts',(0.903949681684066,36.9454122767402,-1.78750548470439));
#6547=CARTESIAN_POINT('Ctrl Pts',(1.38291033277679,37.1537456100734,-1.54529289749872));
#6548=CARTESIAN_POINT('Ctrl Pts',(1.67659613043343,37.3620789434069,-1.09605031831598));
#6549=CARTESIAN_POINT('Ctrl Pts',(1.97028192809006,37.5704122767401,-0.646807739133152));
#6550=CARTESIAN_POINT('Ctrl Pts',(2.,37.7787456100735,-0.110909354270952));
#6551=CARTESIAN_POINT('Ctrl Pts',(2.02971807190997,37.9870789434069,0.424989030591333));
#6552=CARTESIAN_POINT('Ctrl Pts',(1.78750548470433,38.1954122767402,0.903949681684023));
#6553=CARTESIAN_POINT('Ctrl Pts',(1.54529289749872,38.4037456100734,1.3829103327768));
#6554=CARTESIAN_POINT('Ctrl Pts',(1.09605031831595,38.6120789434069,1.67659613043338));
#6555=CARTESIAN_POINT('Ctrl Pts',(0.646807739133154,38.8204122767402,1.97028192809006));
#6556=CARTESIAN_POINT('Ctrl Pts',(0.110909354270921,39.0287456100735,1.99999999999997));
#6557=CARTESIAN_POINT('Ctrl Pts',(-0.424989030591324,39.2370789434069,2.02971807190996));
#6558=CARTESIAN_POINT('Ctrl Pts',(-0.903949681684052,39.4454122767402,1.78750548470429));
#6559=CARTESIAN_POINT('Ctrl Pts',(-1.38291033277679,39.6537456100735,1.54529289749867));
#6560=CARTESIAN_POINT('Ctrl Pts',(-1.67659613043342,39.8620789434069,1.09605031831587));
#6561=CARTESIAN_POINT('Ctrl Pts',(-1.97028192809005,40.0704122767402,0.646807739133166));
#6562=CARTESIAN_POINT('Ctrl Pts',(-2.,40.2787456100735,0.110909354270834));
#6563=CARTESIAN_POINT('Ctrl Pts',(-1.40000000000002,0.278745610073447,0.110909354270819));
#6564=CARTESIAN_POINT('Ctrl Pts',(-1.42971807190993,0.487078943406762,-0.264219515132761));
#6565=CARTESIAN_POINT('Ctrl Pts',(-1.26789024243367,0.695412276740075,-0.603949681684109));
#6566=CARTESIAN_POINT('Ctrl Pts',(-1.10606241295736,0.903745610073446,-0.943679848235563));
#6567=CARTESIAN_POINT('Ctrl Pts',(-0.796050318315929,1.11207894340677,-1.1569808881628));
#6568=CARTESIAN_POINT('Ctrl Pts',(-0.486038223674453,1.3204122767401,-1.37028192809014));
#6569=CARTESIAN_POINT('Ctrl Pts',(-0.110909354270902,1.52874561007343,-1.40000000000009));
#6570=CARTESIAN_POINT('Ctrl Pts',(0.26421951513267,1.73707894340676,-1.42971807191003));
#6571=CARTESIAN_POINT('Ctrl Pts',(0.60394968168407,1.9454122767401,-1.26789024243367));
#6572=CARTESIAN_POINT('Ctrl Pts',(0.943679848235471,2.15374561007345,-1.10606241295738));
#6573=CARTESIAN_POINT('Ctrl Pts',(1.15698088816274,2.36207894340676,-0.796050318316012));
#6574=CARTESIAN_POINT('Ctrl Pts',(1.37028192809006,2.5704122767401,-0.486038223674555));
#6575=CARTESIAN_POINT('Ctrl Pts',(1.39999999999998,2.77874561007344,-0.110909354270902));
#6576=CARTESIAN_POINT('Ctrl Pts',(1.42971807190994,2.98707894340678,0.264219515132648));
#6577=CARTESIAN_POINT('Ctrl Pts',(1.26789024243366,3.19541227674007,0.60394968168399));
#6578=CARTESIAN_POINT('Ctrl Pts',(1.10606241295741,3.40374561007344,0.943679848235385));
#6579=CARTESIAN_POINT('Ctrl Pts',(0.796050318315931,3.61207894340678,1.15698088816276));
#6580=CARTESIAN_POINT('Ctrl Pts',(0.486038223674496,3.82041227674011,1.37028192808997));
#6581=CARTESIAN_POINT('Ctrl Pts',(0.110909354270899,4.02874561007344,1.4));
#6582=CARTESIAN_POINT('Ctrl Pts',(-0.264219515132648,4.23707894340677,1.42971807190986));
#6583=CARTESIAN_POINT('Ctrl Pts',(-0.603949681684091,4.44541227674011,1.2678902424336));
#6584=CARTESIAN_POINT('Ctrl Pts',(-0.943679848235468,4.65374561007345,1.1060624129573));
#6585=CARTESIAN_POINT('Ctrl Pts',(-1.15698088816278,4.86207894340679,0.796050318315845));
#6586=CARTESIAN_POINT('Ctrl Pts',(-1.37028192809003,5.07041227674011,0.486038223674474));
#6587=CARTESIAN_POINT('Ctrl Pts',(-1.40000000000002,5.27874561007345,0.110909354270819));
#6588=CARTESIAN_POINT('Ctrl Pts',(-1.42971807190992,5.4870789434068,-0.264219515132837));
#6589=CARTESIAN_POINT('Ctrl Pts',(-1.26789024243366,5.69541227674011,-0.603949681684078));
#6590=CARTESIAN_POINT('Ctrl Pts',(-1.10606241295738,5.90374561007345,-0.943679848235563));
#6591=CARTESIAN_POINT('Ctrl Pts',(-0.79605031831595,6.11207894340678,-1.15698088816284));
#6592=CARTESIAN_POINT('Ctrl Pts',(-0.486038223674474,6.32041227674012,-1.37028192809014));
#6593=CARTESIAN_POINT('Ctrl Pts',(-0.110909354270923,6.52874561007347,-1.40000000000009));
#6594=CARTESIAN_POINT('Ctrl Pts',(0.264219515132672,6.7370789434068,-1.42971807191003));
#6595=CARTESIAN_POINT('Ctrl Pts',(0.60394968168407,6.94541227674011,-1.26789024243367));
#6596=CARTESIAN_POINT('Ctrl Pts',(0.943679848235474,7.15374561007344,-1.10606241295738));
#6597=CARTESIAN_POINT('Ctrl Pts',(1.15698088816276,7.36207894340676,-0.796050318316012));
#6598=CARTESIAN_POINT('Ctrl Pts',(1.37028192809008,7.57041227674013,-0.486038223674566));
#6599=CARTESIAN_POINT('Ctrl Pts',(1.4,7.77874561007344,-0.110909354270902));
#6600=CARTESIAN_POINT('Ctrl Pts',(1.42971807190995,7.98707894340678,0.264219515132605));
#6601=CARTESIAN_POINT('Ctrl Pts',(1.26789024243366,8.19541227674011,0.603949681683985));
#6602=CARTESIAN_POINT('Ctrl Pts',(1.10606241295739,8.40374561007346,0.943679848235385));
#6603=CARTESIAN_POINT('Ctrl Pts',(0.796050318315911,8.6120789434068,1.15698088816276));
#6604=CARTESIAN_POINT('Ctrl Pts',(0.486038223674474,8.82041227674011,1.37028192809001));
#6605=CARTESIAN_POINT('Ctrl Pts',(0.110909354270881,9.02874561007344,1.4));
#6606=CARTESIAN_POINT('Ctrl Pts',(-0.264219515132648,9.23707894340678,1.42971807190988));
#6607=CARTESIAN_POINT('Ctrl Pts',(-0.603949681684091,9.44541227674012,1.26789024243366));
#6608=CARTESIAN_POINT('Ctrl Pts',(-0.943679848235471,9.65374561007344,1.1060624129573));
#6609=CARTESIAN_POINT('Ctrl Pts',(-1.15698088816276,9.86207894340679,0.796050318315845));
#6610=CARTESIAN_POINT('Ctrl Pts',(-1.37028192809006,10.0704122767401,0.486038223674393));
#6611=CARTESIAN_POINT('Ctrl Pts',(-1.40000000000002,10.2787456100734,0.110909354270819));
#6612=CARTESIAN_POINT('Ctrl Pts',(-1.42971807190993,10.4870789434068,-0.264219515132756));
#6613=CARTESIAN_POINT('Ctrl Pts',(-1.26789024243369,10.6954122767401,-0.60394968168412));
#6614=CARTESIAN_POINT('Ctrl Pts',(-1.10606241295736,10.9037456100735,-0.94367984823553));
#6615=CARTESIAN_POINT('Ctrl Pts',(-0.79605031831595,11.1120789434068,-1.15698088816285));
#6616=CARTESIAN_POINT('Ctrl Pts',(-0.486038223674453,11.3204122767401,-1.37028192809014));
#6617=CARTESIAN_POINT('Ctrl Pts',(-0.110909354270923,11.5287456100735,-1.40000000000009));
#6618=CARTESIAN_POINT('Ctrl Pts',(0.264219515132691,11.7370789434068,-1.42971807191005));
#6619=CARTESIAN_POINT('Ctrl Pts',(0.60394968168405,11.9454122767401,-1.26789024243367));
#6620=CARTESIAN_POINT('Ctrl Pts',(0.943679848235492,12.1537456100735,-1.10606241295747));
#6621=CARTESIAN_POINT('Ctrl Pts',(1.15698088816276,12.3620789434068,-0.796050318316012));
#6622=CARTESIAN_POINT('Ctrl Pts',(1.37028192809006,12.5704122767401,-0.48603822367456));
#6623=CARTESIAN_POINT('Ctrl Pts',(1.4,12.7787456100735,-0.110909354270902));
#6624=CARTESIAN_POINT('Ctrl Pts',(1.42971807190997,12.9870789434068,0.264219515132578));
#6625=CARTESIAN_POINT('Ctrl Pts',(1.26789024243366,13.1954122767402,0.603949681683979));
#6626=CARTESIAN_POINT('Ctrl Pts',(1.10606241295738,13.4037456100734,0.943679848235428));
#6627=CARTESIAN_POINT('Ctrl Pts',(0.796050318315911,13.6120789434068,1.15698088816276));
#6628=CARTESIAN_POINT('Ctrl Pts',(0.486038223674477,13.8204122767401,1.37028192809001));
#6629=CARTESIAN_POINT('Ctrl Pts',(0.110909354270902,14.0287456100735,1.4));
#6630=CARTESIAN_POINT('Ctrl Pts',(-0.264219515132648,14.2370789434068,1.42971807190986));
#6631=CARTESIAN_POINT('Ctrl Pts',(-0.603949681684091,14.4454122767401,1.26789024243366));
#6632=CARTESIAN_POINT('Ctrl Pts',(-0.943679848235471,14.6537456100735,1.10606241295732));
#6633=CARTESIAN_POINT('Ctrl Pts',(-1.15698088816278,14.8620789434068,0.796050318315845));
#6634=CARTESIAN_POINT('Ctrl Pts',(-1.37028192809005,15.0704122767401,0.48603822367442));
#6635=CARTESIAN_POINT('Ctrl Pts',(-1.4,15.2787456100735,0.110909354270819));
#6636=CARTESIAN_POINT('Ctrl Pts',(-1.42971807190992,15.4870789434068,-0.264219515132718));
#6637=CARTESIAN_POINT('Ctrl Pts',(-1.26789024243366,15.6954122767401,-0.603949681684167));
#6638=CARTESIAN_POINT('Ctrl Pts',(-1.10606241295736,15.9037456100735,-0.943679848235573));
#6639=CARTESIAN_POINT('Ctrl Pts',(-0.796050318315929,16.1120789434068,-1.15698088816286));
#6640=CARTESIAN_POINT('Ctrl Pts',(-0.486038223674453,16.3204122767402,-1.37028192809016));
#6641=CARTESIAN_POINT('Ctrl Pts',(-0.110909354270902,16.5287456100735,-1.40000000000009));
#6642=CARTESIAN_POINT('Ctrl Pts',(0.264219515132672,16.7370789434068,-1.42971807191007));
#6643=CARTESIAN_POINT('Ctrl Pts',(0.60394968168407,16.9454122767402,-1.26789024243367));
#6644=CARTESIAN_POINT('Ctrl Pts',(0.943679848235471,17.1537456100735,-1.10606241295741));
#6645=CARTESIAN_POINT('Ctrl Pts',(1.15698088816274,17.3620789434068,-0.796050318316007));
#6646=CARTESIAN_POINT('Ctrl Pts',(1.37028192809005,17.5704122767402,-0.486038223674528));
#6647=CARTESIAN_POINT('Ctrl Pts',(1.39999999999998,17.7787456100735,-0.110909354270907));
#6648=CARTESIAN_POINT('Ctrl Pts',(1.42971807190994,17.9870789434068,0.2642195151326));
#6649=CARTESIAN_POINT('Ctrl Pts',(1.26789024243364,18.1954122767402,0.603949681683979));
#6650=CARTESIAN_POINT('Ctrl Pts',(1.10606241295739,18.4037456100735,0.943679848235406));
#6651=CARTESIAN_POINT('Ctrl Pts',(0.796050318315929,18.6120789434068,1.15698088816276));
#6652=CARTESIAN_POINT('Ctrl Pts',(0.486038223674496,18.8204122767402,1.37028192808999));
#6653=CARTESIAN_POINT('Ctrl Pts',(0.110909354270902,19.0287456100735,1.39999999999996));
#6654=CARTESIAN_POINT('Ctrl Pts',(-0.26421951513267,19.2370789434068,1.42971807190988));
#6655=CARTESIAN_POINT('Ctrl Pts',(-0.60394968168407,19.4454122767402,1.26789024243363));
#6656=CARTESIAN_POINT('Ctrl Pts',(-0.943679848235452,19.6537456100735,1.1060624129573));
#6657=CARTESIAN_POINT('Ctrl Pts',(-1.15698088816278,19.8620789434068,0.796050318315845));
#6658=CARTESIAN_POINT('Ctrl Pts',(-1.37028192809005,20.0704122767402,0.486038223674393));
#6659=CARTESIAN_POINT('Ctrl Pts',(-1.4,20.2787456100735,0.110909354270813));
#6660=CARTESIAN_POINT('Ctrl Pts',(-1.42971807190994,20.4870789434068,-0.26421951513274));
#6661=CARTESIAN_POINT('Ctrl Pts',(-1.26789024243366,20.6954122767402,-0.603949681684167));
#6662=CARTESIAN_POINT('Ctrl Pts',(-1.10606241295736,20.9037456100735,-0.943679848235573));
#6663=CARTESIAN_POINT('Ctrl Pts',(-0.79605031831595,21.1120789434068,-1.15698088816285));
#6664=CARTESIAN_POINT('Ctrl Pts',(-0.486038223674453,21.3204122767402,-1.37028192809015));
#6665=CARTESIAN_POINT('Ctrl Pts',(-0.110909354270923,21.5287456100735,-1.4000000000001));
#6666=CARTESIAN_POINT('Ctrl Pts',(0.264219515132691,21.7370789434068,-1.42971807191004));
#6667=CARTESIAN_POINT('Ctrl Pts',(0.60394968168407,21.9454122767402,-1.26789024243367));
#6668=CARTESIAN_POINT('Ctrl Pts',(0.943679848235474,22.1537456100735,-1.10606241295747));
#6669=CARTESIAN_POINT('Ctrl Pts',(1.15698088816276,22.3620789434068,-0.796050318316001));
#6670=CARTESIAN_POINT('Ctrl Pts',(1.37028192809006,22.5704122767402,-0.486038223674555));
#6671=CARTESIAN_POINT('Ctrl Pts',(1.4,22.7787456100735,-0.110909354270928));
#6672=CARTESIAN_POINT('Ctrl Pts',(1.42971807190997,22.9870789434068,0.264219515132573));
#6673=CARTESIAN_POINT('Ctrl Pts',(1.26789024243366,23.1954122767402,0.603949681684057));
#6674=CARTESIAN_POINT('Ctrl Pts',(1.10606241295738,23.4037456100735,0.943679848235433));
#6675=CARTESIAN_POINT('Ctrl Pts',(0.796050318315926,23.6120789434068,1.15698088816273));
#6676=CARTESIAN_POINT('Ctrl Pts',(0.486038223674474,23.8204122767402,1.37028192809002));
#6677=CARTESIAN_POINT('Ctrl Pts',(0.110909354270881,24.0287456100735,1.39999999999998));
#6678=CARTESIAN_POINT('Ctrl Pts',(-0.264219515132651,24.2370789434069,1.42971807190985));
#6679=CARTESIAN_POINT('Ctrl Pts',(-0.603949681684091,24.4454122767401,1.2678902424336));
#6680=CARTESIAN_POINT('Ctrl Pts',(-0.943679848235471,24.6537456100735,1.10606241295733));
#6681=CARTESIAN_POINT('Ctrl Pts',(-1.15698088816276,24.8620789434068,0.796050318315887));
#6682=CARTESIAN_POINT('Ctrl Pts',(-1.37028192809005,25.0704122767401,0.486038223674404));
#6683=CARTESIAN_POINT('Ctrl Pts',(-1.4,25.2787456100735,0.110909354270813));
#6684=CARTESIAN_POINT('Ctrl Pts',(-1.42971807190994,25.4870789434068,-0.264219515132734));
#6685=CARTESIAN_POINT('Ctrl Pts',(-1.26789024243369,25.6954122767402,-0.603949681684162));
#6686=CARTESIAN_POINT('Ctrl Pts',(-1.10606241295738,25.9037456100735,-0.943679848235541));
#6687=CARTESIAN_POINT('Ctrl Pts',(-0.79605031831595,26.1120789434068,-1.15698088816286));
#6688=CARTESIAN_POINT('Ctrl Pts',(-0.486038223674453,26.3204122767402,-1.37028192809015));
#6689=CARTESIAN_POINT('Ctrl Pts',(-0.110909354270923,26.5287456100735,-1.4000000000001));
#6690=CARTESIAN_POINT('Ctrl Pts',(0.264219515132694,26.7370789434069,-1.42971807191004));
#6691=CARTESIAN_POINT('Ctrl Pts',(0.60394968168405,26.9454122767402,-1.26789024243367));
#6692=CARTESIAN_POINT('Ctrl Pts',(0.943679848235492,27.1537456100735,-1.10606241295747));
#6693=CARTESIAN_POINT('Ctrl Pts',(1.15698088816274,27.3620789434069,-0.796050318316001));
#6694=CARTESIAN_POINT('Ctrl Pts',(1.37028192809008,27.5704122767402,-0.486038223674528));
#6695=CARTESIAN_POINT('Ctrl Pts',(1.39999999999998,27.7787456100735,-0.110909354270917));
#6696=CARTESIAN_POINT('Ctrl Pts',(1.42971807190997,27.9870789434068,0.264219515132594));
#6697=CARTESIAN_POINT('Ctrl Pts',(1.26789024243366,28.1954122767402,0.603949681684047));
#6698=CARTESIAN_POINT('Ctrl Pts',(1.10606241295738,28.4037456100735,0.943679848235406));
#6699=CARTESIAN_POINT('Ctrl Pts',(0.796050318315908,28.6120789434068,1.15698088816274));
#6700=CARTESIAN_POINT('Ctrl Pts',(0.486038223674496,28.8204122767402,1.37028192809));
#6701=CARTESIAN_POINT('Ctrl Pts',(0.110909354270902,29.0287456100735,1.39999999999997));
#6702=CARTESIAN_POINT('Ctrl Pts',(-0.26421951513267,29.2370789434068,1.42971807190989));
#6703=CARTESIAN_POINT('Ctrl Pts',(-0.603949681684091,29.4454122767402,1.26789024243359));
#6704=CARTESIAN_POINT('Ctrl Pts',(-0.943679848235452,29.6537456100735,1.10606241295731));
#6705=CARTESIAN_POINT('Ctrl Pts',(-1.15698088816278,29.8620789434069,0.796050318315892));
#6706=CARTESIAN_POINT('Ctrl Pts',(-1.37028192809005,30.0704122767402,0.486038223674393));
#6707=CARTESIAN_POINT('Ctrl Pts',(-1.4,30.2787456100735,0.11090935427086));
#6708=CARTESIAN_POINT('Ctrl Pts',(-1.42971807190994,30.4870789434069,-0.26421951513274));
#6709=CARTESIAN_POINT('Ctrl Pts',(-1.26789024243366,30.6954122767402,-0.603949681684162));
#6710=CARTESIAN_POINT('Ctrl Pts',(-1.10606241295736,30.9037456100735,-0.943679848235563));
#6711=CARTESIAN_POINT('Ctrl Pts',(-0.79605031831595,31.1120789434068,-1.15698088816285));
#6712=CARTESIAN_POINT('Ctrl Pts',(-0.486038223674471,31.3204122767402,-1.37028192809016));
#6713=CARTESIAN_POINT('Ctrl Pts',(-0.110909354270923,31.5287456100735,-1.4000000000001));
#6714=CARTESIAN_POINT('Ctrl Pts',(0.264219515132691,31.7370789434069,-1.42971807191));
#6715=CARTESIAN_POINT('Ctrl Pts',(0.60394968168407,31.9454122767402,-1.26789024243368));
#6716=CARTESIAN_POINT('Ctrl Pts',(0.943679848235474,32.1537456100735,-1.10606241295744));
#6717=CARTESIAN_POINT('Ctrl Pts',(1.15698088816274,32.3620789434069,-0.796050318315981));
#6718=CARTESIAN_POINT('Ctrl Pts',(1.37028192809005,32.5704122767402,-0.48603822367455));
#6719=CARTESIAN_POINT('Ctrl Pts',(1.4,32.7787456100735,-0.110909354270917));
#6720=CARTESIAN_POINT('Ctrl Pts',(1.42971807190994,32.9870789434069,0.264219515132578));
#6721=CARTESIAN_POINT('Ctrl Pts',(1.26789024243364,33.1954122767402,0.603949681684047));
#6722=CARTESIAN_POINT('Ctrl Pts',(1.10606241295741,33.4037456100735,0.943679848235428));
#6723=CARTESIAN_POINT('Ctrl Pts',(0.796050318315929,33.6120789434069,1.15698088816274));
#6724=CARTESIAN_POINT('Ctrl Pts',(0.486038223674496,33.8204122767402,1.37028192809002));
#6725=CARTESIAN_POINT('Ctrl Pts',(0.110909354270881,34.0287456100735,1.39999999999998));
#6726=CARTESIAN_POINT('Ctrl Pts',(-0.26421951513267,34.2370789434069,1.42971807190985));
#6727=CARTESIAN_POINT('Ctrl Pts',(-0.603949681684091,34.4454122767402,1.26789024243359));
#6728=CARTESIAN_POINT('Ctrl Pts',(-0.943679848235449,34.6537456100735,1.10606241295733));
#6729=CARTESIAN_POINT('Ctrl Pts',(-1.15698088816278,34.8620789434069,0.796050318315903));
#6730=CARTESIAN_POINT('Ctrl Pts',(-1.37028192809003,35.0704122767402,0.486038223674404));
#6731=CARTESIAN_POINT('Ctrl Pts',(-1.4,35.2787456100735,0.11090935427086));
#6732=CARTESIAN_POINT('Ctrl Pts',(-1.42971807190994,35.4870789434069,-0.264219515132756));
#6733=CARTESIAN_POINT('Ctrl Pts',(-1.26789024243369,35.6954122767402,-0.603949681684089));
#6734=CARTESIAN_POINT('Ctrl Pts',(-1.10606241295738,35.9037456100736,-0.943679848235563));
#6735=CARTESIAN_POINT('Ctrl Pts',(-0.79605031831595,36.1120789434069,-1.15698088816278));
#6736=CARTESIAN_POINT('Ctrl Pts',(-0.486038223674474,36.3204122767402,-1.37028192809014));
#6737=CARTESIAN_POINT('Ctrl Pts',(-0.11090935427092,36.5287456100735,-1.40000000000009));
#6738=CARTESIAN_POINT('Ctrl Pts',(0.264219515132672,36.7370789434069,-1.42971807191003));
#6739=CARTESIAN_POINT('Ctrl Pts',(0.60394968168405,36.9454122767402,-1.2678902424337));
#6740=CARTESIAN_POINT('Ctrl Pts',(0.943679848235492,37.1537456100735,-1.10606241295747));
#6741=CARTESIAN_POINT('Ctrl Pts',(1.15698088816274,37.3620789434068,-0.796050318315981));
#6742=CARTESIAN_POINT('Ctrl Pts',(1.37028192809008,37.5704122767402,-0.486038223674555));
#6743=CARTESIAN_POINT('Ctrl Pts',(1.4,37.7787456100735,-0.110909354270923));
#6744=CARTESIAN_POINT('Ctrl Pts',(1.42971807190994,37.9870789434069,0.264219515132605));
#6745=CARTESIAN_POINT('Ctrl Pts',(1.26789024243366,38.1954122767402,0.603949681684011));
#6746=CARTESIAN_POINT('Ctrl Pts',(1.10606241295738,38.4037456100735,0.943679848235417));
#6747=CARTESIAN_POINT('Ctrl Pts',(0.796050318315929,38.6120789434069,1.15698088816273));
#6748=CARTESIAN_POINT('Ctrl Pts',(0.486038223674474,38.8204122767402,1.37028192808999));
#6749=CARTESIAN_POINT('Ctrl Pts',(0.110909354270881,39.0287456100735,1.39999999999998));
#6750=CARTESIAN_POINT('Ctrl Pts',(-0.264219515132648,39.2370789434069,1.42971807190988));
#6751=CARTESIAN_POINT('Ctrl Pts',(-0.603949681684073,39.4454122767402,1.26789024243359));
#6752=CARTESIAN_POINT('Ctrl Pts',(-0.943679848235474,39.6537456100736,1.10606241295731));
#6753=CARTESIAN_POINT('Ctrl Pts',(-1.15698088816278,39.8620789434069,0.796050318315897));
#6754=CARTESIAN_POINT('Ctrl Pts',(-1.37028192809005,40.0704122767402,0.486038223674399));
#6755=CARTESIAN_POINT('Ctrl Pts',(-1.4,40.2787456100735,0.11090935427086));
#6756=CARTESIAN_POINT('Ctrl Pts',(-1.4,-0.278745610073483,-0.110909354270949));
#6757=CARTESIAN_POINT('Ctrl Pts',(-1.37028192809006,-0.0704122767401418,
-0.486038223674447));
#6758=CARTESIAN_POINT('Ctrl Pts',(-1.1569808881628,0.137921056593191,-0.796050318316017));
#6759=CARTESIAN_POINT('Ctrl Pts',(-0.943679848235495,0.346254389926559,
-1.10606241295736));
#6760=CARTESIAN_POINT('Ctrl Pts',(-0.60394968168412,0.554587723259871,-1.26789024243366));
#6761=CARTESIAN_POINT('Ctrl Pts',(-0.264219515132702,0.762921056593206,
-1.42971807191002));
#6762=CARTESIAN_POINT('Ctrl Pts',(0.11090935427085,0.971254389926519,-1.39999999999999));
#6763=CARTESIAN_POINT('Ctrl Pts',(0.486038223674463,1.17958772325989,-1.37028192809015));
#6764=CARTESIAN_POINT('Ctrl Pts',(0.7960503183159,1.3879210565932,-1.15698088816281));
#6765=CARTESIAN_POINT('Ctrl Pts',(1.10606241295738,1.59625438992658,-0.943679848235584));
#6766=CARTESIAN_POINT('Ctrl Pts',(1.26789024243364,1.80458772325987,-0.603949681684177));
#6767=CARTESIAN_POINT('Ctrl Pts',(1.42971807190996,2.01292105659321,-0.264219515132788));
#6768=CARTESIAN_POINT('Ctrl Pts',(1.39999999999998,2.22125438992654,0.110909354270787));
#6769=CARTESIAN_POINT('Ctrl Pts',(1.37028192809009,2.42958772325987,0.486038223674361));
#6770=CARTESIAN_POINT('Ctrl Pts',(1.15698088816276,2.63792105659322,0.796050318315897));
#6771=CARTESIAN_POINT('Ctrl Pts',(0.943679848235517,2.84625438992656,1.10606241295735));
#6772=CARTESIAN_POINT('Ctrl Pts',(0.603949681684099,3.05458772325989,1.26789024243365));
#6773=CARTESIAN_POINT('Ctrl Pts',(0.264219515132705,3.26292105659324,1.42971807190985));
#6774=CARTESIAN_POINT('Ctrl Pts',(-0.110909354270889,3.47125438992654,1.39999999999992));
#6775=CARTESIAN_POINT('Ctrl Pts',(-0.48603822367442,3.67958772325988,1.37028192808998));
#6776=CARTESIAN_POINT('Ctrl Pts',(-0.796050318315921,3.8879210565932,1.15698088816272));
#6777=CARTESIAN_POINT('Ctrl Pts',(-1.10606241295734,4.09625438992655,0.943679848235406));
#6778=CARTESIAN_POINT('Ctrl Pts',(-1.26789024243365,4.30458772325989,0.603949681684094));
#6779=CARTESIAN_POINT('Ctrl Pts',(-1.42971807190994,4.51292105659323,0.2642195151326));
#6780=CARTESIAN_POINT('Ctrl Pts',(-1.4,4.72125438992655,-0.110909354270949));
#6781=CARTESIAN_POINT('Ctrl Pts',(-1.37028192809004,4.9295877232599,-0.486038223674442));
#6782=CARTESIAN_POINT('Ctrl Pts',(-1.15698088816278,5.13792105659321,-0.796050318315991));
#6783=CARTESIAN_POINT('Ctrl Pts',(-0.943679848235495,5.34625438992658,-1.10606241295745));
#6784=CARTESIAN_POINT('Ctrl Pts',(-0.603949681684099,5.55458772325993,-1.26789024243366));
#6785=CARTESIAN_POINT('Ctrl Pts',(-0.264219515132702,5.76292105659326,-1.42971807190998));
#6786=CARTESIAN_POINT('Ctrl Pts',(0.110909354270868,5.97125438992656,-1.40000000000003));
#6787=CARTESIAN_POINT('Ctrl Pts',(0.486038223674442,6.17958772325989,-1.37028192809015));
#6788=CARTESIAN_POINT('Ctrl Pts',(0.796050318315879,6.38792105659323,-1.15698088816278));
#6789=CARTESIAN_POINT('Ctrl Pts',(1.10606241295736,6.59625438992658,-0.943679848235606));
#6790=CARTESIAN_POINT('Ctrl Pts',(1.26789024243365,6.80458772325986,-0.603949681684177));
#6791=CARTESIAN_POINT('Ctrl Pts',(1.42971807190994,7.01292105659325,-0.264219515132794));
#6792=CARTESIAN_POINT('Ctrl Pts',(1.4,7.22125438992654,0.110909354270824));
#6793=CARTESIAN_POINT('Ctrl Pts',(1.37028192809007,7.42958772325991,0.486038223674361));
#6794=CARTESIAN_POINT('Ctrl Pts',(1.15698088816276,7.63792105659323,0.796050318315897));
#6795=CARTESIAN_POINT('Ctrl Pts',(0.943679848235498,7.84625438992655,1.10606241295728));
#6796=CARTESIAN_POINT('Ctrl Pts',(0.603949681684078,8.05458772325989,1.26789024243365));
#6797=CARTESIAN_POINT('Ctrl Pts',(0.264219515132724,8.26292105659323,1.42971807190989));
#6798=CARTESIAN_POINT('Ctrl Pts',(-0.110909354270889,8.47125438992655,1.39999999999992));
#6799=CARTESIAN_POINT('Ctrl Pts',(-0.486038223674439,8.67958772325992,1.37028192808998));
#6800=CARTESIAN_POINT('Ctrl Pts',(-0.796050318315921,8.88792105659323,1.15698088816273));
#6801=CARTESIAN_POINT('Ctrl Pts',(-1.10606241295736,9.09625438992657,0.94367984823539));
#6802=CARTESIAN_POINT('Ctrl Pts',(-1.26789024243365,9.3045877232599,0.603949681684094));
#6803=CARTESIAN_POINT('Ctrl Pts',(-1.42971807190994,9.51292105659322,0.264219515132616));
#6804=CARTESIAN_POINT('Ctrl Pts',(-1.4,9.72125438992658,-0.110909354270954));
#6805=CARTESIAN_POINT('Ctrl Pts',(-1.37028192809006,9.92958772325988,-0.486038223674523));
#6806=CARTESIAN_POINT('Ctrl Pts',(-1.1569808881628,10.1379210565933,-0.796050318315991));
#6807=CARTESIAN_POINT('Ctrl Pts',(-0.943679848235474,10.3462543899266,-1.10606241295745));
#6808=CARTESIAN_POINT('Ctrl Pts',(-0.60394968168412,10.5545877232599,-1.26789024243366));
#6809=CARTESIAN_POINT('Ctrl Pts',(-0.264219515132683,10.7629210565932,-1.42971807191006));
#6810=CARTESIAN_POINT('Ctrl Pts',(0.110909354270847,10.9712543899266,-1.40000000000007));
#6811=CARTESIAN_POINT('Ctrl Pts',(0.486038223674463,11.1795877232599,-1.37028192809018));
#6812=CARTESIAN_POINT('Ctrl Pts',(0.7960503183159,11.3879210565933,-1.15698088816279));
#6813=CARTESIAN_POINT('Ctrl Pts',(1.10606241295736,11.5962543899266,-0.943679848235595));
#6814=CARTESIAN_POINT('Ctrl Pts',(1.26789024243365,11.8045877232599,-0.603949681684188));
#6815=CARTESIAN_POINT('Ctrl Pts',(1.42971807190994,12.0129210565932,-0.264219515132707));
#6816=CARTESIAN_POINT('Ctrl Pts',(1.4,12.2212543899266,0.110909354270855));
#6817=CARTESIAN_POINT('Ctrl Pts',(1.37028192809006,12.4295877232599,0.486038223674382));
#6818=CARTESIAN_POINT('Ctrl Pts',(1.15698088816276,12.6379210565932,0.796050318315897));
#6819=CARTESIAN_POINT('Ctrl Pts',(0.943679848235517,12.8462543899266,1.10606241295731));
#6820=CARTESIAN_POINT('Ctrl Pts',(0.603949681684099,13.0545877232599,1.26789024243365));
#6821=CARTESIAN_POINT('Ctrl Pts',(0.264219515132705,13.2629210565933,1.42971807190989));
#6822=CARTESIAN_POINT('Ctrl Pts',(-0.110909354270889,13.4712543899266,1.39999999999992));
#6823=CARTESIAN_POINT('Ctrl Pts',(-0.48603822367442,13.6795877232599,1.37028192808998));
#6824=CARTESIAN_POINT('Ctrl Pts',(-0.7960503183159,13.8879210565933,1.15698088816275));
#6825=CARTESIAN_POINT('Ctrl Pts',(-1.10606241295736,14.0962543899266,0.943679848235428));
#6826=CARTESIAN_POINT('Ctrl Pts',(-1.26789024243365,14.3045877232599,0.603949681684078));
#6827=CARTESIAN_POINT('Ctrl Pts',(-1.42971807190992,14.5129210565933,0.264219515132632));
#6828=CARTESIAN_POINT('Ctrl Pts',(-1.40000000000002,14.7212543899266,-0.110909354270954));
#6829=CARTESIAN_POINT('Ctrl Pts',(-1.37028192809007,14.9295877232599,-0.486038223674463));
#6830=CARTESIAN_POINT('Ctrl Pts',(-1.15698088816278,15.1379210565933,-0.796050318315991));
#6831=CARTESIAN_POINT('Ctrl Pts',(-0.943679848235495,15.3462543899266,-1.10606241295744));
#6832=CARTESIAN_POINT('Ctrl Pts',(-0.60394968168412,15.55458772326,-1.26789024243366));
#6833=CARTESIAN_POINT('Ctrl Pts',(-0.264219515132702,15.7629210565933,-1.42971807191003));
#6834=CARTESIAN_POINT('Ctrl Pts',(0.110909354270868,15.9712543899266,-1.40000000000008));
#6835=CARTESIAN_POINT('Ctrl Pts',(0.486038223674463,16.1795877232599,-1.37028192809016));
#6836=CARTESIAN_POINT('Ctrl Pts',(0.796050318315879,16.3879210565933,-1.15698088816279));
#6837=CARTESIAN_POINT('Ctrl Pts',(1.10606241295736,16.5962543899266,-0.94367984823559));
#6838=CARTESIAN_POINT('Ctrl Pts',(1.26789024243365,16.8045877232599,-0.603949681684188));
#6839=CARTESIAN_POINT('Ctrl Pts',(1.42971807190996,17.0129210565933,-0.264219515132783));
#6840=CARTESIAN_POINT('Ctrl Pts',(1.39999999999998,17.2212543899266,0.11090935427085));
#6841=CARTESIAN_POINT('Ctrl Pts',(1.37028192809007,17.4295877232599,0.486038223674382));
#6842=CARTESIAN_POINT('Ctrl Pts',(1.15698088816276,17.6379210565933,0.796050318315892));
#6843=CARTESIAN_POINT('Ctrl Pts',(0.943679848235517,17.8462543899266,1.10606241295728));
#6844=CARTESIAN_POINT('Ctrl Pts',(0.603949681684099,18.0545877232599,1.26789024243363));
#6845=CARTESIAN_POINT('Ctrl Pts',(0.264219515132724,18.2629210565933,1.42971807190987));
#6846=CARTESIAN_POINT('Ctrl Pts',(-0.110909354270889,18.4712543899266,1.39999999999997));
#6847=CARTESIAN_POINT('Ctrl Pts',(-0.48603822367442,18.6795877232599,1.37028192808996));
#6848=CARTESIAN_POINT('Ctrl Pts',(-0.796050318315921,18.8879210565933,1.15698088816276));
#6849=CARTESIAN_POINT('Ctrl Pts',(-1.10606241295736,19.0962543899266,0.943679848235417));
#6850=CARTESIAN_POINT('Ctrl Pts',(-1.26789024243365,19.3045877232599,0.603949681684037));
#6851=CARTESIAN_POINT('Ctrl Pts',(-1.42971807190994,19.5129210565933,0.264219515132616));
#6852=CARTESIAN_POINT('Ctrl Pts',(-1.4,19.7212543899266,-0.110909354270954));
#6853=CARTESIAN_POINT('Ctrl Pts',(-1.37028192809006,19.9295877232599,-0.486038223674496));
#6854=CARTESIAN_POINT('Ctrl Pts',(-1.1569808881628,20.1379210565933,-0.796050318315996));
#6855=CARTESIAN_POINT('Ctrl Pts',(-0.943679848235474,20.3462543899266,-1.10606241295739));
#6856=CARTESIAN_POINT('Ctrl Pts',(-0.603949681684099,20.5545877232599,-1.26789024243366));
#6857=CARTESIAN_POINT('Ctrl Pts',(-0.264219515132683,20.7629210565933,-1.42971807191002));
#6858=CARTESIAN_POINT('Ctrl Pts',(0.110909354270868,20.9712543899266,-1.40000000000009));
#6859=CARTESIAN_POINT('Ctrl Pts',(0.486038223674463,21.1795877232599,-1.37028192809016));
#6860=CARTESIAN_POINT('Ctrl Pts',(0.796050318315879,21.3879210565933,-1.15698088816278));
#6861=CARTESIAN_POINT('Ctrl Pts',(1.10606241295736,21.5962543899266,-0.943679848235579));
#6862=CARTESIAN_POINT('Ctrl Pts',(1.26789024243365,21.8045877232599,-0.603949681684177));
#6863=CARTESIAN_POINT('Ctrl Pts',(1.42971807190994,22.0129210565933,-0.264219515132783));
#6864=CARTESIAN_POINT('Ctrl Pts',(1.4,22.2212543899266,0.110909354270855));
#6865=CARTESIAN_POINT('Ctrl Pts',(1.37028192809006,22.42958772326,0.486038223674372));
#6866=CARTESIAN_POINT('Ctrl Pts',(1.15698088816276,22.6379210565933,0.796050318315892));
#6867=CARTESIAN_POINT('Ctrl Pts',(0.943679848235495,22.8462543899266,1.10606241295731));
#6868=CARTESIAN_POINT('Ctrl Pts',(0.603949681684078,23.0545877232599,1.26789024243363));
#6869=CARTESIAN_POINT('Ctrl Pts',(0.264219515132726,23.2629210565933,1.42971807190989));
#6870=CARTESIAN_POINT('Ctrl Pts',(-0.110909354270889,23.4712543899266,1.39999999999997));
#6871=CARTESIAN_POINT('Ctrl Pts',(-0.48603822367442,23.6795877232599,1.37028192808997));
#6872=CARTESIAN_POINT('Ctrl Pts',(-0.796050318315921,23.8879210565932,1.15698088816274));
#6873=CARTESIAN_POINT('Ctrl Pts',(-1.10606241295736,24.0962543899266,0.943679848235433));
#6874=CARTESIAN_POINT('Ctrl Pts',(-1.26789024243367,24.3045877232599,0.603949681684089));
#6875=CARTESIAN_POINT('Ctrl Pts',(-1.42971807190992,24.5129210565933,0.264219515132643));
#6876=CARTESIAN_POINT('Ctrl Pts',(-1.40000000000002,24.7212543899266,-0.110909354270923));
#6877=CARTESIAN_POINT('Ctrl Pts',(-1.37028192809004,24.9295877232599,-0.486038223674528));
#6878=CARTESIAN_POINT('Ctrl Pts',(-1.1569808881628,25.1379210565933,-0.796050318315996));
#6879=CARTESIAN_POINT('Ctrl Pts',(-0.943679848235474,25.3462543899266,-1.10606241295742));
#6880=CARTESIAN_POINT('Ctrl Pts',(-0.60394968168412,25.5545877232599,-1.26789024243365));
#6881=CARTESIAN_POINT('Ctrl Pts',(-0.264219515132702,25.7629210565933,-1.42971807191003));
#6882=CARTESIAN_POINT('Ctrl Pts',(0.110909354270847,25.9712543899266,-1.40000000000008));
#6883=CARTESIAN_POINT('Ctrl Pts',(0.486038223674463,26.17958772326,-1.37028192809014));
#6884=CARTESIAN_POINT('Ctrl Pts',(0.7960503183159,26.3879210565933,-1.15698088816279));
#6885=CARTESIAN_POINT('Ctrl Pts',(1.10606241295738,26.5962543899266,-0.943679848235541));
#6886=CARTESIAN_POINT('Ctrl Pts',(1.26789024243363,26.80458772326,-0.603949681684177));
#6887=CARTESIAN_POINT('Ctrl Pts',(1.42971807190996,27.0129210565933,-0.264219515132761));
#6888=CARTESIAN_POINT('Ctrl Pts',(1.4,27.2212543899266,0.110909354270855));
#6889=CARTESIAN_POINT('Ctrl Pts',(1.37028192809007,27.42958772326,0.486038223674393));
#6890=CARTESIAN_POINT('Ctrl Pts',(1.15698088816278,27.6379210565933,0.796050318315892));
#6891=CARTESIAN_POINT('Ctrl Pts',(0.943679848235495,27.8462543899266,1.10606241295729));
#6892=CARTESIAN_POINT('Ctrl Pts',(0.603949681684099,28.0545877232599,1.26789024243361));
#6893=CARTESIAN_POINT('Ctrl Pts',(0.264219515132724,28.2629210565933,1.42971807190986));
#6894=CARTESIAN_POINT('Ctrl Pts',(-0.110909354270889,28.4712543899266,1.39999999999997));
#6895=CARTESIAN_POINT('Ctrl Pts',(-0.48603822367442,28.67958772326,1.37028192808997));
#6896=CARTESIAN_POINT('Ctrl Pts',(-0.796050318315921,28.8879210565933,1.15698088816275));
#6897=CARTESIAN_POINT('Ctrl Pts',(-1.10606241295734,29.0962543899266,0.943679848235406));
#6898=CARTESIAN_POINT('Ctrl Pts',(-1.26789024243365,29.30458772326,0.603949681684083));
#6899=CARTESIAN_POINT('Ctrl Pts',(-1.42971807190992,29.5129210565933,0.264219515132621));
#6900=CARTESIAN_POINT('Ctrl Pts',(-1.40000000000002,29.7212543899266,-0.110909354270923));
#6901=CARTESIAN_POINT('Ctrl Pts',(-1.37028192809006,29.92958772326,-0.486038223674506));
#6902=CARTESIAN_POINT('Ctrl Pts',(-1.1569808881628,30.1379210565933,-0.796050318315996));
#6903=CARTESIAN_POINT('Ctrl Pts',(-0.943679848235495,30.3462543899266,-1.10606241295744));
#6904=CARTESIAN_POINT('Ctrl Pts',(-0.60394968168412,30.5545877232599,-1.26789024243366));
#6905=CARTESIAN_POINT('Ctrl Pts',(-0.264219515132702,30.7629210565933,-1.42971807191004));
#6906=CARTESIAN_POINT('Ctrl Pts',(0.110909354270868,30.9712543899266,-1.40000000000007));
#6907=CARTESIAN_POINT('Ctrl Pts',(0.486038223674439,31.17958772326,-1.37028192809015));
#6908=CARTESIAN_POINT('Ctrl Pts',(0.796050318315879,31.3879210565933,-1.15698088816279));
#6909=CARTESIAN_POINT('Ctrl Pts',(1.10606241295736,31.5962543899266,-0.943679848235557));
#6910=CARTESIAN_POINT('Ctrl Pts',(1.26789024243365,31.80458772326,-0.603949681684177));
#6911=CARTESIAN_POINT('Ctrl Pts',(1.42971807190996,32.0129210565933,-0.264219515132783));
#6912=CARTESIAN_POINT('Ctrl Pts',(1.39999999999998,32.2212543899266,0.11090935427085));
#6913=CARTESIAN_POINT('Ctrl Pts',(1.37028192809008,32.42958772326,0.486038223674377));
#6914=CARTESIAN_POINT('Ctrl Pts',(1.15698088816278,32.6379210565933,0.796050318315892));
#6915=CARTESIAN_POINT('Ctrl Pts',(0.943679848235498,32.8462543899267,1.1060624129573));
#6916=CARTESIAN_POINT('Ctrl Pts',(0.603949681684078,33.05458772326,1.26789024243359));
#6917=CARTESIAN_POINT('Ctrl Pts',(0.264219515132705,33.2629210565933,1.4297180719099));
#6918=CARTESIAN_POINT('Ctrl Pts',(-0.110909354270871,33.4712543899267,1.39999999999998));
#6919=CARTESIAN_POINT('Ctrl Pts',(-0.486038223674439,33.67958772326,1.37028192808999));
#6920=CARTESIAN_POINT('Ctrl Pts',(-0.796050318315921,33.8879210565933,1.15698088816275));
#6921=CARTESIAN_POINT('Ctrl Pts',(-1.10606241295736,34.0962543899266,0.943679848235417));
#6922=CARTESIAN_POINT('Ctrl Pts',(-1.26789024243367,34.30458772326,0.603949681684083));
#6923=CARTESIAN_POINT('Ctrl Pts',(-1.42971807190994,34.5129210565933,0.264219515132643));
#6924=CARTESIAN_POINT('Ctrl Pts',(-1.4,34.7212543899266,-0.110909354270923));
#6925=CARTESIAN_POINT('Ctrl Pts',(-1.37028192809004,34.92958772326,-0.486038223674517));
#6926=CARTESIAN_POINT('Ctrl Pts',(-1.1569808881628,35.1379210565933,-0.796050318315944));
#6927=CARTESIAN_POINT('Ctrl Pts',(-0.943679848235495,35.3462543899267,-1.10606241295742));
#6928=CARTESIAN_POINT('Ctrl Pts',(-0.60394968168412,35.55458772326,-1.26789024243366));
#6929=CARTESIAN_POINT('Ctrl Pts',(-0.26421951513268,35.7629210565933,-1.42971807191003));
#6930=CARTESIAN_POINT('Ctrl Pts',(0.110909354270847,35.9712543899266,-1.40000000000004));
#6931=CARTESIAN_POINT('Ctrl Pts',(0.486038223674442,36.17958772326,-1.37028192809012));
#6932=CARTESIAN_POINT('Ctrl Pts',(0.796050318315903,36.3879210565933,-1.15698088816279));
#6933=CARTESIAN_POINT('Ctrl Pts',(1.10606241295738,36.5962543899266,-0.943679848235568));
#6934=CARTESIAN_POINT('Ctrl Pts',(1.26789024243365,36.80458772326,-0.603949681684162));
#6935=CARTESIAN_POINT('Ctrl Pts',(1.42971807190994,37.0129210565933,-0.264219515132788));
#6936=CARTESIAN_POINT('Ctrl Pts',(1.4,37.2212543899267,0.110909354270845));
#6937=CARTESIAN_POINT('Ctrl Pts',(1.37028192809007,37.42958772326,0.486038223674372));
#6938=CARTESIAN_POINT('Ctrl Pts',(1.15698088816278,37.6379210565933,0.796050318315845));
#6939=CARTESIAN_POINT('Ctrl Pts',(0.943679848235495,37.8462543899266,1.1060624129573));
#6940=CARTESIAN_POINT('Ctrl Pts',(0.603949681684099,38.05458772326,1.26789024243359));
#6941=CARTESIAN_POINT('Ctrl Pts',(0.264219515132702,38.2629210565934,1.42971807190987));
#6942=CARTESIAN_POINT('Ctrl Pts',(-0.110909354270891,38.4712543899267,1.39999999999999));
#6943=CARTESIAN_POINT('Ctrl Pts',(-0.486038223674442,38.67958772326,1.37028192808997));
#6944=CARTESIAN_POINT('Ctrl Pts',(-0.796050318315942,38.8879210565933,1.15698088816275));
#6945=CARTESIAN_POINT('Ctrl Pts',(-1.10606241295734,39.0962543899267,0.943679848235401));
#6946=CARTESIAN_POINT('Ctrl Pts',(-1.26789024243367,39.30458772326,0.603949681684089));
#6947=CARTESIAN_POINT('Ctrl Pts',(-1.42971807190992,39.5129210565933,0.264219515132632));
#6948=CARTESIAN_POINT('Ctrl Pts',(-1.40000000000002,39.7212543899266,-0.110909354270923));
#6949=CARTESIAN_POINT('Ctrl Pts',(-2.,-0.27874561007344,-0.110909354270924));
#6950=CARTESIAN_POINT('Ctrl Pts',(-1.97028192809006,-0.0704122767402082,
-0.646807739133109));
#6951=CARTESIAN_POINT('Ctrl Pts',(-1.67659613043344,0.137921056593222,-1.0960503183159));
#6952=CARTESIAN_POINT('Ctrl Pts',(-1.38291033277682,0.346254389926512,-1.54529289749873));
#6953=CARTESIAN_POINT('Ctrl Pts',(-0.903949681684104,0.554587723259871,
-1.78750548470438));
#6954=CARTESIAN_POINT('Ctrl Pts',(-0.424989030591367,0.762921056593226,
-2.02971807190993));
#6955=CARTESIAN_POINT('Ctrl Pts',(0.110909354270878,0.971254389926561,-2.00000000000006));
#6956=CARTESIAN_POINT('Ctrl Pts',(0.646807739133123,1.17958772325984,-1.97028192809007));
#6957=CARTESIAN_POINT('Ctrl Pts',(1.09605031831591,1.38792105659322,-1.67659613043344));
#6958=CARTESIAN_POINT('Ctrl Pts',(1.54529289749868,1.59625438992652,-1.38291033277687));
#6959=CARTESIAN_POINT('Ctrl Pts',(1.78750548470428,1.80458772325989,-0.903949681684113));
#6960=CARTESIAN_POINT('Ctrl Pts',(2.02971807190996,2.01292105659317,-0.42498903059139));
#6961=CARTESIAN_POINT('Ctrl Pts',(2.,2.22125438992656,0.110909354270855));
#6962=CARTESIAN_POINT('Ctrl Pts',(1.97028192809007,2.42958772325984,0.646807739133102));
#6963=CARTESIAN_POINT('Ctrl Pts',(1.67659613043345,2.63792105659317,1.09605031831587));
#6964=CARTESIAN_POINT('Ctrl Pts',(1.38291033277682,2.8462543899265,1.54529289749866));
#6965=CARTESIAN_POINT('Ctrl Pts',(0.903949681684104,3.0545877232599,1.78750548470426));
#6966=CARTESIAN_POINT('Ctrl Pts',(0.424989030591383,3.26292105659317,2.02971807190993));
#6967=CARTESIAN_POINT('Ctrl Pts',(-0.11090935427085,3.47125438992654,1.99999999999995));
#6968=CARTESIAN_POINT('Ctrl Pts',(-0.646807739133109,3.67958772325983,1.97028192809007));
#6969=CARTESIAN_POINT('Ctrl Pts',(-1.0960503183159,3.88792105659323,1.67659613043343));
#6970=CARTESIAN_POINT('Ctrl Pts',(-1.54529289749868,4.09625438992648,1.38291033277681));
#6971=CARTESIAN_POINT('Ctrl Pts',(-1.78750548470431,4.30458772325989,0.903949681684051));
#6972=CARTESIAN_POINT('Ctrl Pts',(-2.02971807190994,4.51292105659318,0.424989030591333));
#6973=CARTESIAN_POINT('Ctrl Pts',(-2.,4.72125438992654,-0.110909354270966));
#6974=CARTESIAN_POINT('Ctrl Pts',(-1.97028192809006,4.92958772325984,-0.646807739133087));
#6975=CARTESIAN_POINT('Ctrl Pts',(-1.67659613043343,5.13792105659321,-1.09605031831595));
#6976=CARTESIAN_POINT('Ctrl Pts',(-1.38291033277682,5.34625438992653,-1.54529289749872));
#6977=CARTESIAN_POINT('Ctrl Pts',(-0.903949681684091,5.5545877232599,-1.78750548470436));
#6978=CARTESIAN_POINT('Ctrl Pts',(-0.424989030591382,5.76292105659322,-2.02971807190993));
#6979=CARTESIAN_POINT('Ctrl Pts',(0.110909354270865,5.97125438992659,-2.00000000000009));
#6980=CARTESIAN_POINT('Ctrl Pts',(0.64680773913311,6.17958772325983,-1.97028192809005));
#6981=CARTESIAN_POINT('Ctrl Pts',(1.0960503183159,6.38792105659326,-1.67659613043349));
#6982=CARTESIAN_POINT('Ctrl Pts',(1.54529289749868,6.5962543899265,-1.38291033277683));
#6983=CARTESIAN_POINT('Ctrl Pts',(1.7875054847043,6.80458772325989,-0.903949681684162));
#6984=CARTESIAN_POINT('Ctrl Pts',(2.02971807190991,7.01292105659322,-0.424989030591398));
#6985=CARTESIAN_POINT('Ctrl Pts',(2.,7.22125438992656,0.110909354270862));
#6986=CARTESIAN_POINT('Ctrl Pts',(1.97028192809006,7.42958772325989,0.646807739133109));
#6987=CARTESIAN_POINT('Ctrl Pts',(1.67659613043344,7.63792105659322,1.09605031831585));
#6988=CARTESIAN_POINT('Ctrl Pts',(1.38291033277683,7.84625438992656,1.54529289749869));
#6989=CARTESIAN_POINT('Ctrl Pts',(0.903949681684104,8.05458772325989,1.78750548470431));
#6990=CARTESIAN_POINT('Ctrl Pts',(0.424989030591398,8.26292105659318,2.02971807190991));
#6991=CARTESIAN_POINT('Ctrl Pts',(-0.110909354270878,8.47125438992655,1.99999999999995));
#6992=CARTESIAN_POINT('Ctrl Pts',(-0.646807739133123,8.67958772325983,1.97028192809004));
#6993=CARTESIAN_POINT('Ctrl Pts',(-1.0960503183159,8.88792105659324,1.67659613043339));
#6994=CARTESIAN_POINT('Ctrl Pts',(-1.54529289749868,9.0962543899265,1.38291033277682));
#6995=CARTESIAN_POINT('Ctrl Pts',(-1.78750548470431,9.3045877232599,0.903949681684085));
#6996=CARTESIAN_POINT('Ctrl Pts',(-2.02971807190993,9.51292105659317,0.424989030591355));
#6997=CARTESIAN_POINT('Ctrl Pts',(-2.,9.72125438992657,-0.110909354270924));
#6998=CARTESIAN_POINT('Ctrl Pts',(-1.97028192809007,9.92958772325983,-0.646807739133123));
#6999=CARTESIAN_POINT('Ctrl Pts',(-1.67659613043344,10.1379210565932,-1.09605031831599));
#7000=CARTESIAN_POINT('Ctrl Pts',(-1.38291033277681,10.3462543899265,-1.54529289749875));
#7001=CARTESIAN_POINT('Ctrl Pts',(-0.903949681684116,10.5545877232599,-1.78750548470438));
#7002=CARTESIAN_POINT('Ctrl Pts',(-0.424989030591382,10.7629210565932,-2.02971807190998));
#7003=CARTESIAN_POINT('Ctrl Pts',(0.110909354270878,10.9712543899266,-2.00000000000009));
#7004=CARTESIAN_POINT('Ctrl Pts',(0.646807739133123,11.1795877232599,-1.97028192809007));
#7005=CARTESIAN_POINT('Ctrl Pts',(1.09605031831591,11.3879210565932,-1.67659613043351));
#7006=CARTESIAN_POINT('Ctrl Pts',(1.54529289749868,11.5962543899265,-1.38291033277682));
#7007=CARTESIAN_POINT('Ctrl Pts',(1.78750548470431,11.8045877232599,-0.903949681684182));
#7008=CARTESIAN_POINT('Ctrl Pts',(2.02971807190993,12.0129210565932,-0.424989030591383));
#7009=CARTESIAN_POINT('Ctrl Pts',(2.,12.2212543899266,0.110909354270862));
#7010=CARTESIAN_POINT('Ctrl Pts',(1.97028192809007,12.4295877232599,0.646807739133051));
#7011=CARTESIAN_POINT('Ctrl Pts',(1.67659613043345,12.6379210565932,1.09605031831589));
#7012=CARTESIAN_POINT('Ctrl Pts',(1.38291033277683,12.8462543899266,1.54529289749867));
#7013=CARTESIAN_POINT('Ctrl Pts',(0.903949681684118,13.0545877232599,1.78750548470425));
#7014=CARTESIAN_POINT('Ctrl Pts',(0.424989030591382,13.2629210565932,2.02971807190993));
#7015=CARTESIAN_POINT('Ctrl Pts',(-0.110909354270864,13.4712543899266,1.99999999999997));
#7016=CARTESIAN_POINT('Ctrl Pts',(-0.646807739133109,13.6795877232599,1.97028192809006));
#7017=CARTESIAN_POINT('Ctrl Pts',(-1.0960503183159,13.8879210565932,1.67659613043339));
#7018=CARTESIAN_POINT('Ctrl Pts',(-1.54529289749868,14.0962543899266,1.38291033277682));
#7019=CARTESIAN_POINT('Ctrl Pts',(-1.7875054847043,14.3045877232599,0.903949681684092));
#7020=CARTESIAN_POINT('Ctrl Pts',(-2.02971807190993,14.5129210565932,0.424989030591326));
#7021=CARTESIAN_POINT('Ctrl Pts',(-2.,14.7212543899266,-0.110909354270938));
#7022=CARTESIAN_POINT('Ctrl Pts',(-1.97028192809006,14.9295877232599,-0.646807739133109));
#7023=CARTESIAN_POINT('Ctrl Pts',(-1.67659613043344,15.1379210565933,-1.09605031831595));
#7024=CARTESIAN_POINT('Ctrl Pts',(-1.38291033277683,15.3462543899265,-1.54529289749874));
#7025=CARTESIAN_POINT('Ctrl Pts',(-0.903949681684104,15.5545877232599,-1.78750548470439));
#7026=CARTESIAN_POINT('Ctrl Pts',(-0.424989030591382,15.7629210565932,-2.02971807190993));
#7027=CARTESIAN_POINT('Ctrl Pts',(0.110909354270852,15.9712543899266,-2.00000000000006));
#7028=CARTESIAN_POINT('Ctrl Pts',(0.646807739133109,16.1795877232599,-1.97028192809006));
#7029=CARTESIAN_POINT('Ctrl Pts',(1.0960503183159,16.3879210565933,-1.67659613043349));
#7030=CARTESIAN_POINT('Ctrl Pts',(1.5452928974987,16.5962543899265,-1.38291033277688));
#7031=CARTESIAN_POINT('Ctrl Pts',(1.78750548470431,16.8045877232599,-0.903949681684148));
#7032=CARTESIAN_POINT('Ctrl Pts',(2.02971807190993,17.0129210565932,-0.424989030591383));
#7033=CARTESIAN_POINT('Ctrl Pts',(2.,17.2212543899266,0.110909354270813));
#7034=CARTESIAN_POINT('Ctrl Pts',(1.97028192809007,17.4295877232599,0.646807739133109));
#7035=CARTESIAN_POINT('Ctrl Pts',(1.67659613043345,17.6379210565933,1.09605031831585));
#7036=CARTESIAN_POINT('Ctrl Pts',(1.38291033277684,17.8462543899265,1.54529289749865));
#7037=CARTESIAN_POINT('Ctrl Pts',(0.903949681684104,18.0545877232599,1.78750548470431));
#7038=CARTESIAN_POINT('Ctrl Pts',(0.424989030591369,18.2629210565932,2.02971807190994));
#7039=CARTESIAN_POINT('Ctrl Pts',(-0.110909354270865,18.4712543899266,2.));
#7040=CARTESIAN_POINT('Ctrl Pts',(-0.646807739133109,18.6795877232599,1.97028192809006));
#7041=CARTESIAN_POINT('Ctrl Pts',(-1.0960503183159,18.8879210565933,1.6765961304334));
#7042=CARTESIAN_POINT('Ctrl Pts',(-1.54529289749867,19.0962543899266,1.38291033277682));
#7043=CARTESIAN_POINT('Ctrl Pts',(-1.78750548470431,19.3045877232599,0.903949681684071));
#7044=CARTESIAN_POINT('Ctrl Pts',(-2.02971807190993,19.5129210565932,0.42498903059134));
#7045=CARTESIAN_POINT('Ctrl Pts',(-2.,19.7212543899266,-0.110909354270924));
#7046=CARTESIAN_POINT('Ctrl Pts',(-1.97028192809006,19.9295877232599,-0.646807739133152));
#7047=CARTESIAN_POINT('Ctrl Pts',(-1.67659613043345,20.1379210565933,-1.09605031831597));
#7048=CARTESIAN_POINT('Ctrl Pts',(-1.38291033277682,20.3462543899266,-1.54529289749875));
#7049=CARTESIAN_POINT('Ctrl Pts',(-0.903949681684103,20.5545877232599,-1.78750548470438));
#7050=CARTESIAN_POINT('Ctrl Pts',(-0.424989030591367,20.7629210565932,-2.02971807190997));
#7051=CARTESIAN_POINT('Ctrl Pts',(0.110909354270864,20.9712543899266,-2.0000000000001));
#7052=CARTESIAN_POINT('Ctrl Pts',(0.64680773913311,21.1795877232599,-1.97028192809011));
#7053=CARTESIAN_POINT('Ctrl Pts',(1.0960503183159,21.3879210565933,-1.67659613043352));
#7054=CARTESIAN_POINT('Ctrl Pts',(1.54529289749868,21.5962543899266,-1.38291033277682));
#7055=CARTESIAN_POINT('Ctrl Pts',(1.78750548470431,21.8045877232599,-0.90394968168419));
#7056=CARTESIAN_POINT('Ctrl Pts',(2.02971807190991,22.0129210565932,-0.42498903059139));
#7057=CARTESIAN_POINT('Ctrl Pts',(2.,22.2212543899266,0.110909354270855));
#7058=CARTESIAN_POINT('Ctrl Pts',(1.9702819280901,22.4295877232599,0.646807739133087));
#7059=CARTESIAN_POINT('Ctrl Pts',(1.67659613043345,22.6379210565933,1.09605031831588));
#7060=CARTESIAN_POINT('Ctrl Pts',(1.38291033277683,22.8462543899266,1.54529289749862));
#7061=CARTESIAN_POINT('Ctrl Pts',(0.903949681684118,23.0545877232599,1.78750548470426));
#7062=CARTESIAN_POINT('Ctrl Pts',(0.424989030591383,23.2629210565932,2.02971807190993));
#7063=CARTESIAN_POINT('Ctrl Pts',(-0.110909354270864,23.4712543899266,1.99999999999997));
#7064=CARTESIAN_POINT('Ctrl Pts',(-0.646807739133109,23.6795877232599,1.97028192809003));
#7065=CARTESIAN_POINT('Ctrl Pts',(-1.09605031831588,23.8879210565933,1.67659613043339));
#7066=CARTESIAN_POINT('Ctrl Pts',(-1.54529289749869,24.0962543899266,1.38291033277682));
#7067=CARTESIAN_POINT('Ctrl Pts',(-1.78750548470431,24.3045877232599,0.903949681684092));
#7068=CARTESIAN_POINT('Ctrl Pts',(-2.02971807190995,24.5129210565932,0.424989030591319));
#7069=CARTESIAN_POINT('Ctrl Pts',(-2.,24.7212543899266,-0.110909354270938));
#7070=CARTESIAN_POINT('Ctrl Pts',(-1.97028192809005,24.9295877232599,-0.646807739133109));
#7071=CARTESIAN_POINT('Ctrl Pts',(-1.67659613043344,25.1379210565933,-1.09605031831594));
#7072=CARTESIAN_POINT('Ctrl Pts',(-1.38291033277682,25.3462543899266,-1.54529289749872));
#7073=CARTESIAN_POINT('Ctrl Pts',(-0.903949681684104,25.55458772326,-1.7875054847044));
#7074=CARTESIAN_POINT('Ctrl Pts',(-0.424989030591382,25.7629210565933,-2.02971807190993));
#7075=CARTESIAN_POINT('Ctrl Pts',(0.110909354270864,25.9712543899266,-2.00000000000006));
#7076=CARTESIAN_POINT('Ctrl Pts',(0.646807739133109,26.1795877232599,-1.97028192809006));
#7077=CARTESIAN_POINT('Ctrl Pts',(1.0960503183159,26.3879210565933,-1.67659613043348));
#7078=CARTESIAN_POINT('Ctrl Pts',(1.5452928974987,26.5962543899266,-1.38291033277687));
#7079=CARTESIAN_POINT('Ctrl Pts',(1.78750548470431,26.80458772326,-0.903949681684155));
#7080=CARTESIAN_POINT('Ctrl Pts',(2.02971807190993,27.0129210565933,-0.424989030591383));
#7081=CARTESIAN_POINT('Ctrl Pts',(2.00000000000003,27.2212543899266,0.11090935427082));
#7082=CARTESIAN_POINT('Ctrl Pts',(1.97028192809007,27.4295877232599,0.646807739133109));
#7083=CARTESIAN_POINT('Ctrl Pts',(1.67659613043345,27.6379210565933,1.09605031831587));
#7084=CARTESIAN_POINT('Ctrl Pts',(1.38291033277684,27.8462543899266,1.54529289749868));
#7085=CARTESIAN_POINT('Ctrl Pts',(0.903949681684103,28.0545877232599,1.78750548470431));
#7086=CARTESIAN_POINT('Ctrl Pts',(0.424989030591382,28.2629210565932,2.02971807190993));
#7087=CARTESIAN_POINT('Ctrl Pts',(-0.110909354270852,28.4712543899266,1.99999999999998));
#7088=CARTESIAN_POINT('Ctrl Pts',(-0.646807739133109,28.6795877232599,1.97028192809006));
#7089=CARTESIAN_POINT('Ctrl Pts',(-1.0960503183159,28.8879210565933,1.67659613043341));
#7090=CARTESIAN_POINT('Ctrl Pts',(-1.54529289749868,29.0962543899266,1.38291033277682));
#7091=CARTESIAN_POINT('Ctrl Pts',(-1.78750548470432,29.30458772326,0.903949681684071));
#7092=CARTESIAN_POINT('Ctrl Pts',(-2.02971807190993,29.5129210565933,0.42498903059134));
#7093=CARTESIAN_POINT('Ctrl Pts',(-2.,29.7212543899266,-0.110909354270917));
#7094=CARTESIAN_POINT('Ctrl Pts',(-1.97028192809006,29.9295877232599,-0.646807739133087));
#7095=CARTESIAN_POINT('Ctrl Pts',(-1.67659613043345,30.1379210565933,-1.09605031831597));
#7096=CARTESIAN_POINT('Ctrl Pts',(-1.38291033277683,30.3462543899266,-1.54529289749872));
#7097=CARTESIAN_POINT('Ctrl Pts',(-0.903949681684103,30.55458772326,-1.78750548470437));
#7098=CARTESIAN_POINT('Ctrl Pts',(-0.424989030591367,30.7629210565933,-2.02971807190996));
#7099=CARTESIAN_POINT('Ctrl Pts',(0.110909354270865,30.9712543899266,-2.00000000000009));
#7100=CARTESIAN_POINT('Ctrl Pts',(0.646807739133123,31.1795877232599,-1.97028192809004));
#7101=CARTESIAN_POINT('Ctrl Pts',(1.0960503183159,31.3879210565933,-1.67659613043352));
#7102=CARTESIAN_POINT('Ctrl Pts',(1.54529289749868,31.5962543899266,-1.38291033277685));
#7103=CARTESIAN_POINT('Ctrl Pts',(1.78750548470431,31.80458772326,-0.903949681684169));
#7104=CARTESIAN_POINT('Ctrl Pts',(2.02971807190993,32.0129210565933,-0.424989030591419));
#7105=CARTESIAN_POINT('Ctrl Pts',(2.,32.2212543899266,0.110909354270869));
#7106=CARTESIAN_POINT('Ctrl Pts',(1.97028192809004,32.4295877232599,0.646807739133087));
#7107=CARTESIAN_POINT('Ctrl Pts',(1.67659613043345,32.6379210565933,1.09605031831587));
#7108=CARTESIAN_POINT('Ctrl Pts',(1.38291033277682,32.8462543899266,1.54529289749868));
#7109=CARTESIAN_POINT('Ctrl Pts',(0.903949681684104,33.0545877232599,1.78750548470431));
#7110=CARTESIAN_POINT('Ctrl Pts',(0.424989030591383,33.2629210565932,2.02971807190993));
#7111=CARTESIAN_POINT('Ctrl Pts',(-0.110909354270864,33.4712543899267,1.99999999999997));
#7112=CARTESIAN_POINT('Ctrl Pts',(-0.646807739133109,33.6795877232599,1.97028192809004));
#7113=CARTESIAN_POINT('Ctrl Pts',(-1.09605031831588,33.8879210565934,1.6765961304334));
#7114=CARTESIAN_POINT('Ctrl Pts',(-1.54529289749868,34.0962543899266,1.38291033277683));
#7115=CARTESIAN_POINT('Ctrl Pts',(-1.78750548470431,34.30458772326,0.903949681684037));
#7116=CARTESIAN_POINT('Ctrl Pts',(-2.02971807190994,34.5129210565932,0.424989030591383));
#7117=CARTESIAN_POINT('Ctrl Pts',(-2.,34.7212543899267,-0.110909354270938));
#7118=CARTESIAN_POINT('Ctrl Pts',(-1.97028192809006,34.9295877232599,-0.646807739133123));
#7119=CARTESIAN_POINT('Ctrl Pts',(-1.67659613043344,35.1379210565933,-1.09605031831594));
#7120=CARTESIAN_POINT('Ctrl Pts',(-1.38291033277682,35.3462543899267,-1.54529289749875));
#7121=CARTESIAN_POINT('Ctrl Pts',(-0.903949681684103,35.55458772326,-1.78750548470439));
#7122=CARTESIAN_POINT('Ctrl Pts',(-0.424989030591382,35.7629210565932,-2.02971807190993));
#7123=CARTESIAN_POINT('Ctrl Pts',(0.110909354270864,35.9712543899267,-2.00000000000003));
#7124=CARTESIAN_POINT('Ctrl Pts',(0.64680773913311,36.1795877232599,-1.97028192809006));
#7125=CARTESIAN_POINT('Ctrl Pts',(1.0960503183159,36.3879210565933,-1.67659613043348));
#7126=CARTESIAN_POINT('Ctrl Pts',(1.54529289749869,36.5962543899266,-1.38291033277682));
#7127=CARTESIAN_POINT('Ctrl Pts',(1.78750548470431,36.80458772326,-0.903949681684127));
#7128=CARTESIAN_POINT('Ctrl Pts',(2.02971807190993,37.0129210565932,-0.424989030591383));
#7129=CARTESIAN_POINT('Ctrl Pts',(2.,37.2212543899267,0.110909354270834));
#7130=CARTESIAN_POINT('Ctrl Pts',(1.97028192809006,37.4295877232599,0.646807739133109));
#7131=CARTESIAN_POINT('Ctrl Pts',(1.67659613043345,37.6379210565933,1.09605031831588));
#7132=CARTESIAN_POINT('Ctrl Pts',(1.38291033277681,37.8462543899266,1.54529289749865));
#7133=CARTESIAN_POINT('Ctrl Pts',(0.903949681684104,38.0545877232599,1.78750548470431));
#7134=CARTESIAN_POINT('Ctrl Pts',(0.424989030591383,38.2629210565933,2.02971807190991));
#7135=CARTESIAN_POINT('Ctrl Pts',(-0.11090935427085,38.4712543899266,1.99999999999995));
#7136=CARTESIAN_POINT('Ctrl Pts',(-0.64680773913311,38.67958772326,1.97028192809006));
#7137=CARTESIAN_POINT('Ctrl Pts',(-1.0960503183159,38.8879210565933,1.67659613043344));
#7138=CARTESIAN_POINT('Ctrl Pts',(-1.54529289749868,39.0962543899266,1.38291033277682));
#7139=CARTESIAN_POINT('Ctrl Pts',(-1.78750548470431,39.30458772326,0.903949681684064));
#7140=CARTESIAN_POINT('Ctrl Pts',(-2.02971807190993,39.5129210565932,0.424989030591369));
#7141=CARTESIAN_POINT('Ctrl Pts',(-2.,39.7212543899267,-0.110909354270917));
#7142=CARTESIAN_POINT('Ctrl Pts',(-2.59980895670905,-0.278745610073447,
-0.11090935427086));
#7143=CARTESIAN_POINT('Ctrl Pts',(-2.5700908847991,-0.0704122767401095,
-0.807526064696338));
#7144=CARTESIAN_POINT('Ctrl Pts',(-2.19604592436092,0.137921056593207,-1.39595479667049));
#7145=CARTESIAN_POINT('Ctrl Pts',(-1.82200096392271,0.346254389926554,-1.98438352864466));
#7146=CARTESIAN_POINT('Ctrl Pts',(-1.20385416003863,0.554587723259855,-2.30695527863182));
#7147=CARTESIAN_POINT('Ctrl Pts',(-0.585707356154528,0.762921056593228,
-2.62952702861907));
#7148=CARTESIAN_POINT('Ctrl Pts',(0.11090935427086,0.971254389926535,-2.59980895670912));
#7149=CARTESIAN_POINT('Ctrl Pts',(0.807526064696268,1.17958772325987,-2.57009088479919));
#7150=CARTESIAN_POINT('Ctrl Pts',(1.39595479667041,1.38792105659322,-2.196045924361));
#7151=CARTESIAN_POINT('Ctrl Pts',(1.98438352864458,1.59625438992655,-1.82200096392273));
#7152=CARTESIAN_POINT('Ctrl Pts',(2.30695527863176,1.80458772325989,-1.20385416003868));
#7153=CARTESIAN_POINT('Ctrl Pts',(2.62952702861898,2.01292105659322,-0.58570735615462));
#7154=CARTESIAN_POINT('Ctrl Pts',(2.59980895670903,2.22125438992652,0.110909354270808));
#7155=CARTESIAN_POINT('Ctrl Pts',(2.57009088479911,2.42958772325989,0.807526064696155));
#7156=CARTESIAN_POINT('Ctrl Pts',(2.1960459243609,2.63792105659321,1.39595479667038));
#7157=CARTESIAN_POINT('Ctrl Pts',(1.82200096392273,2.84625438992655,1.98438352864455));
#7158=CARTESIAN_POINT('Ctrl Pts',(1.20385416003861,3.05458772325989,2.3069552786317));
#7159=CARTESIAN_POINT('Ctrl Pts',(0.585707356154531,3.26292105659321,2.62952702861891));
#7160=CARTESIAN_POINT('Ctrl Pts',(-0.11090935427086,3.47125438992654,2.59980895670896));
#7161=CARTESIAN_POINT('Ctrl Pts',(-0.807526064696246,3.67958772325991,2.57009088479904));
#7162=CARTESIAN_POINT('Ctrl Pts',(-1.39595479667041,3.8879210565932,2.1960459243609));
#7163=CARTESIAN_POINT('Ctrl Pts',(-1.98438352864456,4.09625438992658,1.82200096392269));
#7164=CARTESIAN_POINT('Ctrl Pts',(-2.3069552786318,4.30458772325988,1.20385416003854));
#7165=CARTESIAN_POINT('Ctrl Pts',(-2.62952702861897,4.51292105659321,0.585707356154447));
#7166=CARTESIAN_POINT('Ctrl Pts',(-2.59980895670904,4.72125438992652,-0.110909354270855));
#7167=CARTESIAN_POINT('Ctrl Pts',(-2.5700908847991,4.92958772325988,-0.807526064696333));
#7168=CARTESIAN_POINT('Ctrl Pts',(-2.19604592436094,5.13792105659322,-1.39595479667042));
#7169=CARTESIAN_POINT('Ctrl Pts',(-1.82200096392273,5.34625438992655,-1.98438352864466));
#7170=CARTESIAN_POINT('Ctrl Pts',(-1.20385416003865,5.55458772325989,-2.30695527863179));
#7171=CARTESIAN_POINT('Ctrl Pts',(-0.585707356154528,5.76292105659322,-2.62952702861911));
#7172=CARTESIAN_POINT('Ctrl Pts',(0.110909354270839,5.97125438992656,-2.59980895670905));
#7173=CARTESIAN_POINT('Ctrl Pts',(0.807526064696268,6.1795877232599,-2.57009088479919));
#7174=CARTESIAN_POINT('Ctrl Pts',(1.39595479667041,6.38792105659324,-2.196045924361));
#7175=CARTESIAN_POINT('Ctrl Pts',(1.9843835286446,6.59625438992657,-1.82200096392282));
#7176=CARTESIAN_POINT('Ctrl Pts',(2.30695527863178,6.80458772325989,-1.20385416003871));
#7177=CARTESIAN_POINT('Ctrl Pts',(2.62952702861898,7.01292105659322,-0.585707356154609));
#7178=CARTESIAN_POINT('Ctrl Pts',(2.59980895670904,7.22125438992658,0.110909354270855));
#7179=CARTESIAN_POINT('Ctrl Pts',(2.57009088479913,7.42958772325989,0.807526064696236));
#7180=CARTESIAN_POINT('Ctrl Pts',(2.19604592436092,7.63792105659324,1.39595479667033));
#7181=CARTESIAN_POINT('Ctrl Pts',(1.82200096392274,7.84625438992655,1.98438352864452));
#7182=CARTESIAN_POINT('Ctrl Pts',(1.20385416003861,8.05458772325989,2.30695527863176));
#7183=CARTESIAN_POINT('Ctrl Pts',(0.585707356154531,8.26292105659324,2.62952702861887));
#7184=CARTESIAN_POINT('Ctrl Pts',(-0.11090935427086,8.47125438992656,2.59980895670904));
#7185=CARTESIAN_POINT('Ctrl Pts',(-0.807526064696241,8.67958772325989,2.57009088479907));
#7186=CARTESIAN_POINT('Ctrl Pts',(-1.39595479667041,8.88792105659322,2.19604592436091));
#7187=CARTESIAN_POINT('Ctrl Pts',(-1.98438352864456,9.09625438992657,1.82200096392265));
#7188=CARTESIAN_POINT('Ctrl Pts',(-2.3069552786318,9.30458772325988,1.20385416003854));
#7189=CARTESIAN_POINT('Ctrl Pts',(-2.62952702861897,9.51292105659323,0.585707356154528));
#7190=CARTESIAN_POINT('Ctrl Pts',(-2.59980895670904,9.72125438992655,-0.11090935427086));
#7191=CARTESIAN_POINT('Ctrl Pts',(-2.57009088479911,9.92958772325989,-0.807526064696419));
#7192=CARTESIAN_POINT('Ctrl Pts',(-2.19604592436092,10.1379210565932,-1.39595479667049));
#7193=CARTESIAN_POINT('Ctrl Pts',(-1.82200096392273,10.3462543899266,-1.98438352864459));
#7194=CARTESIAN_POINT('Ctrl Pts',(-1.20385416003865,10.5545877232599,-2.30695527863179));
#7195=CARTESIAN_POINT('Ctrl Pts',(-0.585707356154528,10.7629210565933,-2.6295270286191));
#7196=CARTESIAN_POINT('Ctrl Pts',(0.11090935427086,10.9712543899266,-2.59980895670905));
#7197=CARTESIAN_POINT('Ctrl Pts',(0.807526064696249,11.1795877232599,-2.57009088479919));
#7198=CARTESIAN_POINT('Ctrl Pts',(1.39595479667039,11.3879210565932,-2.196045924361));
#7199=CARTESIAN_POINT('Ctrl Pts',(1.98438352864458,11.5962543899266,-1.82200096392274));
#7200=CARTESIAN_POINT('Ctrl Pts',(2.30695527863176,11.8045877232599,-1.20385416003872));
#7201=CARTESIAN_POINT('Ctrl Pts',(2.62952702861898,12.0129210565933,-0.585707356154631));
#7202=CARTESIAN_POINT('Ctrl Pts',(2.59980895670904,12.2212543899266,0.11090935427085));
#7203=CARTESIAN_POINT('Ctrl Pts',(2.57009088479911,12.4295877232599,0.807526064696171));
#7204=CARTESIAN_POINT('Ctrl Pts',(2.1960459243609,12.6379210565932,1.39595479667034));
#7205=CARTESIAN_POINT('Ctrl Pts',(1.82200096392273,12.8462543899266,1.98438352864456));
#7206=CARTESIAN_POINT('Ctrl Pts',(1.20385416003863,13.0545877232599,2.30695527863174));
#7207=CARTESIAN_POINT('Ctrl Pts',(0.585707356154552,13.2629210565932,2.62952702861889));
#7208=CARTESIAN_POINT('Ctrl Pts',(-0.11090935427086,13.4712543899266,2.599808956709));
#7209=CARTESIAN_POINT('Ctrl Pts',(-0.807526064696246,13.6795877232599,2.57009088479904));
#7210=CARTESIAN_POINT('Ctrl Pts',(-1.39595479667043,13.8879210565933,2.1960459243609));
#7211=CARTESIAN_POINT('Ctrl Pts',(-1.98438352864458,14.0962543899266,1.82200096392269));
#7212=CARTESIAN_POINT('Ctrl Pts',(-2.3069552786318,14.3045877232599,1.20385416003854));
#7213=CARTESIAN_POINT('Ctrl Pts',(-2.62952702861897,14.5129210565932,0.585707356154453));
#7214=CARTESIAN_POINT('Ctrl Pts',(-2.59980895670906,14.7212543899266,-0.110909354270865));
#7215=CARTESIAN_POINT('Ctrl Pts',(-2.57009088479911,14.9295877232599,-0.807526064696338));
#7216=CARTESIAN_POINT('Ctrl Pts',(-2.19604592436092,15.1379210565932,-1.39595479667049));
#7217=CARTESIAN_POINT('Ctrl Pts',(-1.82200096392273,15.3462543899266,-1.98438352864467));
#7218=CARTESIAN_POINT('Ctrl Pts',(-1.20385416003865,15.5545877232599,-2.30695527863179));
#7219=CARTESIAN_POINT('Ctrl Pts',(-0.585707356154509,15.7629210565933,-2.62952702861908));
#7220=CARTESIAN_POINT('Ctrl Pts',(0.110909354270839,15.9712543899266,-2.59980895670905));
#7221=CARTESIAN_POINT('Ctrl Pts',(0.807526064696268,16.1795877232599,-2.57009088479922));
#7222=CARTESIAN_POINT('Ctrl Pts',(1.39595479667041,16.3879210565933,-2.19604592436098));
#7223=CARTESIAN_POINT('Ctrl Pts',(1.9843835286446,16.5962543899266,-1.82200096392274));
#7224=CARTESIAN_POINT('Ctrl Pts',(2.30695527863178,16.8045877232599,-1.20385416003872));
#7225=CARTESIAN_POINT('Ctrl Pts',(2.629527028619,17.0129210565933,-0.58570735615462));
#7226=CARTESIAN_POINT('Ctrl Pts',(2.59980895670902,17.2212543899266,0.110909354270855));
#7227=CARTESIAN_POINT('Ctrl Pts',(2.57009088479911,17.42958772326,0.807526064696182));
#7228=CARTESIAN_POINT('Ctrl Pts',(2.1960459243609,17.6379210565933,1.3959547966704));
#7229=CARTESIAN_POINT('Ctrl Pts',(1.82200096392273,17.8462543899266,1.98438352864452));
#7230=CARTESIAN_POINT('Ctrl Pts',(1.20385416003863,18.0545877232599,2.30695527863173));
#7231=CARTESIAN_POINT('Ctrl Pts',(0.585707356154531,18.2629210565933,2.62952702861889));
#7232=CARTESIAN_POINT('Ctrl Pts',(-0.11090935427086,18.4712543899266,2.599808956709));
#7233=CARTESIAN_POINT('Ctrl Pts',(-0.807526064696244,18.6795877232599,2.57009088479907));
#7234=CARTESIAN_POINT('Ctrl Pts',(-1.39595479667041,18.8879210565933,2.19604592436089));
#7235=CARTESIAN_POINT('Ctrl Pts',(-1.98438352864458,19.0962543899266,1.82200096392266));
#7236=CARTESIAN_POINT('Ctrl Pts',(-2.3069552786318,19.3045877232599,1.20385416003862));
#7237=CARTESIAN_POINT('Ctrl Pts',(-2.62952702861896,19.5129210565933,0.585707356154491));
#7238=CARTESIAN_POINT('Ctrl Pts',(-2.59980895670904,19.7212543899266,-0.110909354270865));
#7239=CARTESIAN_POINT('Ctrl Pts',(-2.5700908847991,19.9295877232599,-0.8075260646963));
#7240=CARTESIAN_POINT('Ctrl Pts',(-2.19604592436092,20.1379210565933,-1.39595479667049));
#7241=CARTESIAN_POINT('Ctrl Pts',(-1.82200096392271,20.3462543899266,-1.98438352864466));
#7242=CARTESIAN_POINT('Ctrl Pts',(-1.20385416003865,20.5545877232599,-2.30695527863182));
#7243=CARTESIAN_POINT('Ctrl Pts',(-0.585707356154528,20.7629210565933,-2.62952702861907));
#7244=CARTESIAN_POINT('Ctrl Pts',(0.110909354270839,20.9712543899266,-2.59980895670905));
#7245=CARTESIAN_POINT('Ctrl Pts',(0.807526064696249,21.1795877232599,-2.5700908847992));
#7246=CARTESIAN_POINT('Ctrl Pts',(1.39595479667039,21.3879210565933,-2.19604592436098));
#7247=CARTESIAN_POINT('Ctrl Pts',(1.9843835286446,21.5962543899266,-1.8220009639228));
#7248=CARTESIAN_POINT('Ctrl Pts',(2.30695527863176,21.8045877232599,-1.20385416003872));
#7249=CARTESIAN_POINT('Ctrl Pts',(2.62952702861898,22.0129210565933,-0.585707356154604));
#7250=CARTESIAN_POINT('Ctrl Pts',(2.59980895670904,22.2212543899266,0.11090935427085));
#7251=CARTESIAN_POINT('Ctrl Pts',(2.57009088479913,22.42958772326,0.807526064696171));
#7252=CARTESIAN_POINT('Ctrl Pts',(2.19604592436092,22.6379210565933,1.3959547966704));
#7253=CARTESIAN_POINT('Ctrl Pts',(1.82200096392275,22.8462543899266,1.98438352864454));
#7254=CARTESIAN_POINT('Ctrl Pts',(1.20385416003863,23.0545877232599,2.30695527863174));
#7255=CARTESIAN_POINT('Ctrl Pts',(0.58570735615455,23.2629210565933,2.62952702861891));
#7256=CARTESIAN_POINT('Ctrl Pts',(-0.110909354270881,23.4712543899266,2.599808956709));
#7257=CARTESIAN_POINT('Ctrl Pts',(-0.807526064696225,23.6795877232599,2.57009088479905));
#7258=CARTESIAN_POINT('Ctrl Pts',(-1.39595479667043,23.8879210565933,2.19604592436087));
#7259=CARTESIAN_POINT('Ctrl Pts',(-1.98438352864458,24.0962543899266,1.82200096392269));
#7260=CARTESIAN_POINT('Ctrl Pts',(-2.3069552786318,24.3045877232599,1.20385416003862));
#7261=CARTESIAN_POINT('Ctrl Pts',(-2.62952702861898,24.5129210565933,0.585707356154485));
#7262=CARTESIAN_POINT('Ctrl Pts',(-2.59980895670906,24.7212543899266,-0.110909354270829));
#7263=CARTESIAN_POINT('Ctrl Pts',(-2.5700908847991,24.92958772326,-0.807526064696322));
#7264=CARTESIAN_POINT('Ctrl Pts',(-2.19604592436094,25.1379210565933,-1.39595479667048));
#7265=CARTESIAN_POINT('Ctrl Pts',(-1.82200096392273,25.3462543899266,-1.98438352864461));
#7266=CARTESIAN_POINT('Ctrl Pts',(-1.20385416003865,25.5545877232599,-2.30695527863182));
#7267=CARTESIAN_POINT('Ctrl Pts',(-0.585707356154509,25.7629210565933,-2.62952702861915));
#7268=CARTESIAN_POINT('Ctrl Pts',(0.110909354270839,25.9712543899266,-2.59980895670905));
#7269=CARTESIAN_POINT('Ctrl Pts',(0.807526064696246,26.17958772326,-2.57009088479919));
#7270=CARTESIAN_POINT('Ctrl Pts',(1.39595479667039,26.3879210565933,-2.19604592436098));
#7271=CARTESIAN_POINT('Ctrl Pts',(1.98438352864458,26.5962543899266,-1.82200096392281));
#7272=CARTESIAN_POINT('Ctrl Pts',(2.30695527863176,26.80458772326,-1.20385416003873));
#7273=CARTESIAN_POINT('Ctrl Pts',(2.629527028619,27.0129210565933,-0.585707356154641));
#7274=CARTESIAN_POINT('Ctrl Pts',(2.59980895670904,27.2212543899266,0.110909354270782));
#7275=CARTESIAN_POINT('Ctrl Pts',(2.57009088479911,27.42958772326,0.807526064696187));
#7276=CARTESIAN_POINT('Ctrl Pts',(2.1960459243609,27.6379210565932,1.39595479667041));
#7277=CARTESIAN_POINT('Ctrl Pts',(1.82200096392273,27.8462543899266,1.98438352864453));
#7278=CARTESIAN_POINT('Ctrl Pts',(1.20385416003861,28.05458772326,2.30695527863173));
#7279=CARTESIAN_POINT('Ctrl Pts',(0.585707356154552,28.2629210565933,2.62952702861888));
#7280=CARTESIAN_POINT('Ctrl Pts',(-0.11090935427086,28.4712543899266,2.59980895670899));
#7281=CARTESIAN_POINT('Ctrl Pts',(-0.807526064696246,28.67958772326,2.57009088479907));
#7282=CARTESIAN_POINT('Ctrl Pts',(-1.39595479667043,28.8879210565933,2.19604592436087));
#7283=CARTESIAN_POINT('Ctrl Pts',(-1.98438352864458,29.0962543899266,1.82200096392266));
#7284=CARTESIAN_POINT('Ctrl Pts',(-2.3069552786318,29.3045877232599,1.20385416003859));
#7285=CARTESIAN_POINT('Ctrl Pts',(-2.62952702861898,29.5129210565933,0.585707356154469));
#7286=CARTESIAN_POINT('Ctrl Pts',(-2.59980895670906,29.7212543899266,-0.110909354270912));
#7287=CARTESIAN_POINT('Ctrl Pts',(-2.5700908847991,29.92958772326,-0.807526064696306));
#7288=CARTESIAN_POINT('Ctrl Pts',(-2.19604592436092,30.1379210565933,-1.39595479667046));
#7289=CARTESIAN_POINT('Ctrl Pts',(-1.82200096392273,30.3462543899266,-1.98438352864468));
#7290=CARTESIAN_POINT('Ctrl Pts',(-1.20385416003865,30.5545877232599,-2.30695527863181));
#7291=CARTESIAN_POINT('Ctrl Pts',(-0.585707356154507,30.7629210565933,-2.6295270286191));
#7292=CARTESIAN_POINT('Ctrl Pts',(0.110909354270839,30.9712543899266,-2.59980895670908));
#7293=CARTESIAN_POINT('Ctrl Pts',(0.807526064696246,31.17958772326,-2.57009088479918));
#7294=CARTESIAN_POINT('Ctrl Pts',(1.39595479667041,31.3879210565933,-2.19604592436097));
#7295=CARTESIAN_POINT('Ctrl Pts',(1.9843835286446,31.5962543899266,-1.82200096392281));
#7296=CARTESIAN_POINT('Ctrl Pts',(2.30695527863178,31.80458772326,-1.20385416003872));
#7297=CARTESIAN_POINT('Ctrl Pts',(2.629527028619,32.0129210565933,-0.585707356154615));
#7298=CARTESIAN_POINT('Ctrl Pts',(2.59980895670902,32.2212543899266,0.110909354270782));
#7299=CARTESIAN_POINT('Ctrl Pts',(2.57009088479913,32.4295877232599,0.807526064696171));
#7300=CARTESIAN_POINT('Ctrl Pts',(2.1960459243609,32.6379210565933,1.3959547966704));
#7301=CARTESIAN_POINT('Ctrl Pts',(1.82200096392275,32.8462543899266,1.98438352864454));
#7302=CARTESIAN_POINT('Ctrl Pts',(1.20385416003863,33.05458772326,2.30695527863173));
#7303=CARTESIAN_POINT('Ctrl Pts',(0.585707356154531,33.2629210565933,2.62952702861892));
#7304=CARTESIAN_POINT('Ctrl Pts',(-0.11090935427086,33.4712543899266,2.59980895670899));
#7305=CARTESIAN_POINT('Ctrl Pts',(-0.807526064696225,33.67958772326,2.57009088479904));
#7306=CARTESIAN_POINT('Ctrl Pts',(-1.39595479667043,33.8879210565933,2.19604592436087));
#7307=CARTESIAN_POINT('Ctrl Pts',(-1.98438352864458,34.0962543899266,1.82200096392268));
#7308=CARTESIAN_POINT('Ctrl Pts',(-2.30695527863178,34.3045877232599,1.2038541600386));
#7309=CARTESIAN_POINT('Ctrl Pts',(-2.62952702861898,34.5129210565933,0.585707356154485));
#7310=CARTESIAN_POINT('Ctrl Pts',(-2.59980895670904,34.7212543899266,-0.110909354270923));
#7311=CARTESIAN_POINT('Ctrl Pts',(-2.5700908847991,34.92958772326,-0.807526064696322));
#7312=CARTESIAN_POINT('Ctrl Pts',(-2.19604592436092,35.1379210565933,-1.39595479667045));
#7313=CARTESIAN_POINT('Ctrl Pts',(-1.82200096392271,35.3462543899266,-1.98438352864466));
#7314=CARTESIAN_POINT('Ctrl Pts',(-1.20385416003863,35.55458772326,-2.30695527863182));
#7315=CARTESIAN_POINT('Ctrl Pts',(-0.585707356154509,35.7629210565933,-2.62952702861903));
#7316=CARTESIAN_POINT('Ctrl Pts',(0.110909354270858,35.9712543899266,-2.59980895670908));
#7317=CARTESIAN_POINT('Ctrl Pts',(0.807526064696268,36.17958772326,-2.57009088479921));
#7318=CARTESIAN_POINT('Ctrl Pts',(1.3959547966704,36.3879210565933,-2.19604592436097));
#7319=CARTESIAN_POINT('Ctrl Pts',(1.98438352864458,36.5962543899266,-1.82200096392283));
#7320=CARTESIAN_POINT('Ctrl Pts',(2.30695527863176,36.80458772326,-1.20385416003864));
#7321=CARTESIAN_POINT('Ctrl Pts',(2.629527028619,37.0129210565933,-0.585707356154631));
#7322=CARTESIAN_POINT('Ctrl Pts',(2.59980895670904,37.2212543899266,0.110909354270793));
#7323=CARTESIAN_POINT('Ctrl Pts',(2.57009088479913,37.42958772326,0.807526064696182));
#7324=CARTESIAN_POINT('Ctrl Pts',(2.1960459243609,37.6379210565933,1.39595479667037));
#7325=CARTESIAN_POINT('Ctrl Pts',(1.82200096392275,37.8462543899266,1.98438352864452));
#7326=CARTESIAN_POINT('Ctrl Pts',(1.20385416003863,38.05458772326,2.30695527863174));
#7327=CARTESIAN_POINT('Ctrl Pts',(0.585707356154552,38.2629210565933,2.62952702861889));
#7328=CARTESIAN_POINT('Ctrl Pts',(-0.110909354270881,38.4712543899266,2.599808956709));
#7329=CARTESIAN_POINT('Ctrl Pts',(-0.807526064696225,38.67958772326,2.57009088479908));
#7330=CARTESIAN_POINT('Ctrl Pts',(-1.39595479667043,38.8879210565933,2.19604592436087));
#7331=CARTESIAN_POINT('Ctrl Pts',(-1.98438352864458,39.0962543899267,1.82200096392266));
#7332=CARTESIAN_POINT('Ctrl Pts',(-2.30695527863182,39.30458772326,1.20385416003859));
#7333=CARTESIAN_POINT('Ctrl Pts',(-2.62952702861897,39.5129210565933,0.585707356154453));
#7334=CARTESIAN_POINT('Ctrl Pts',(-2.59980895670906,39.7212543899267,-0.110909354270912));
#7335=CARTESIAN_POINT('Ctrl Pts',(-2.599999979715,0.278627239826795,0.110862256246242));
#7336=CARTESIAN_POINT('Ctrl Pts',(-2.62970543174724,0.486960573160142,-0.585805638639407));
#7337=CARTESIAN_POINT('Ctrl Pts',(-2.30709716039532,0.695293906493465,-1.20399045962746));
#7338=CARTESIAN_POINT('Ctrl Pts',(-1.98448888904339,0.903627239826795,-1.82217528061545));
#7339=CARTESIAN_POINT('Ctrl Pts',(-1.39600952008762,1.11196057316013,-2.19623490414907));
#7340=CARTESIAN_POINT('Ctrl Pts',(-0.807530151131804,1.32029390649347,-2.57029452768285));
#7341=CARTESIAN_POINT('Ctrl Pts',(-0.110862256246242,1.5286272398268,-2.59999997971506));
#7342=CARTESIAN_POINT('Ctrl Pts',(0.585805638639342,1.73696057316013,-2.62970543174735));
#7343=CARTESIAN_POINT('Ctrl Pts',(1.20399045962738,1.94529390649346,-2.3070971603954));
#7344=CARTESIAN_POINT('Ctrl Pts',(1.82217528061545,2.15362723982677,-1.98448888904346));
#7345=CARTESIAN_POINT('Ctrl Pts',(2.19623490414905,2.36196057316013,-1.3960095200876));
#7346=CARTESIAN_POINT('Ctrl Pts',(2.57029452768271,2.57029390649346,-0.807530151131844));
#7347=CARTESIAN_POINT('Ctrl Pts',(2.59999997971496,2.7786272398268,-0.110862256246237));
#7348=CARTESIAN_POINT('Ctrl Pts',(2.62970543174727,2.98696057316012,0.585805638639234));
#7349=CARTESIAN_POINT('Ctrl Pts',(2.3070971603953,3.19529390649347,1.20399045962738));
#7350=CARTESIAN_POINT('Ctrl Pts',(1.98448888904339,3.40362723982677,1.82217528061537));
#7351=CARTESIAN_POINT('Ctrl Pts',(1.39600952008757,3.61196057316014,2.19623490414904));
#7352=CARTESIAN_POINT('Ctrl Pts',(0.807530151131806,3.82029390649348,2.57029452768262));
#7353=CARTESIAN_POINT('Ctrl Pts',(0.110862256246242,4.0286272398268,2.59999997971498));
#7354=CARTESIAN_POINT('Ctrl Pts',(-0.58580563863932,4.23696057316013,2.62970543174725));
#7355=CARTESIAN_POINT('Ctrl Pts',(-1.2039904596274,4.44529390649346,2.30709716039531));
#7356=CARTESIAN_POINT('Ctrl Pts',(-1.82217528061542,4.6536272398268,1.9844888890433));
#7357=CARTESIAN_POINT('Ctrl Pts',(-2.19623490414908,4.8619605731601,1.39600952008752));
#7358=CARTESIAN_POINT('Ctrl Pts',(-2.57029452768269,5.07029390649345,0.807530151131704));
#7359=CARTESIAN_POINT('Ctrl Pts',(-2.599999979715,5.2786272398268,0.110862256246242));
#7360=CARTESIAN_POINT('Ctrl Pts',(-2.62970543174724,5.48696057316013,-0.585805638639487));
#7361=CARTESIAN_POINT('Ctrl Pts',(-2.30709716039534,5.69529390649347,-1.20399045962746));
#7362=CARTESIAN_POINT('Ctrl Pts',(-1.98448888904338,5.90362723982679,-1.82217528061554));
#7363=CARTESIAN_POINT('Ctrl Pts',(-1.39600952008762,6.11196057316013,-2.19623490414907));
#7364=CARTESIAN_POINT('Ctrl Pts',(-0.807530151131785,6.32029390649347,-2.57029452768279));
#7365=CARTESIAN_POINT('Ctrl Pts',(-0.110862256246242,6.52862723982682,-2.59999997971506));
#7366=CARTESIAN_POINT('Ctrl Pts',(0.585805638639323,6.73696057316013,-2.62970543174735));
#7367=CARTESIAN_POINT('Ctrl Pts',(1.20399045962736,6.94529390649349,-2.3070971603954));
#7368=CARTESIAN_POINT('Ctrl Pts',(1.82217528061547,7.1536272398268,-1.98448888904338));
#7369=CARTESIAN_POINT('Ctrl Pts',(2.19623490414908,7.36196057316014,-1.3960095200876));
#7370=CARTESIAN_POINT('Ctrl Pts',(2.57029452768273,7.5702939064935,-0.807530151131904));
#7371=CARTESIAN_POINT('Ctrl Pts',(2.59999997971498,7.7786272398268,-0.110862256246237));
#7372=CARTESIAN_POINT('Ctrl Pts',(2.62970543174725,7.98696057316015,0.585805638639229));
#7373=CARTESIAN_POINT('Ctrl Pts',(2.3070971603953,8.19529390649346,1.20399045962738));
#7374=CARTESIAN_POINT('Ctrl Pts',(1.9844888890434,8.40362723982681,1.82217528061536));
#7375=CARTESIAN_POINT('Ctrl Pts',(1.39600952008757,8.61196057316016,2.19623490414907));
#7376=CARTESIAN_POINT('Ctrl Pts',(0.807530151131809,8.82029390649348,2.57029452768262));
#7377=CARTESIAN_POINT('Ctrl Pts',(0.110862256246222,9.0286272398268,2.59999997971494));
#7378=CARTESIAN_POINT('Ctrl Pts',(-0.58580563863932,9.23696057316016,2.62970543174721));
#7379=CARTESIAN_POINT('Ctrl Pts',(-1.2039904596274,9.44529390649347,2.30709716039531));
#7380=CARTESIAN_POINT('Ctrl Pts',(-1.82217528061542,9.65362723982683,1.98448888904329));
#7381=CARTESIAN_POINT('Ctrl Pts',(-2.1962349041491,9.86196057316016,1.39600952008751));
#7382=CARTESIAN_POINT('Ctrl Pts',(-2.5702945276827,10.0702939064935,0.80753015113172));
#7383=CARTESIAN_POINT('Ctrl Pts',(-2.59999997971498,10.2786272398268,0.110862256246242));
#7384=CARTESIAN_POINT('Ctrl Pts',(-2.62970543174724,10.4869605731602,-0.585805638639412));
#7385=CARTESIAN_POINT('Ctrl Pts',(-2.30709716039534,10.6952939064935,-1.20399045962747));
#7386=CARTESIAN_POINT('Ctrl Pts',(-1.98448888904336,10.9036272398268,-1.82217528061554));
#7387=CARTESIAN_POINT('Ctrl Pts',(-1.39600952008762,11.1119605731601,-2.19623490414907));
#7388=CARTESIAN_POINT('Ctrl Pts',(-0.807530151131806,11.3202939064935,-2.57029452768279));
#7389=CARTESIAN_POINT('Ctrl Pts',(-0.110862256246242,11.5286272398268,-2.59999997971505));
#7390=CARTESIAN_POINT('Ctrl Pts',(0.585805638639342,11.7369605731602,-2.62970543174735));
#7391=CARTESIAN_POINT('Ctrl Pts',(1.20399045962738,11.9452939064935,-2.3070971603954));
#7392=CARTESIAN_POINT('Ctrl Pts',(1.82217528061545,12.1536272398268,-1.98448888904347));
#7393=CARTESIAN_POINT('Ctrl Pts',(2.19623490414905,12.3619605731601,-1.3960095200876));
#7394=CARTESIAN_POINT('Ctrl Pts',(2.57029452768273,12.5702939064935,-0.807530151131898));
#7395=CARTESIAN_POINT('Ctrl Pts',(2.59999997971498,12.7786272398268,-0.110862256246237));
#7396=CARTESIAN_POINT('Ctrl Pts',(2.62970543174727,12.9869605731601,0.585805638639229));
#7397=CARTESIAN_POINT('Ctrl Pts',(2.3070971603953,13.1952939064935,1.20399045962738));
#7398=CARTESIAN_POINT('Ctrl Pts',(1.98448888904339,13.4036272398268,1.82217528061536));
#7399=CARTESIAN_POINT('Ctrl Pts',(1.39600952008758,13.6119605731601,2.19623490414906));
#7400=CARTESIAN_POINT('Ctrl Pts',(0.807530151131806,13.8202939064935,2.57029452768263));
#7401=CARTESIAN_POINT('Ctrl Pts',(0.110862256246242,14.0286272398268,2.59999997971497));
#7402=CARTESIAN_POINT('Ctrl Pts',(-0.585805638639299,14.2369605731602,2.62970543174722));
#7403=CARTESIAN_POINT('Ctrl Pts',(-1.20399045962738,14.4452939064935,2.30709716039531));
#7404=CARTESIAN_POINT('Ctrl Pts',(-1.82217528061545,14.6536272398268,1.9844888890433));
#7405=CARTESIAN_POINT('Ctrl Pts',(-2.19623490414908,14.8619605731602,1.39600952008751));
#7406=CARTESIAN_POINT('Ctrl Pts',(-2.57029452768271,15.0702939064935,0.807530151131736));
#7407=CARTESIAN_POINT('Ctrl Pts',(-2.59999997971498,15.2786272398268,0.110862256246242));
#7408=CARTESIAN_POINT('Ctrl Pts',(-2.62970543174723,15.4869605731602,-0.585805638639412));
#7409=CARTESIAN_POINT('Ctrl Pts',(-2.30709716039532,15.6952939064935,-1.20399045962746));
#7410=CARTESIAN_POINT('Ctrl Pts',(-1.98448888904338,15.9036272398268,-1.82217528061553));
#7411=CARTESIAN_POINT('Ctrl Pts',(-1.39600952008762,16.1119605731601,-2.19623490414907));
#7412=CARTESIAN_POINT('Ctrl Pts',(-0.807530151131785,16.3202939064935,-2.57029452768285));
#7413=CARTESIAN_POINT('Ctrl Pts',(-0.110862256246242,16.5286272398268,-2.59999997971506));
#7414=CARTESIAN_POINT('Ctrl Pts',(0.585805638639345,16.7369605731602,-2.62970543174732));
#7415=CARTESIAN_POINT('Ctrl Pts',(1.20399045962736,16.9452939064935,-2.3070971603954));
#7416=CARTESIAN_POINT('Ctrl Pts',(1.82217528061547,17.1536272398268,-1.98448888904346));
#7417=CARTESIAN_POINT('Ctrl Pts',(2.19623490414905,17.3619605731602,-1.3960095200876));
#7418=CARTESIAN_POINT('Ctrl Pts',(2.57029452768272,17.5702939064935,-0.807530151131855));
#7419=CARTESIAN_POINT('Ctrl Pts',(2.59999997971496,17.7786272398268,-0.110862256246237));
#7420=CARTESIAN_POINT('Ctrl Pts',(2.62970543174727,17.9869605731602,0.58580563863925));
#7421=CARTESIAN_POINT('Ctrl Pts',(2.3070971603953,18.1952939064935,1.20399045962738));
#7422=CARTESIAN_POINT('Ctrl Pts',(1.98448888904339,18.4036272398268,1.82217528061535));
#7423=CARTESIAN_POINT('Ctrl Pts',(1.39600952008758,18.6119605731602,2.19623490414907));
#7424=CARTESIAN_POINT('Ctrl Pts',(0.807530151131809,18.8202939064935,2.57029452768262));
#7425=CARTESIAN_POINT('Ctrl Pts',(0.110862256246222,19.0286272398268,2.59999997971497));
#7426=CARTESIAN_POINT('Ctrl Pts',(-0.58580563863932,19.2369605731602,2.62970543174719));
#7427=CARTESIAN_POINT('Ctrl Pts',(-1.2039904596274,19.4452939064935,2.30709716039531));
#7428=CARTESIAN_POINT('Ctrl Pts',(-1.82217528061545,19.6536272398268,1.98448888904328));
#7429=CARTESIAN_POINT('Ctrl Pts',(-2.1962349041491,19.8619605731602,1.39600952008757));
#7430=CARTESIAN_POINT('Ctrl Pts',(-2.57029452768269,20.0702939064935,0.807530151131736));
#7431=CARTESIAN_POINT('Ctrl Pts',(-2.59999997971498,20.2786272398269,0.110862256246232));
#7432=CARTESIAN_POINT('Ctrl Pts',(-2.62970543174724,20.4869605731602,-0.58580563863938));
#7433=CARTESIAN_POINT('Ctrl Pts',(-2.30709716039534,20.6952939064935,-1.20399045962747));
#7434=CARTESIAN_POINT('Ctrl Pts',(-1.98448888904338,20.9036272398268,-1.82217528061549));
#7435=CARTESIAN_POINT('Ctrl Pts',(-1.3960095200876,21.1119605731601,-2.19623490414907));
#7436=CARTESIAN_POINT('Ctrl Pts',(-0.807530151131806,21.3202939064935,-2.5702945276828));
#7437=CARTESIAN_POINT('Ctrl Pts',(-0.110862256246263,21.5286272398268,-2.59999997971503));
#7438=CARTESIAN_POINT('Ctrl Pts',(0.585805638639342,21.7369605731602,-2.62970543174737));
#7439=CARTESIAN_POINT('Ctrl Pts',(1.20399045962736,21.9452939064935,-2.3070971603954));
#7440=CARTESIAN_POINT('Ctrl Pts',(1.82217528061545,22.1536272398268,-1.98448888904342));
#7441=CARTESIAN_POINT('Ctrl Pts',(2.19623490414905,22.3619605731602,-1.39600952008764));
#7442=CARTESIAN_POINT('Ctrl Pts',(2.57029452768271,22.5702939064935,-0.807530151131882));
#7443=CARTESIAN_POINT('Ctrl Pts',(2.59999997971498,22.7786272398268,-0.110862256246242));
#7444=CARTESIAN_POINT('Ctrl Pts',(2.62970543174725,22.9869605731602,0.585805638639224));
#7445=CARTESIAN_POINT('Ctrl Pts',(2.30709716039531,23.1952939064935,1.20399045962736));
#7446=CARTESIAN_POINT('Ctrl Pts',(1.98448888904341,23.4036272398269,1.82217528061539));
#7447=CARTESIAN_POINT('Ctrl Pts',(1.39600952008758,23.6119605731602,2.19623490414907));
#7448=CARTESIAN_POINT('Ctrl Pts',(0.807530151131828,23.8202939064935,2.57029452768264));
#7449=CARTESIAN_POINT('Ctrl Pts',(0.110862256246222,24.0286272398268,2.59999997971497));
#7450=CARTESIAN_POINT('Ctrl Pts',(-0.585805638639299,24.2369605731602,2.62970543174718));
#7451=CARTESIAN_POINT('Ctrl Pts',(-1.2039904596274,24.4452939064935,2.30709716039532));
#7452=CARTESIAN_POINT('Ctrl Pts',(-1.82217528061544,24.6536272398269,1.9844888890433));
#7453=CARTESIAN_POINT('Ctrl Pts',(-2.19623490414908,24.8619605731602,1.39600952008758));
#7454=CARTESIAN_POINT('Ctrl Pts',(-2.5702945276827,25.0702939064935,0.807530151131763));
#7455=CARTESIAN_POINT('Ctrl Pts',(-2.59999997971498,25.2786272398269,0.110862256246232));
#7456=CARTESIAN_POINT('Ctrl Pts',(-2.62970543174725,25.4869605731602,-0.58580563863938));
#7457=CARTESIAN_POINT('Ctrl Pts',(-2.30709716039532,25.6952939064935,-1.20399045962744));
#7458=CARTESIAN_POINT('Ctrl Pts',(-1.98448888904338,25.9036272398269,-1.82217528061553));
#7459=CARTESIAN_POINT('Ctrl Pts',(-1.39600952008761,26.1119605731602,-2.19623490414911));
#7460=CARTESIAN_POINT('Ctrl Pts',(-0.807530151131806,26.3202939064935,-2.57029452768279));
#7461=CARTESIAN_POINT('Ctrl Pts',(-0.110862256246242,26.5286272398269,-2.59999997971503));
#7462=CARTESIAN_POINT('Ctrl Pts',(0.585805638639323,26.7369605731602,-2.62970543174736));
#7463=CARTESIAN_POINT('Ctrl Pts',(1.20399045962738,26.9452939064935,-2.30709716039544));
#7464=CARTESIAN_POINT('Ctrl Pts',(1.82217528061545,27.1536272398269,-1.98448888904342));
#7465=CARTESIAN_POINT('Ctrl Pts',(2.19623490414907,27.3619605731602,-1.39600952008769));
#7466=CARTESIAN_POINT('Ctrl Pts',(2.5702945276827,27.5702939064935,-0.807530151131893));
#7467=CARTESIAN_POINT('Ctrl Pts',(2.59999997971496,27.7786272398269,-0.110862256246331));
#7468=CARTESIAN_POINT('Ctrl Pts',(2.62970543174725,27.9869605731602,0.58580563863925));
#7469=CARTESIAN_POINT('Ctrl Pts',(2.30709716039531,28.1952939064935,1.20399045962735));
#7470=CARTESIAN_POINT('Ctrl Pts',(1.98448888904339,28.4036272398269,1.82217528061536));
#7471=CARTESIAN_POINT('Ctrl Pts',(1.39600952008758,28.6119605731601,2.19623490414907));
#7472=CARTESIAN_POINT('Ctrl Pts',(0.807530151131809,28.8202939064936,2.57029452768262));
#7473=CARTESIAN_POINT('Ctrl Pts',(0.110862256246242,29.0286272398268,2.59999997971497));
#7474=CARTESIAN_POINT('Ctrl Pts',(-0.58580563863932,29.2369605731602,2.6297054317472));
#7475=CARTESIAN_POINT('Ctrl Pts',(-1.2039904596274,29.4452939064935,2.30709716039532));
#7476=CARTESIAN_POINT('Ctrl Pts',(-1.82217528061545,29.6536272398269,1.98448888904329));
#7477=CARTESIAN_POINT('Ctrl Pts',(-2.19623490414908,29.8619605731602,1.39600952008757));
#7478=CARTESIAN_POINT('Ctrl Pts',(-2.5702945276827,30.0702939064936,0.807530151131736));
#7479=CARTESIAN_POINT('Ctrl Pts',(-2.59999997971498,30.2786272398269,0.110862256246195));
#7480=CARTESIAN_POINT('Ctrl Pts',(-2.62970543174725,30.4869605731602,-0.585805638639385));
#7481=CARTESIAN_POINT('Ctrl Pts',(-2.30709716039534,30.6952939064935,-1.20399045962744));
#7482=CARTESIAN_POINT('Ctrl Pts',(-1.98448888904338,30.9036272398269,-1.82217528061551));
#7483=CARTESIAN_POINT('Ctrl Pts',(-1.3960095200876,31.1119605731602,-2.19623490414911));
#7484=CARTESIAN_POINT('Ctrl Pts',(-0.807530151131806,31.3202939064935,-2.57029452768284));
#7485=CARTESIAN_POINT('Ctrl Pts',(-0.110862256246242,31.5286272398269,-2.59999997971504));
#7486=CARTESIAN_POINT('Ctrl Pts',(0.585805638639323,31.7369605731602,-2.62970543174734));
#7487=CARTESIAN_POINT('Ctrl Pts',(1.20399045962736,31.9452939064936,-2.30709716039543));
#7488=CARTESIAN_POINT('Ctrl Pts',(1.82217528061545,32.1536272398269,-1.98448888904345));
#7489=CARTESIAN_POINT('Ctrl Pts',(2.19623490414904,32.3619605731602,-1.39600952008769));
#7490=CARTESIAN_POINT('Ctrl Pts',(2.57029452768271,32.5702939064935,-0.807530151131882));
#7491=CARTESIAN_POINT('Ctrl Pts',(2.59999997971498,32.7786272398269,-0.110862256246289));
#7492=CARTESIAN_POINT('Ctrl Pts',(2.62970543174725,32.9869605731603,0.585805638639218));
#7493=CARTESIAN_POINT('Ctrl Pts',(2.30709716039531,33.1952939064935,1.20399045962734));
#7494=CARTESIAN_POINT('Ctrl Pts',(1.98448888904338,33.4036272398269,1.82217528061539));
#7495=CARTESIAN_POINT('Ctrl Pts',(1.3960095200876,33.6119605731602,2.19623490414906));
#7496=CARTESIAN_POINT('Ctrl Pts',(0.807530151131828,33.8202939064936,2.57029452768264));
#7497=CARTESIAN_POINT('Ctrl Pts',(0.110862256246222,34.0286272398269,2.59999997971497));
#7498=CARTESIAN_POINT('Ctrl Pts',(-0.585805638639323,34.2369605731602,2.62970543174719));
#7499=CARTESIAN_POINT('Ctrl Pts',(-1.2039904596274,34.4452939064935,2.30709716039531));
#7500=CARTESIAN_POINT('Ctrl Pts',(-1.82217528061545,34.6536272398269,1.9844888890433));
#7501=CARTESIAN_POINT('Ctrl Pts',(-2.1962349041491,34.8619605731602,1.39600952008757));
#7502=CARTESIAN_POINT('Ctrl Pts',(-2.5702945276827,35.0702939064936,0.807530151131747));
#7503=CARTESIAN_POINT('Ctrl Pts',(-2.59999997971498,35.2786272398269,0.110862256246206));
#7504=CARTESIAN_POINT('Ctrl Pts',(-2.62970543174723,35.4869605731602,-0.585805638639401));
#7505=CARTESIAN_POINT('Ctrl Pts',(-2.30709716039534,35.6952939064935,-1.20399045962745));
#7506=CARTESIAN_POINT('Ctrl Pts',(-1.98448888904336,35.9036272398269,-1.82217528061553));
#7507=CARTESIAN_POINT('Ctrl Pts',(-1.3960095200876,36.1119605731602,-2.19623490414911));
#7508=CARTESIAN_POINT('Ctrl Pts',(-0.807530151131785,36.3202939064935,-2.5702945276828));
#7509=CARTESIAN_POINT('Ctrl Pts',(-0.110862256246263,36.5286272398269,-2.59999997971503));
#7510=CARTESIAN_POINT('Ctrl Pts',(0.585805638639323,36.7369605731602,-2.62970543174736));
#7511=CARTESIAN_POINT('Ctrl Pts',(1.20399045962738,36.9452939064935,-2.30709716039542));
#7512=CARTESIAN_POINT('Ctrl Pts',(1.82217528061547,37.1536272398269,-1.98448888904344));
#7513=CARTESIAN_POINT('Ctrl Pts',(2.19623490414907,37.3619605731602,-1.39600952008768));
#7514=CARTESIAN_POINT('Ctrl Pts',(2.57029452768271,37.5702939064935,-0.807530151131898));
#7515=CARTESIAN_POINT('Ctrl Pts',(2.59999997971498,37.7786272398269,-0.110862256246305));
#7516=CARTESIAN_POINT('Ctrl Pts',(2.62970543174725,37.9869605731602,0.585805638639256));
#7517=CARTESIAN_POINT('Ctrl Pts',(2.30709716039532,38.1952939064936,1.20399045962733));
#7518=CARTESIAN_POINT('Ctrl Pts',(1.98448888904339,38.4036272398269,1.82217528061537));
#7519=CARTESIAN_POINT('Ctrl Pts',(1.3960095200876,38.6119605731602,2.19623490414906));
#7520=CARTESIAN_POINT('Ctrl Pts',(0.807530151131828,38.8202939064936,2.57029452768263));
#7521=CARTESIAN_POINT('Ctrl Pts',(0.110862256246222,39.0286272398269,2.59999997971497));
#7522=CARTESIAN_POINT('Ctrl Pts',(-0.58580563863932,39.2369605731602,2.62970543174721));
#7523=CARTESIAN_POINT('Ctrl Pts',(-1.2039904596274,39.4452939064936,2.30709716039531));
#7524=CARTESIAN_POINT('Ctrl Pts',(-1.82217528061542,39.6536272398269,1.98448888904328));
#7525=CARTESIAN_POINT('Ctrl Pts',(-2.19623490414908,39.8619605731602,1.39600952008758));
#7526=CARTESIAN_POINT('Ctrl Pts',(-2.5702945276827,40.0702939064936,0.807530151131726));
#7527=CARTESIAN_POINT('Ctrl Pts',(-2.59999997971498,40.2786272398269,0.110862256246201));
#7528=CARTESIAN_POINT('Ctrl Pts',(-2.00006370137914,0.278745603789511,0.110909351770506));
#7529=CARTESIAN_POINT('Ctrl Pts',(-2.02978177261913,0.487078937122742,-0.425006101824765));
#7530=CARTESIAN_POINT('Ctrl Pts',(-1.78756065046676,0.695412270456132,-0.903981534539017));
#7531=CARTESIAN_POINT('Ctrl Pts',(-1.5453395283144,0.903745603789377,-1.38295696725319));
#7532=CARTESIAN_POINT('Ctrl Pts',(-1.09608216684017,1.11207893712281,-1.67665129869622));
#7533=CARTESIAN_POINT('Ctrl Pts',(-0.646824805365941,1.32041227045615,-1.97034563013915));
#7534=CARTESIAN_POINT('Ctrl Pts',(-0.110909351770586,1.52874560378948,-2.00006370137914));
#7535=CARTESIAN_POINT('Ctrl Pts',(0.425006101824744,1.73707893712275,-2.02978177261916));
#7536=CARTESIAN_POINT('Ctrl Pts',(0.903981534538964,1.94541227045615,-1.78756065046677));
#7537=CARTESIAN_POINT('Ctrl Pts',(1.38295696725319,2.15374560378948,-1.5453395283144));
#7538=CARTESIAN_POINT('Ctrl Pts',(1.67665129869617,2.36207893712281,-1.09608216684018));
#7539=CARTESIAN_POINT('Ctrl Pts',(1.97034563013914,2.57041227045613,-0.646824805365955));
#7540=CARTESIAN_POINT('Ctrl Pts',(2.00006370137916,2.77874560378949,-0.110909351770603));
#7541=CARTESIAN_POINT('Ctrl Pts',(2.02978177261913,2.98707893712281,0.425006101824722));
#7542=CARTESIAN_POINT('Ctrl Pts',(1.78756065046677,3.19541227045615,0.903981534538913));
#7543=CARTESIAN_POINT('Ctrl Pts',(1.5453395283144,3.40374560378943,1.38295696725317));
#7544=CARTESIAN_POINT('Ctrl Pts',(1.09608216684017,3.61207893712282,1.67665129869616));
#7545=CARTESIAN_POINT('Ctrl Pts',(0.646824805365943,3.8204122704561,1.97034563013913));
#7546=CARTESIAN_POINT('Ctrl Pts',(0.1109093517706,4.02874560378949,2.00006370137908));
#7547=CARTESIAN_POINT('Ctrl Pts',(-0.425006101824727,4.23707893712277,2.02978177261911));
#7548=CARTESIAN_POINT('Ctrl Pts',(-0.903981534538964,4.44541227045615,1.78756065046676));
#7549=CARTESIAN_POINT('Ctrl Pts',(-1.38295696725319,4.65374560378948,1.54533952831435));
#7550=CARTESIAN_POINT('Ctrl Pts',(-1.67665129869618,4.86207893712285,1.09608216684011));
#7551=CARTESIAN_POINT('Ctrl Pts',(-1.97034563013914,5.07041227045609,0.646824805365927));
#7552=CARTESIAN_POINT('Ctrl Pts',(-2.00006370137914,5.27874560378947,0.110909351770506));
#7553=CARTESIAN_POINT('Ctrl Pts',(-2.02978177261913,5.48707893712276,-0.425006101824808));
#7554=CARTESIAN_POINT('Ctrl Pts',(-1.78756065046676,5.69541227045614,-0.903981534539017));
#7555=CARTESIAN_POINT('Ctrl Pts',(-1.5453395283144,5.90374560378943,-1.38295696725317));
#7556=CARTESIAN_POINT('Ctrl Pts',(-1.09608216684016,6.11207893712282,-1.67665129869616));
#7557=CARTESIAN_POINT('Ctrl Pts',(-0.646824805365928,6.32041227045614,-1.97034563013915));
#7558=CARTESIAN_POINT('Ctrl Pts',(-0.110909351770598,6.52874560378952,-2.00006370137919));
#7559=CARTESIAN_POINT('Ctrl Pts',(0.425006101824742,6.73707893712276,-2.02978177261914));
#7560=CARTESIAN_POINT('Ctrl Pts',(0.903981534538965,6.94541227045619,-1.78756065046677));
#7561=CARTESIAN_POINT('Ctrl Pts',(1.3829569672532,7.15374560378946,-1.54533952831446));
#7562=CARTESIAN_POINT('Ctrl Pts',(1.67665129869614,7.36207893712281,-1.09608216684023));
#7563=CARTESIAN_POINT('Ctrl Pts',(1.97034563013915,7.57041227045615,-0.646824805365941));
#7564=CARTESIAN_POINT('Ctrl Pts',(2.00006370137914,7.77874560378953,-0.11090935177061));
#7565=CARTESIAN_POINT('Ctrl Pts',(2.02978177261913,7.98707893712276,0.425006101824722));
#7566=CARTESIAN_POINT('Ctrl Pts',(1.78756065046677,8.19541227045616,0.903981534538955));
#7567=CARTESIAN_POINT('Ctrl Pts',(1.54533952831442,8.40374560378946,1.38295696725319));
#7568=CARTESIAN_POINT('Ctrl Pts',(1.09608216684017,8.61207893712284,1.67665129869611));
#7569=CARTESIAN_POINT('Ctrl Pts',(0.646824805365943,8.82041227045615,1.97034563013914));
#7570=CARTESIAN_POINT('Ctrl Pts',(0.110909351770597,9.0287456037895,2.00006370137908));
#7571=CARTESIAN_POINT('Ctrl Pts',(-0.42500610182474,9.23707893712282,2.02978177261913));
#7572=CARTESIAN_POINT('Ctrl Pts',(-0.903981534538962,9.44541227045615,1.78756065046671));
#7573=CARTESIAN_POINT('Ctrl Pts',(-1.38295696725319,9.65374560378948,1.5453395283144));
#7574=CARTESIAN_POINT('Ctrl Pts',(-1.67665129869616,9.86207893712282,1.09608216684017));
#7575=CARTESIAN_POINT('Ctrl Pts',(-1.97034563013914,10.0704122704562,0.646824805365941));
#7576=CARTESIAN_POINT('Ctrl Pts',(-2.00006370137912,10.2787456037895,0.110909351770534));
#7577=CARTESIAN_POINT('Ctrl Pts',(-2.02978177261913,10.4870789371228,-0.425006101824744));
#7578=CARTESIAN_POINT('Ctrl Pts',(-1.78756065046676,10.6954122704562,-0.903981534539066));
#7579=CARTESIAN_POINT('Ctrl Pts',(-1.5453395283144,10.9037456037894,-1.3829569672532));
#7580=CARTESIAN_POINT('Ctrl Pts',(-1.09608216684017,11.1120789371228,-1.67665129869622));
#7581=CARTESIAN_POINT('Ctrl Pts',(-0.646824805365941,11.3204122704561,-1.97034563013915));
#7582=CARTESIAN_POINT('Ctrl Pts',(-0.1109093517706,11.5287456037895,-2.00006370137916));
#7583=CARTESIAN_POINT('Ctrl Pts',(0.425006101824742,11.7370789371228,-2.02978177261915));
#7584=CARTESIAN_POINT('Ctrl Pts',(0.903981534538964,11.9454122704562,-1.78756065046677));
#7585=CARTESIAN_POINT('Ctrl Pts',(1.38295696725319,12.1537456037895,-1.54533952831446));
#7586=CARTESIAN_POINT('Ctrl Pts',(1.67665129869616,12.3620789371228,-1.09608216684018));
#7587=CARTESIAN_POINT('Ctrl Pts',(1.97034563013917,12.5704122704561,-0.646824805365955));
#7588=CARTESIAN_POINT('Ctrl Pts',(2.00006370137914,12.7787456037895,-0.110909351770652));
#7589=CARTESIAN_POINT('Ctrl Pts',(2.02978177261913,12.9870789371228,0.425006101824744));
#7590=CARTESIAN_POINT('Ctrl Pts',(1.78756065046676,13.1954122704562,0.903981534538906));
#7591=CARTESIAN_POINT('Ctrl Pts',(1.5453395283144,13.4037456037895,1.38295696725318));
#7592=CARTESIAN_POINT('Ctrl Pts',(1.09608216684017,13.6120789371228,1.67665129869616));
#7593=CARTESIAN_POINT('Ctrl Pts',(0.646824805365943,13.8204122704562,1.97034563013915));
#7594=CARTESIAN_POINT('Ctrl Pts',(0.1109093517706,14.0287456037895,2.0000637013791));
#7595=CARTESIAN_POINT('Ctrl Pts',(-0.425006101824742,14.2370789371228,2.02978177261913));
#7596=CARTESIAN_POINT('Ctrl Pts',(-0.903981534538964,14.4454122704562,1.78756065046667));
#7597=CARTESIAN_POINT('Ctrl Pts',(-1.38295696725319,14.6537456037895,1.54533952831435));
#7598=CARTESIAN_POINT('Ctrl Pts',(-1.67665129869616,14.8620789371229,1.09608216684011));
#7599=CARTESIAN_POINT('Ctrl Pts',(-1.97034563013913,15.0704122704562,0.646824805365955));
#7600=CARTESIAN_POINT('Ctrl Pts',(-2.00006370137914,15.2787456037895,0.110909351770541));
#7601=CARTESIAN_POINT('Ctrl Pts',(-2.02978177261913,15.4870789371228,-0.425006101824851));
#7602=CARTESIAN_POINT('Ctrl Pts',(-1.78756065046676,15.6954122704562,-0.903981534538976));
#7603=CARTESIAN_POINT('Ctrl Pts',(-1.5453395283144,15.9037456037895,-1.38295696725319));
#7604=CARTESIAN_POINT('Ctrl Pts',(-1.09608216684016,16.1120789371229,-1.6766512986962));
#7605=CARTESIAN_POINT('Ctrl Pts',(-0.646824805365941,16.3204122704561,-1.9703456301392));
#7606=CARTESIAN_POINT('Ctrl Pts',(-0.1109093517706,16.5287456037895,-2.00006370137919));
#7607=CARTESIAN_POINT('Ctrl Pts',(0.425006101824744,16.7370789371228,-2.02978177261913));
#7608=CARTESIAN_POINT('Ctrl Pts',(0.903981534538977,16.9454122704562,-1.78756065046677));
#7609=CARTESIAN_POINT('Ctrl Pts',(1.38295696725319,17.1537456037895,-1.5453395283144));
#7610=CARTESIAN_POINT('Ctrl Pts',(1.67665129869616,17.3620789371229,-1.09608216684022));
#7611=CARTESIAN_POINT('Ctrl Pts',(1.97034563013914,17.5704122704561,-0.646824805365941));
#7612=CARTESIAN_POINT('Ctrl Pts',(2.00006370137914,17.7787456037895,-0.11090935177061));
#7613=CARTESIAN_POINT('Ctrl Pts',(2.02978177261913,17.9870789371228,0.425006101824686));
#7614=CARTESIAN_POINT('Ctrl Pts',(1.78756065046677,18.1954122704562,0.903981534538948));
#7615=CARTESIAN_POINT('Ctrl Pts',(1.54533952831442,18.4037456037895,1.38295696725319));
#7616=CARTESIAN_POINT('Ctrl Pts',(1.09608216684017,18.6120789371228,1.67665129869611));
#7617=CARTESIAN_POINT('Ctrl Pts',(0.646824805365943,18.8204122704562,1.97034563013914));
#7618=CARTESIAN_POINT('Ctrl Pts',(0.110909351770598,19.0287456037895,2.00006370137909));
#7619=CARTESIAN_POINT('Ctrl Pts',(-0.425006101824742,19.2370789371228,2.02978177261913));
#7620=CARTESIAN_POINT('Ctrl Pts',(-0.903981534538962,19.4454122704562,1.78756065046669));
#7621=CARTESIAN_POINT('Ctrl Pts',(-1.38295696725319,19.6537456037895,1.5453395283144));
#7622=CARTESIAN_POINT('Ctrl Pts',(-1.67665129869616,19.8620789371228,1.09608216684013));
#7623=CARTESIAN_POINT('Ctrl Pts',(-1.97034563013915,20.0704122704561,0.646824805365941));
#7624=CARTESIAN_POINT('Ctrl Pts',(-2.00006370137912,20.2787456037895,0.110909351770513));
#7625=CARTESIAN_POINT('Ctrl Pts',(-2.02978177261911,20.4870789371228,-0.425006101824801));
#7626=CARTESIAN_POINT('Ctrl Pts',(-1.78756065046676,20.6954122704562,-0.903981534539024));
#7627=CARTESIAN_POINT('Ctrl Pts',(-1.54533952831439,20.9037456037895,-1.38295696725322));
#7628=CARTESIAN_POINT('Ctrl Pts',(-1.09608216684018,21.1120789371229,-1.67665129869622));
#7629=CARTESIAN_POINT('Ctrl Pts',(-0.646824805365943,21.3204122704561,-1.97034563013915));
#7630=CARTESIAN_POINT('Ctrl Pts',(-0.1109093517706,21.5287456037895,-2.00006370137914));
#7631=CARTESIAN_POINT('Ctrl Pts',(0.425006101824742,21.7370789371228,-2.02978177261912));
#7632=CARTESIAN_POINT('Ctrl Pts',(0.903981534538964,21.9454122704562,-1.7875606504668));
#7633=CARTESIAN_POINT('Ctrl Pts',(1.38295696725319,22.1537456037895,-1.54533952831446));
#7634=CARTESIAN_POINT('Ctrl Pts',(1.67665129869617,22.3620789371229,-1.09608216684019));
#7635=CARTESIAN_POINT('Ctrl Pts',(1.97034563013912,22.5704122704561,-0.646824805365941));
#7636=CARTESIAN_POINT('Ctrl Pts',(2.00006370137914,22.7787456037895,-0.110909351770638));
#7637=CARTESIAN_POINT('Ctrl Pts',(2.02978177261915,22.9870789371228,0.425006101824744));
#7638=CARTESIAN_POINT('Ctrl Pts',(1.78756065046677,23.1954122704562,0.903981534538906));
#7639=CARTESIAN_POINT('Ctrl Pts',(1.5453395283144,23.4037456037895,1.38295696725318));
#7640=CARTESIAN_POINT('Ctrl Pts',(1.09608216684017,23.6120789371229,1.67665129869614));
#7641=CARTESIAN_POINT('Ctrl Pts',(0.646824805365957,23.8204122704561,1.97034563013915));
#7642=CARTESIAN_POINT('Ctrl Pts',(0.1109093517706,24.0287456037895,2.00006370137905));
#7643=CARTESIAN_POINT('Ctrl Pts',(-0.425006101824742,24.2370789371228,2.02978177261914));
#7644=CARTESIAN_POINT('Ctrl Pts',(-0.903981534538964,24.4454122704562,1.78756065046667));
#7645=CARTESIAN_POINT('Ctrl Pts',(-1.38295696725317,24.6537456037895,1.54533952831433));
#7646=CARTESIAN_POINT('Ctrl Pts',(-1.67665129869615,24.8620789371229,1.09608216684012));
#7647=CARTESIAN_POINT('Ctrl Pts',(-1.97034563013914,25.0704122704562,0.646824805365955));
#7648=CARTESIAN_POINT('Ctrl Pts',(-2.00006370137914,25.2787456037895,0.110909351770548));
#7649=CARTESIAN_POINT('Ctrl Pts',(-2.02978177261913,25.4870789371228,-0.425006101824772));
#7650=CARTESIAN_POINT('Ctrl Pts',(-1.78756065046676,25.6954122704562,-0.903981534538976));
#7651=CARTESIAN_POINT('Ctrl Pts',(-1.5453395283144,25.9037456037895,-1.38295696725319));
#7652=CARTESIAN_POINT('Ctrl Pts',(-1.09608216684017,26.1120789371229,-1.67665129869619));
#7653=CARTESIAN_POINT('Ctrl Pts',(-0.646824805365941,26.3204122704561,-1.9703456301392));
#7654=CARTESIAN_POINT('Ctrl Pts',(-0.1109093517706,26.5287456037895,-2.00006370137917));
#7655=CARTESIAN_POINT('Ctrl Pts',(0.425006101824756,26.7370789371228,-2.02978177261913));
#7656=CARTESIAN_POINT('Ctrl Pts',(0.903981534538977,26.9454122704562,-1.78756065046682));
#7657=CARTESIAN_POINT('Ctrl Pts',(1.38295696725319,27.1537456037895,-1.5453395283144));
#7658=CARTESIAN_POINT('Ctrl Pts',(1.67665129869614,27.3620789371229,-1.09608216684021));
#7659=CARTESIAN_POINT('Ctrl Pts',(1.97034563013914,27.5704122704562,-0.646824805365969));
#7660=CARTESIAN_POINT('Ctrl Pts',(2.00006370137911,27.7787456037896,-0.110909351770603));
#7661=CARTESIAN_POINT('Ctrl Pts',(2.02978177261913,27.9870789371228,0.425006101824736));
#7662=CARTESIAN_POINT('Ctrl Pts',(1.78756065046677,28.1954122704562,0.903981534538934));
#7663=CARTESIAN_POINT('Ctrl Pts',(1.54533952831439,28.4037456037895,1.38295696725318));
#7664=CARTESIAN_POINT('Ctrl Pts',(1.09608216684017,28.6120789371229,1.67665129869612));
#7665=CARTESIAN_POINT('Ctrl Pts',(0.646824805365943,28.8204122704562,1.97034563013911));
#7666=CARTESIAN_POINT('Ctrl Pts',(0.110909351770614,29.0287456037896,2.0000637013791));
#7667=CARTESIAN_POINT('Ctrl Pts',(-0.425006101824742,29.2370789371228,2.02978177261913));
#7668=CARTESIAN_POINT('Ctrl Pts',(-0.903981534538962,29.4454122704562,1.78756065046671));
#7669=CARTESIAN_POINT('Ctrl Pts',(-1.38295696725319,29.6537456037896,1.54533952831437));
#7670=CARTESIAN_POINT('Ctrl Pts',(-1.67665129869616,29.8620789371229,1.0960821668401));
#7671=CARTESIAN_POINT('Ctrl Pts',(-1.97034563013914,30.0704122704562,0.646824805365912));
#7672=CARTESIAN_POINT('Ctrl Pts',(-2.00006370137914,30.2787456037896,0.110909351770527));
#7673=CARTESIAN_POINT('Ctrl Pts',(-2.02978177261913,30.4870789371228,-0.425006101824801));
#7674=CARTESIAN_POINT('Ctrl Pts',(-1.78756065046675,30.6954122704562,-0.90398153453901));
#7675=CARTESIAN_POINT('Ctrl Pts',(-1.5453395283144,30.9037456037895,-1.38295696725315));
#7676=CARTESIAN_POINT('Ctrl Pts',(-1.09608216684017,31.1120789371229,-1.67665129869622));
#7677=CARTESIAN_POINT('Ctrl Pts',(-0.646824805365941,31.3204122704562,-1.97034563013915));
#7678=CARTESIAN_POINT('Ctrl Pts',(-0.110909351770598,31.5287456037896,-2.00006370137914));
#7679=CARTESIAN_POINT('Ctrl Pts',(0.425006101824744,31.7370789371229,-2.02978177261914));
#7680=CARTESIAN_POINT('Ctrl Pts',(0.903981534538951,31.9454122704562,-1.78756065046679));
#7681=CARTESIAN_POINT('Ctrl Pts',(1.38295696725319,32.1537456037895,-1.54533952831446));
#7682=CARTESIAN_POINT('Ctrl Pts',(1.67665129869616,32.3620789371229,-1.09608216684022));
#7683=CARTESIAN_POINT('Ctrl Pts',(1.97034563013914,32.5704122704561,-0.646824805365941));
#7684=CARTESIAN_POINT('Ctrl Pts',(2.00006370137914,32.7787456037896,-0.11090935177061));
#7685=CARTESIAN_POINT('Ctrl Pts',(2.02978177261913,32.9870789371229,0.425006101824715));
#7686=CARTESIAN_POINT('Ctrl Pts',(1.78756065046676,33.1954122704563,0.903981534538906));
#7687=CARTESIAN_POINT('Ctrl Pts',(1.5453395283144,33.4037456037895,1.3829569672532));
#7688=CARTESIAN_POINT('Ctrl Pts',(1.09608216684017,33.6120789371229,1.67665129869615));
#7689=CARTESIAN_POINT('Ctrl Pts',(0.646824805365943,33.8204122704562,1.97034563013915));
#7690=CARTESIAN_POINT('Ctrl Pts',(0.1109093517706,34.0287456037896,2.00006370137906));
#7691=CARTESIAN_POINT('Ctrl Pts',(-0.425006101824742,34.2370789371229,2.02978177261912));
#7692=CARTESIAN_POINT('Ctrl Pts',(-0.903981534538964,34.4454122704562,1.7875606504667));
#7693=CARTESIAN_POINT('Ctrl Pts',(-1.3829569672532,34.6537456037895,1.54533952831438));
#7694=CARTESIAN_POINT('Ctrl Pts',(-1.67665129869615,34.8620789371228,1.09608216684013));
#7695=CARTESIAN_POINT('Ctrl Pts',(-1.97034563013914,35.0704122704562,0.646824805365955));
#7696=CARTESIAN_POINT('Ctrl Pts',(-2.00006370137914,35.2787456037896,0.110909351770548));
#7697=CARTESIAN_POINT('Ctrl Pts',(-2.02978177261913,35.4870789371229,-0.425006101824787));
#7698=CARTESIAN_POINT('Ctrl Pts',(-1.78756065046676,35.6954122704562,-0.903981534538996));
#7699=CARTESIAN_POINT('Ctrl Pts',(-1.5453395283144,35.9037456037895,-1.3829569672532));
#7700=CARTESIAN_POINT('Ctrl Pts',(-1.09608216684017,36.1120789371229,-1.67665129869619));
#7701=CARTESIAN_POINT('Ctrl Pts',(-0.646824805365928,36.3204122704562,-1.97034563013915));
#7702=CARTESIAN_POINT('Ctrl Pts',(-0.1109093517706,36.5287456037896,-2.00006370137918));
#7703=CARTESIAN_POINT('Ctrl Pts',(0.425006101824742,36.7370789371229,-2.02978177261914));
#7704=CARTESIAN_POINT('Ctrl Pts',(0.903981534538964,36.9454122704562,-1.78756065046682));
#7705=CARTESIAN_POINT('Ctrl Pts',(1.38295696725319,37.1537456037895,-1.5453395283144));
#7706=CARTESIAN_POINT('Ctrl Pts',(1.67665129869617,37.3620789371229,-1.09608216684022));
#7707=CARTESIAN_POINT('Ctrl Pts',(1.97034563013915,37.5704122704562,-0.646824805365941));
#7708=CARTESIAN_POINT('Ctrl Pts',(2.00006370137914,37.7787456037895,-0.110909351770645));
#7709=CARTESIAN_POINT('Ctrl Pts',(2.02978177261915,37.9870789371229,0.425006101824736));
#7710=CARTESIAN_POINT('Ctrl Pts',(1.78756065046677,38.1954122704563,0.90398153453892));
#7711=CARTESIAN_POINT('Ctrl Pts',(1.5453395283144,38.4037456037895,1.38295696725319));
#7712=CARTESIAN_POINT('Ctrl Pts',(1.09608216684019,38.6120789371229,1.67665129869612));
#7713=CARTESIAN_POINT('Ctrl Pts',(0.646824805365943,38.8204122704562,1.97034563013916));
#7714=CARTESIAN_POINT('Ctrl Pts',(0.110909351770614,39.0287456037896,2.0000637013791));
#7715=CARTESIAN_POINT('Ctrl Pts',(-0.425006101824727,39.2370789371229,2.02978177261914));
#7716=CARTESIAN_POINT('Ctrl Pts',(-0.90398153453895,39.4454122704563,1.78756065046672));
#7717=CARTESIAN_POINT('Ctrl Pts',(-1.38295696725319,39.6537456037896,1.54533952831436));
#7718=CARTESIAN_POINT('Ctrl Pts',(-1.67665129869616,39.8620789371229,1.09608216684011));
#7719=CARTESIAN_POINT('Ctrl Pts',(-1.97034563013914,40.0704122704562,0.646824805365955));
#7720=CARTESIAN_POINT('Ctrl Pts',(-2.00006370137914,40.2787456037896,0.110909351770527));
#7721=CARTESIAN_POINT('',(-2.,-0.278745610073463,-0.11090935427092));
#7722=CARTESIAN_POINT('Origin',(-2.,-2.08166817117217E-14,-3.46944695195361E-14));
#7723=CARTESIAN_POINT('',(-2.,39.7212543899267,-0.110909354270961));
#7724=CARTESIAN_POINT('Ctrl Pts',(-2.,-0.278745610073463,-0.11090935427092));
#7725=CARTESIAN_POINT('Ctrl Pts',(-1.97028192809006,-0.0704122767402083,
-0.646807739133109));
#7726=CARTESIAN_POINT('Ctrl Pts',(-1.67659613043344,0.137921056593222,-1.0960503183159));
#7727=CARTESIAN_POINT('Ctrl Pts',(-1.38291033277683,0.346254389926512,-1.54529289749873));
#7728=CARTESIAN_POINT('Ctrl Pts',(-0.903949681684104,0.554587723259871,
-1.78750548470438));
#7729=CARTESIAN_POINT('Ctrl Pts',(-0.424989030591367,0.762921056593226,
-2.02971807190993));
#7730=CARTESIAN_POINT('Ctrl Pts',(0.110909354270878,0.971254389926561,-2.00000000000006));
#7731=CARTESIAN_POINT('Ctrl Pts',(0.646807739133123,1.17958772325984,-1.97028192809007));
#7732=CARTESIAN_POINT('Ctrl Pts',(1.09605031831591,1.38792105659322,-1.67659613043344));
#7733=CARTESIAN_POINT('Ctrl Pts',(1.54529289749868,1.59625438992652,-1.38291033277687));
#7734=CARTESIAN_POINT('Ctrl Pts',(1.78750548470428,1.80458772325989,-0.903949681684113));
#7735=CARTESIAN_POINT('Ctrl Pts',(2.02971807190996,2.01292105659317,-0.424989030591391));
#7736=CARTESIAN_POINT('Ctrl Pts',(2.,2.22125438992656,0.110909354270855));
#7737=CARTESIAN_POINT('Ctrl Pts',(1.97028192809007,2.42958772325984,0.646807739133102));
#7738=CARTESIAN_POINT('Ctrl Pts',(1.67659613043345,2.63792105659317,1.09605031831587));
#7739=CARTESIAN_POINT('Ctrl Pts',(1.38291033277683,2.8462543899265,1.54529289749866));
#7740=CARTESIAN_POINT('Ctrl Pts',(0.903949681684104,3.0545877232599,1.78750548470426));
#7741=CARTESIAN_POINT('Ctrl Pts',(0.424989030591383,3.26292105659317,2.02971807190993));
#7742=CARTESIAN_POINT('Ctrl Pts',(-0.11090935427085,3.47125438992654,1.99999999999995));
#7743=CARTESIAN_POINT('Ctrl Pts',(-0.646807739133109,3.67958772325983,1.97028192809007));
#7744=CARTESIAN_POINT('Ctrl Pts',(-1.0960503183159,3.88792105659323,1.67659613043343));
#7745=CARTESIAN_POINT('Ctrl Pts',(-1.54529289749868,4.09625438992648,1.38291033277681));
#7746=CARTESIAN_POINT('Ctrl Pts',(-1.78750548470431,4.30458772325989,0.903949681684051));
#7747=CARTESIAN_POINT('Ctrl Pts',(-2.02971807190994,4.51292105659318,0.424989030591333));
#7748=CARTESIAN_POINT('Ctrl Pts',(-2.,4.72125438992654,-0.110909354270966));
#7749=CARTESIAN_POINT('Ctrl Pts',(-1.97028192809006,4.92958772325984,-0.646807739133087));
#7750=CARTESIAN_POINT('Ctrl Pts',(-1.67659613043343,5.13792105659321,-1.09605031831595));
#7751=CARTESIAN_POINT('Ctrl Pts',(-1.38291033277683,5.34625438992653,-1.54529289749872));
#7752=CARTESIAN_POINT('Ctrl Pts',(-0.903949681684091,5.5545877232599,-1.78750548470436));
#7753=CARTESIAN_POINT('Ctrl Pts',(-0.424989030591382,5.76292105659322,-2.02971807190993));
#7754=CARTESIAN_POINT('Ctrl Pts',(0.110909354270865,5.97125438992659,-2.00000000000009));
#7755=CARTESIAN_POINT('Ctrl Pts',(0.646807739133111,6.17958772325983,-1.97028192809005));
#7756=CARTESIAN_POINT('Ctrl Pts',(1.0960503183159,6.38792105659326,-1.67659613043349));
#7757=CARTESIAN_POINT('Ctrl Pts',(1.54529289749868,6.5962543899265,-1.38291033277683));
#7758=CARTESIAN_POINT('Ctrl Pts',(1.7875054847043,6.80458772325989,-0.903949681684162));
#7759=CARTESIAN_POINT('Ctrl Pts',(2.02971807190991,7.01292105659322,-0.424989030591398));
#7760=CARTESIAN_POINT('Ctrl Pts',(2.,7.22125438992656,0.110909354270862));
#7761=CARTESIAN_POINT('Ctrl Pts',(1.97028192809006,7.42958772325989,0.646807739133109));
#7762=CARTESIAN_POINT('Ctrl Pts',(1.67659613043344,7.63792105659322,1.09605031831585));
#7763=CARTESIAN_POINT('Ctrl Pts',(1.38291033277683,7.84625438992656,1.54529289749869));
#7764=CARTESIAN_POINT('Ctrl Pts',(0.903949681684104,8.05458772325989,1.78750548470431));
#7765=CARTESIAN_POINT('Ctrl Pts',(0.424989030591398,8.26292105659318,2.02971807190991));
#7766=CARTESIAN_POINT('Ctrl Pts',(-0.110909354270878,8.47125438992655,1.99999999999995));
#7767=CARTESIAN_POINT('Ctrl Pts',(-0.646807739133123,8.67958772325983,1.97028192809004));
#7768=CARTESIAN_POINT('Ctrl Pts',(-1.0960503183159,8.88792105659324,1.67659613043339));
#7769=CARTESIAN_POINT('Ctrl Pts',(-1.54529289749868,9.0962543899265,1.38291033277683));
#7770=CARTESIAN_POINT('Ctrl Pts',(-1.78750548470431,9.3045877232599,0.903949681684085));
#7771=CARTESIAN_POINT('Ctrl Pts',(-2.02971807190993,9.51292105659317,0.424989030591355));
#7772=CARTESIAN_POINT('Ctrl Pts',(-2.,9.72125438992657,-0.110909354270924));
#7773=CARTESIAN_POINT('Ctrl Pts',(-1.97028192809007,9.92958772325984,-0.646807739133123));
#7774=CARTESIAN_POINT('Ctrl Pts',(-1.67659613043344,10.1379210565932,-1.09605031831599));
#7775=CARTESIAN_POINT('Ctrl Pts',(-1.38291033277681,10.3462543899265,-1.54529289749875));
#7776=CARTESIAN_POINT('Ctrl Pts',(-0.903949681684116,10.5545877232599,-1.78750548470438));
#7777=CARTESIAN_POINT('Ctrl Pts',(-0.424989030591382,10.7629210565932,-2.02971807190998));
#7778=CARTESIAN_POINT('Ctrl Pts',(0.110909354270878,10.9712543899266,-2.00000000000009));
#7779=CARTESIAN_POINT('Ctrl Pts',(0.646807739133123,11.1795877232599,-1.97028192809007));
#7780=CARTESIAN_POINT('Ctrl Pts',(1.09605031831591,11.3879210565932,-1.67659613043351));
#7781=CARTESIAN_POINT('Ctrl Pts',(1.54529289749868,11.5962543899266,-1.38291033277683));
#7782=CARTESIAN_POINT('Ctrl Pts',(1.78750548470431,11.8045877232599,-0.903949681684182));
#7783=CARTESIAN_POINT('Ctrl Pts',(2.02971807190994,12.0129210565932,-0.424989030591383));
#7784=CARTESIAN_POINT('Ctrl Pts',(2.,12.2212543899266,0.110909354270862));
#7785=CARTESIAN_POINT('Ctrl Pts',(1.97028192809007,12.4295877232599,0.646807739133051));
#7786=CARTESIAN_POINT('Ctrl Pts',(1.67659613043345,12.6379210565932,1.09605031831589));
#7787=CARTESIAN_POINT('Ctrl Pts',(1.38291033277683,12.8462543899266,1.54529289749867));
#7788=CARTESIAN_POINT('Ctrl Pts',(0.903949681684118,13.0545877232599,1.78750548470425));
#7789=CARTESIAN_POINT('Ctrl Pts',(0.424989030591382,13.2629210565932,2.02971807190993));
#7790=CARTESIAN_POINT('Ctrl Pts',(-0.110909354270864,13.4712543899266,1.99999999999997));
#7791=CARTESIAN_POINT('Ctrl Pts',(-0.646807739133109,13.6795877232599,1.97028192809006));
#7792=CARTESIAN_POINT('Ctrl Pts',(-1.0960503183159,13.8879210565932,1.67659613043339));
#7793=CARTESIAN_POINT('Ctrl Pts',(-1.54529289749868,14.0962543899266,1.38291033277683));
#7794=CARTESIAN_POINT('Ctrl Pts',(-1.7875054847043,14.3045877232599,0.903949681684092));
#7795=CARTESIAN_POINT('Ctrl Pts',(-2.02971807190994,14.5129210565932,0.424989030591326));
#7796=CARTESIAN_POINT('Ctrl Pts',(-2.,14.7212543899266,-0.110909354270938));
#7797=CARTESIAN_POINT('Ctrl Pts',(-1.97028192809006,14.9295877232599,-0.646807739133109));
#7798=CARTESIAN_POINT('Ctrl Pts',(-1.67659613043344,15.1379210565933,-1.09605031831595));
#7799=CARTESIAN_POINT('Ctrl Pts',(-1.38291033277683,15.3462543899265,-1.54529289749874));
#7800=CARTESIAN_POINT('Ctrl Pts',(-0.903949681684104,15.5545877232599,-1.78750548470439));
#7801=CARTESIAN_POINT('Ctrl Pts',(-0.424989030591382,15.7629210565932,-2.02971807190993));
#7802=CARTESIAN_POINT('Ctrl Pts',(0.110909354270852,15.9712543899266,-2.00000000000006));
#7803=CARTESIAN_POINT('Ctrl Pts',(0.646807739133109,16.1795877232599,-1.97028192809006));
#7804=CARTESIAN_POINT('Ctrl Pts',(1.0960503183159,16.3879210565933,-1.67659613043349));
#7805=CARTESIAN_POINT('Ctrl Pts',(1.5452928974987,16.5962543899265,-1.38291033277688));
#7806=CARTESIAN_POINT('Ctrl Pts',(1.78750548470431,16.8045877232599,-0.903949681684148));
#7807=CARTESIAN_POINT('Ctrl Pts',(2.02971807190994,17.0129210565932,-0.424989030591383));
#7808=CARTESIAN_POINT('Ctrl Pts',(2.,17.2212543899266,0.110909354270813));
#7809=CARTESIAN_POINT('Ctrl Pts',(1.97028192809007,17.4295877232599,0.646807739133109));
#7810=CARTESIAN_POINT('Ctrl Pts',(1.67659613043345,17.6379210565933,1.09605031831585));
#7811=CARTESIAN_POINT('Ctrl Pts',(1.38291033277684,17.8462543899265,1.54529289749865));
#7812=CARTESIAN_POINT('Ctrl Pts',(0.903949681684104,18.0545877232599,1.78750548470431));
#7813=CARTESIAN_POINT('Ctrl Pts',(0.424989030591369,18.2629210565932,2.02971807190994));
#7814=CARTESIAN_POINT('Ctrl Pts',(-0.110909354270865,18.4712543899266,2.));
#7815=CARTESIAN_POINT('Ctrl Pts',(-0.646807739133109,18.6795877232599,1.97028192809006));
#7816=CARTESIAN_POINT('Ctrl Pts',(-1.0960503183159,18.8879210565933,1.6765961304334));
#7817=CARTESIAN_POINT('Ctrl Pts',(-1.54529289749867,19.0962543899266,1.38291033277683));
#7818=CARTESIAN_POINT('Ctrl Pts',(-1.78750548470431,19.3045877232599,0.903949681684071));
#7819=CARTESIAN_POINT('Ctrl Pts',(-2.02971807190993,19.5129210565932,0.42498903059134));
#7820=CARTESIAN_POINT('Ctrl Pts',(-2.,19.7212543899266,-0.110909354270924));
#7821=CARTESIAN_POINT('Ctrl Pts',(-1.97028192809006,19.9295877232599,-0.646807739133152));
#7822=CARTESIAN_POINT('Ctrl Pts',(-1.67659613043345,20.1379210565933,-1.09605031831597));
#7823=CARTESIAN_POINT('Ctrl Pts',(-1.38291033277683,20.3462543899266,-1.54529289749875));
#7824=CARTESIAN_POINT('Ctrl Pts',(-0.903949681684103,20.5545877232599,-1.78750548470438));
#7825=CARTESIAN_POINT('Ctrl Pts',(-0.424989030591367,20.7629210565932,-2.02971807190997));
#7826=CARTESIAN_POINT('Ctrl Pts',(0.110909354270864,20.9712543899266,-2.0000000000001));
#7827=CARTESIAN_POINT('Ctrl Pts',(0.646807739133111,21.1795877232599,-1.97028192809011));
#7828=CARTESIAN_POINT('Ctrl Pts',(1.0960503183159,21.3879210565933,-1.67659613043352));
#7829=CARTESIAN_POINT('Ctrl Pts',(1.54529289749868,21.5962543899266,-1.38291033277683));
#7830=CARTESIAN_POINT('Ctrl Pts',(1.78750548470431,21.8045877232599,-0.90394968168419));
#7831=CARTESIAN_POINT('Ctrl Pts',(2.02971807190991,22.0129210565932,-0.424989030591391));
#7832=CARTESIAN_POINT('Ctrl Pts',(2.,22.2212543899266,0.110909354270855));
#7833=CARTESIAN_POINT('Ctrl Pts',(1.97028192809009,22.4295877232599,0.646807739133087));
#7834=CARTESIAN_POINT('Ctrl Pts',(1.67659613043345,22.6379210565933,1.09605031831588));
#7835=CARTESIAN_POINT('Ctrl Pts',(1.38291033277683,22.8462543899266,1.54529289749862));
#7836=CARTESIAN_POINT('Ctrl Pts',(0.903949681684118,23.0545877232599,1.78750548470426));
#7837=CARTESIAN_POINT('Ctrl Pts',(0.424989030591383,23.2629210565932,2.02971807190993));
#7838=CARTESIAN_POINT('Ctrl Pts',(-0.110909354270864,23.4712543899266,1.99999999999997));
#7839=CARTESIAN_POINT('Ctrl Pts',(-0.646807739133109,23.6795877232599,1.97028192809003));
#7840=CARTESIAN_POINT('Ctrl Pts',(-1.09605031831588,23.8879210565933,1.67659613043339));
#7841=CARTESIAN_POINT('Ctrl Pts',(-1.54529289749869,24.0962543899266,1.38291033277683));
#7842=CARTESIAN_POINT('Ctrl Pts',(-1.78750548470431,24.3045877232599,0.903949681684092));
#7843=CARTESIAN_POINT('Ctrl Pts',(-2.02971807190995,24.5129210565932,0.424989030591319));
#7844=CARTESIAN_POINT('Ctrl Pts',(-2.,24.7212543899266,-0.110909354270938));
#7845=CARTESIAN_POINT('Ctrl Pts',(-1.97028192809005,24.9295877232599,-0.646807739133109));
#7846=CARTESIAN_POINT('Ctrl Pts',(-1.67659613043344,25.1379210565933,-1.09605031831594));
#7847=CARTESIAN_POINT('Ctrl Pts',(-1.38291033277683,25.3462543899266,-1.54529289749872));
#7848=CARTESIAN_POINT('Ctrl Pts',(-0.903949681684104,25.55458772326,-1.7875054847044));
#7849=CARTESIAN_POINT('Ctrl Pts',(-0.424989030591382,25.7629210565933,-2.02971807190993));
#7850=CARTESIAN_POINT('Ctrl Pts',(0.110909354270864,25.9712543899266,-2.00000000000006));
#7851=CARTESIAN_POINT('Ctrl Pts',(0.646807739133109,26.1795877232599,-1.97028192809006));
#7852=CARTESIAN_POINT('Ctrl Pts',(1.0960503183159,26.3879210565933,-1.67659613043348));
#7853=CARTESIAN_POINT('Ctrl Pts',(1.5452928974987,26.5962543899266,-1.38291033277687));
#7854=CARTESIAN_POINT('Ctrl Pts',(1.78750548470431,26.80458772326,-0.903949681684155));
#7855=CARTESIAN_POINT('Ctrl Pts',(2.02971807190994,27.0129210565933,-0.424989030591383));
#7856=CARTESIAN_POINT('Ctrl Pts',(2.00000000000003,27.2212543899266,0.11090935427082));
#7857=CARTESIAN_POINT('Ctrl Pts',(1.97028192809007,27.4295877232599,0.646807739133109));
#7858=CARTESIAN_POINT('Ctrl Pts',(1.67659613043345,27.6379210565933,1.09605031831587));
#7859=CARTESIAN_POINT('Ctrl Pts',(1.38291033277684,27.8462543899266,1.54529289749868));
#7860=CARTESIAN_POINT('Ctrl Pts',(0.903949681684103,28.0545877232599,1.78750548470431));
#7861=CARTESIAN_POINT('Ctrl Pts',(0.424989030591382,28.2629210565932,2.02971807190993));
#7862=CARTESIAN_POINT('Ctrl Pts',(-0.110909354270852,28.4712543899266,1.99999999999998));
#7863=CARTESIAN_POINT('Ctrl Pts',(-0.646807739133109,28.6795877232599,1.97028192809006));
#7864=CARTESIAN_POINT('Ctrl Pts',(-1.0960503183159,28.8879210565933,1.67659613043341));
#7865=CARTESIAN_POINT('Ctrl Pts',(-1.54529289749868,29.0962543899266,1.38291033277683));
#7866=CARTESIAN_POINT('Ctrl Pts',(-1.78750548470432,29.30458772326,0.903949681684071));
#7867=CARTESIAN_POINT('Ctrl Pts',(-2.02971807190994,29.5129210565933,0.42498903059134));
#7868=CARTESIAN_POINT('Ctrl Pts',(-2.,29.7212543899266,-0.110909354270917));
#7869=CARTESIAN_POINT('Ctrl Pts',(-1.97028192809006,29.9295877232599,-0.646807739133087));
#7870=CARTESIAN_POINT('Ctrl Pts',(-1.67659613043345,30.1379210565933,-1.09605031831597));
#7871=CARTESIAN_POINT('Ctrl Pts',(-1.38291033277683,30.3462543899266,-1.54529289749872));
#7872=CARTESIAN_POINT('Ctrl Pts',(-0.903949681684103,30.55458772326,-1.78750548470437));
#7873=CARTESIAN_POINT('Ctrl Pts',(-0.424989030591367,30.7629210565933,-2.02971807190996));
#7874=CARTESIAN_POINT('Ctrl Pts',(0.110909354270865,30.9712543899266,-2.00000000000009));
#7875=CARTESIAN_POINT('Ctrl Pts',(0.646807739133123,31.1795877232599,-1.97028192809004));
#7876=CARTESIAN_POINT('Ctrl Pts',(1.0960503183159,31.3879210565933,-1.67659613043352));
#7877=CARTESIAN_POINT('Ctrl Pts',(1.54529289749868,31.5962543899266,-1.38291033277685));
#7878=CARTESIAN_POINT('Ctrl Pts',(1.78750548470431,31.80458772326,-0.903949681684169));
#7879=CARTESIAN_POINT('Ctrl Pts',(2.02971807190994,32.0129210565933,-0.424989030591419));
#7880=CARTESIAN_POINT('Ctrl Pts',(2.,32.2212543899266,0.110909354270869));
#7881=CARTESIAN_POINT('Ctrl Pts',(1.97028192809004,32.4295877232599,0.646807739133087));
#7882=CARTESIAN_POINT('Ctrl Pts',(1.67659613043345,32.6379210565933,1.09605031831587));
#7883=CARTESIAN_POINT('Ctrl Pts',(1.38291033277683,32.8462543899266,1.54529289749868));
#7884=CARTESIAN_POINT('Ctrl Pts',(0.903949681684104,33.0545877232599,1.78750548470431));
#7885=CARTESIAN_POINT('Ctrl Pts',(0.424989030591383,33.2629210565932,2.02971807190993));
#7886=CARTESIAN_POINT('Ctrl Pts',(-0.110909354270864,33.4712543899267,1.99999999999997));
#7887=CARTESIAN_POINT('Ctrl Pts',(-0.646807739133109,33.6795877232599,1.97028192809004));
#7888=CARTESIAN_POINT('Ctrl Pts',(-1.09605031831588,33.8879210565934,1.6765961304334));
#7889=CARTESIAN_POINT('Ctrl Pts',(-1.54529289749868,34.0962543899266,1.38291033277683));
#7890=CARTESIAN_POINT('Ctrl Pts',(-1.78750548470431,34.30458772326,0.903949681684037));
#7891=CARTESIAN_POINT('Ctrl Pts',(-2.02971807190994,34.5129210565932,0.424989030591383));
#7892=CARTESIAN_POINT('Ctrl Pts',(-2.,34.7212543899267,-0.110909354270938));
#7893=CARTESIAN_POINT('Ctrl Pts',(-1.97028192809006,34.9295877232599,-0.646807739133123));
#7894=CARTESIAN_POINT('Ctrl Pts',(-1.67659613043344,35.1379210565933,-1.09605031831594));
#7895=CARTESIAN_POINT('Ctrl Pts',(-1.38291033277683,35.3462543899267,-1.54529289749875));
#7896=CARTESIAN_POINT('Ctrl Pts',(-0.903949681684103,35.55458772326,-1.78750548470439));
#7897=CARTESIAN_POINT('Ctrl Pts',(-0.424989030591382,35.7629210565932,-2.02971807190993));
#7898=CARTESIAN_POINT('Ctrl Pts',(0.110909354270864,35.9712543899267,-2.00000000000003));
#7899=CARTESIAN_POINT('Ctrl Pts',(0.646807739133111,36.1795877232599,-1.97028192809006));
#7900=CARTESIAN_POINT('Ctrl Pts',(1.0960503183159,36.3879210565933,-1.67659613043348));
#7901=CARTESIAN_POINT('Ctrl Pts',(1.54529289749869,36.5962543899266,-1.38291033277682));
#7902=CARTESIAN_POINT('Ctrl Pts',(1.78750548470431,36.80458772326,-0.903949681684127));
#7903=CARTESIAN_POINT('Ctrl Pts',(2.02971807190994,37.0129210565932,-0.424989030591383));
#7904=CARTESIAN_POINT('Ctrl Pts',(2.,37.2212543899267,0.110909354270834));
#7905=CARTESIAN_POINT('Ctrl Pts',(1.97028192809006,37.4295877232599,0.646807739133109));
#7906=CARTESIAN_POINT('Ctrl Pts',(1.67659613043345,37.6379210565933,1.09605031831588));
#7907=CARTESIAN_POINT('Ctrl Pts',(1.38291033277681,37.8462543899266,1.54529289749865));
#7908=CARTESIAN_POINT('Ctrl Pts',(0.903949681684104,38.0545877232599,1.78750548470431));
#7909=CARTESIAN_POINT('Ctrl Pts',(0.424989030591383,38.2629210565933,2.02971807190991));
#7910=CARTESIAN_POINT('Ctrl Pts',(-0.11090935427085,38.4712543899266,1.99999999999995));
#7911=CARTESIAN_POINT('Ctrl Pts',(-0.646807739133111,38.67958772326,1.97028192809006));
#7912=CARTESIAN_POINT('Ctrl Pts',(-1.0960503183159,38.8879210565933,1.67659613043344));
#7913=CARTESIAN_POINT('Ctrl Pts',(-1.54529289749868,39.0962543899266,1.38291033277682));
#7914=CARTESIAN_POINT('Ctrl Pts',(-1.78750548470431,39.30458772326,0.903949681684064));
#7915=CARTESIAN_POINT('Ctrl Pts',(-2.02971807190993,39.5129210565932,0.424989030591368));
#7916=CARTESIAN_POINT('Ctrl Pts',(-2.,39.7212543899267,-0.110909354270961));
#7917=CARTESIAN_POINT('',(-1.99999999999999,40.2787456100736,0.110909354270809));
#7918=CARTESIAN_POINT('Origin',(-1.99999999999999,40.0000000000001,-7.63278329429795E-14));
#7919=CARTESIAN_POINT('',(-2.00308415717522,0.327811454287795,-0.014474292615955));
#7920=CARTESIAN_POINT('Ctrl Pts',(-2.00308415717522,0.327811454287795,-0.014474292615955));
#7921=CARTESIAN_POINT('Ctrl Pts',(-2.00266941950797,0.3499571598645,-0.0706947258144284));
#7922=CARTESIAN_POINT('Ctrl Pts',(-1.99988284484963,0.37238501496934,-0.127135039387294));
#7923=CARTESIAN_POINT('Ctrl Pts',(-1.99469178463351,0.394978788957426,-0.183493113344122));
#7924=CARTESIAN_POINT('Ctrl Pts',(-1.98950037298493,0.417574092533932,-0.239855002717413));
#7925=CARTESIAN_POINT('Ctrl Pts',(-1.98190404906885,0.440335059872151,-0.296133914952173));
#7926=CARTESIAN_POINT('Ctrl Pts',(-1.97192179180133,0.463139554738375,-0.352023517509166));
#7927=CARTESIAN_POINT('Ctrl Pts',(-1.96194535902849,0.485930743530098,-0.407880509336571));
#7928=CARTESIAN_POINT('Ctrl Pts',(-1.94958586765235,0.508765113065188,-0.463347912701799));
#7929=CARTESIAN_POINT('Ctrl Pts',(-1.93491390431575,0.531519187675631,-0.518126779296725));
#7930=CARTESIAN_POINT('Ctrl Pts',(-1.92022340561799,0.554302007927083,-0.572974849041457));
#7931=CARTESIAN_POINT('Ctrl Pts',(-1.90321484710063,0.577004036127603,-0.627131948034054));
#7932=CARTESIAN_POINT('Ctrl Pts',(-1.88400825633397,0.59950422083275,-0.680315621374878));
#7933=CARTESIAN_POINT('Ctrl Pts',(-1.86482690562689,0.621974837250142,-0.733429404171343));
#7934=CARTESIAN_POINT('Ctrl Pts',(-1.84345373271557,0.64424387424164,-0.785571733351559));
#7935=CARTESIAN_POINT('Ctrl Pts',(-1.82005202898671,0.666197857568301,-0.836488448064752));
#7936=CARTESIAN_POINT('Ctrl Pts',(-1.80960152082968,0.676001856648568,-0.859226345638543));
#7937=CARTESIAN_POINT('Ctrl Pts',(-1.79874701482939,0.68574314488471,-0.88172023997714));
#7938=CARTESIAN_POINT('Ctrl Pts',(-1.78750548470434,0.695412276740075,-0.903949681684082));
#7939=CARTESIAN_POINT('Ctrl Pts',(-1.76228706012996,0.717103298307556,-0.953817581585667));
#7940=CARTESIAN_POINT('Ctrl Pts',(-1.73483868812781,0.739157960797294,-1.00290422620941));
#7941=CARTESIAN_POINT('Ctrl Pts',(-1.70524671607301,0.761466638112126,-1.05092079729495));
#7942=CARTESIAN_POINT('Ctrl Pts',(-1.67569471956003,0.783745178825665,-1.09887250320548));
#7943=CARTESIAN_POINT('Ctrl Pts',(-1.644005063612,0.806276796082526,-1.14575631858766));
#7944=CARTESIAN_POINT('Ctrl Pts',(-1.610312845326,0.828943478358563,-1.19129904937546));
#7945=CARTESIAN_POINT('Ctrl Pts',(-1.57620686948493,0.851888519006865,-1.23740106803152));
#7946=CARTESIAN_POINT('Ctrl Pts',(-1.54004908312197,0.874971676226894,-1.28212811955073));
#7947=CARTESIAN_POINT('Ctrl Pts',(-1.50202718276504,0.898065543699821,-1.32522270849081));
#7948=CARTESIAN_POINT('Ctrl Pts',(-1.46447392216126,0.920874767210976,-1.36778613414519));
#7949=CARTESIAN_POINT('Ctrl Pts',(-1.42510278850771,0.943694135502599,-1.40875659069773));
#7950=CARTESIAN_POINT('Ctrl Pts',(-1.38413434133606,0.966400507514448,-1.4479202360624));
#7951=CARTESIAN_POINT('Ctrl Pts',(-1.3423990056442,0.989531920191343,-1.48781698585533));
#7952=CARTESIAN_POINT('Ctrl Pts',(-1.29900653939395,1.01254574679517,-1.52583806568238));
#7953=CARTESIAN_POINT('Ctrl Pts',(-1.25422343600175,1.03531613020345,-1.56180167033104));
#7954=CARTESIAN_POINT('Ctrl Pts',(-1.20944033260954,1.05808651361172,-1.5977652749797));
#7955=CARTESIAN_POINT('Ctrl Pts',(-1.16326733827024,1.08061317258821,-1.63167113305563));
#7956=CARTESIAN_POINT('Ctrl Pts',(-1.11599400238479,1.10277908871816,-1.66338758908019));
#7957=CARTESIAN_POINT('Ctrl Pts',(-1.10936742882085,1.10588621181613,-1.66783346591748));
#7958=CARTESIAN_POINT('Ctrl Pts',(-1.1027192606465,1.1089862646405,-1.67223640644771));
#7959=CARTESIAN_POINT('Ctrl Pts',(-1.09605031831594,1.11207894340675,-1.67659613043344));
#7960=CARTESIAN_POINT('Ctrl Pts',(-1.04927657204218,1.13376996497337,-1.70717378629317));
#7961=CARTESIAN_POINT('Ctrl Pts',(-1.00096226228592,1.15582462746222,-1.73595988152172));
#7962=CARTESIAN_POINT('Ctrl Pts',(-0.951326577197707,1.17813330477615,-1.76274746585609));
#7963=CARTESIAN_POINT('Ctrl Pts',(-0.901757944525814,1.20041184549145,-1.78949886307521));
#7964=CARTESIAN_POINT('Ctrl Pts',(-0.850871989742473,1.22294346275011,-1.81425661025049));
#7965=CARTESIAN_POINT('Ctrl Pts',(-0.79892230739882,1.24561014502797,-1.83685166292907));
#7966=CARTESIAN_POINT('Ctrl Pts',(-0.746334656571898,1.26855518567611,-1.85972419433008));
#7967=CARTESIAN_POINT('Ctrl Pts',(-0.692657569277719,1.29163834289596,-1.88038006400027));
#7968=CARTESIAN_POINT('Ctrl Pts',(-0.638182343198804,1.31473221036871,-1.89869012260928));
#7969=CARTESIAN_POINT('Ctrl Pts',(-0.58437855269953,1.33754143387742,-1.91677450019409));
#7970=CARTESIAN_POINT('Ctrl Pts',(-0.529796922509381,1.36036080216659,-1.93257038954486));
#7971=CARTESIAN_POINT('Ctrl Pts',(-0.474735383828777,1.38306717417602,-1.94600287774858));
#7972=CARTESIAN_POINT('Ctrl Pts',(-0.418643147985475,1.40619858685387,-1.95968680875268));
#7973=CARTESIAN_POINT('Ctrl Pts',(-0.3620536299641,1.42921241345865,-1.97091779663782));
#7974=CARTESIAN_POINT('Ctrl Pts',(-0.305288522439514,1.45198279686787,-1.97967164017963));
#7975=CARTESIAN_POINT('Ctrl Pts',(-0.248523414914927,1.47475318027709,-1.98842548372145));
#7976=CARTESIAN_POINT('Ctrl Pts',(-0.191583499807998,1.49727983925449,-1.99470232098299));
#7977=CARTESIAN_POINT('Ctrl Pts',(-0.134785361994971,1.51944575538534,-1.99853290967568));
#7978=CARTESIAN_POINT('Ctrl Pts',(-0.126823642530318,1.52255287848314,-1.99906986517686));
#7979=CARTESIAN_POINT('Ctrl Pts',(-0.118864689737994,1.52565293130735,-1.99955883944018));
#7980=CARTESIAN_POINT('Ctrl Pts',(-0.110909354270907,1.52874561007343,-2.00000000000001));
#7981=CARTESIAN_POINT('Ctrl Pts',(-0.0551132738209439,1.5504366316466,-2.0030941536268));
#7982=CARTESIAN_POINT('Ctrl Pts',(0.00112119342568086,1.57249129414221,
-2.00386648849188));
#7983=CARTESIAN_POINT('Ctrl Pts',(0.0575007498306207,1.59479997146302,-2.00224737448543));
#7984=CARTESIAN_POINT('Ctrl Pts',(0.113804143542876,1.61707851216972,-2.00063044772718));
#7985=CARTESIAN_POINT('Ctrl Pts',(0.170251546646483,1.63961012941955,-1.99662830833083));
#7986=CARTESIAN_POINT('Ctrl Pts',(0.226538817591831,1.66227681168847,-1.99022135678145));
#7987=CARTESIAN_POINT('Ctrl Pts',(0.283517324835077,1.68522185233709,-1.98373572461041));
#7988=CARTESIAN_POINT('Ctrl Pts',(0.34033098086939,1.70830500955743,-1.97478568883516));
#7989=CARTESIAN_POINT('Ctrl Pts',(0.396662939836441,1.73139887703068,-1.96340505169596));
#7990=CARTESIAN_POINT('Ctrl Pts',(0.452300578026043,1.75420810054139,-1.95216468684573));
#7991=CARTESIAN_POINT('Ctrl Pts',(0.507467601030938,1.77702746883257,-1.93855351320271));
#7992=CARTESIAN_POINT('Ctrl Pts',(0.561868536406385,1.79973384084398,-1.92265561988137));
#7993=CARTESIAN_POINT('Ctrl Pts',(0.617287803103204,1.82286525352159,-1.90646013383298));
#7994=CARTESIAN_POINT('Ctrl Pts',(0.671911257239619,1.84587908012614,-1.88789169564054));
#7995=CARTESIAN_POINT('Ctrl Pts',(0.725448204174811,1.86864946353513,-1.86709019276638));
#7996=CARTESIAN_POINT('Ctrl Pts',(0.778985151110002,1.89141984694411,-1.84628868989223));
#7997=CARTESIAN_POINT('Ctrl Pts',(0.831434982712155,1.91394650592129,-1.82325463286289));
#7998=CARTESIAN_POINT('Ctrl Pts',(0.882538907291713,1.93611242205192,-1.79817295107595));
#7999=CARTESIAN_POINT('Ctrl Pts',(0.889702436356562,1.93921954514975,-1.79465710844832));
#8000=CARTESIAN_POINT('Ctrl Pts',(0.896839578793958,1.94231959797399,-1.79110109618596));
#8001=CARTESIAN_POINT('Ctrl Pts',(0.903949681684062,1.94541227674011,-1.78750548470435));
#8002=CARTESIAN_POINT('Ctrl Pts',(0.953817581594439,1.96710329831142,-1.76228706012554));
#8003=CARTESIAN_POINT('Ctrl Pts',(1.00290422622669,1.98915796080511,-1.73483868811816));
#8004=CARTESIAN_POINT('Ctrl Pts',(1.0509207973203,2.01146663812396,-1.70524671605739));
#8005=CARTESIAN_POINT('Ctrl Pts',(1.09887250322638,2.0337451788357,-1.67569471954618));
#8006=CARTESIAN_POINT('Ctrl Pts',(1.14575631860424,2.05627679609069,-1.6440050636003));
#8007=CARTESIAN_POINT('Ctrl Pts',(1.19129904938792,2.07894347836483,-1.6103128453168));
#8008=CARTESIAN_POINT('Ctrl Pts',(1.23740106804277,2.10188851901268,-1.57620686947607));
#8009=CARTESIAN_POINT('Ctrl Pts',(1.28212811956079,2.12497167623223,-1.54004908311355));
#8010=CARTESIAN_POINT('Ctrl Pts',(1.32522270849975,2.14806554370468,-1.50202718275716));
#8011=CARTESIAN_POINT('Ctrl Pts',(1.36778613414331,2.17087476721016,-1.46447392216248));
#8012=CARTESIAN_POINT('Ctrl Pts',(1.40875659068581,2.19369413549609,-1.42510278851892));
#8013=CARTESIAN_POINT('Ctrl Pts',(1.44792023604139,2.21640050750233,-1.38413434135804));
#8014=CARTESIAN_POINT('Ctrl Pts',(1.4878169858386,2.23953192018137,-1.34239900566296));
#8015=CARTESIAN_POINT('Ctrl Pts',(1.52583806566963,2.26254574678733,-1.29900653940915));
#8016=CARTESIAN_POINT('Ctrl Pts',(1.56180167032191,2.28531613019772,-1.2542234360131));
#8017=CARTESIAN_POINT('Ctrl Pts',(1.59776527497418,2.3080865136081,-1.20944033261705));
#8018=CARTESIAN_POINT('Ctrl Pts',(1.63167113305336,2.33061317258665,-1.16326733827364));
#8019=CARTESIAN_POINT('Ctrl Pts',(1.66338758908079,2.35277908871862,-1.11599400238388));
#8020=CARTESIAN_POINT('Ctrl Pts',(1.66783346591787,2.35588621181643,-1.10936742882024));
#8021=CARTESIAN_POINT('Ctrl Pts',(1.67223640644789,2.35898626464066,-1.10271926064619));
#8022=CARTESIAN_POINT('Ctrl Pts',(1.67659613043342,2.36207894340677,-1.09605031831594));
#8023=CARTESIAN_POINT('Ctrl Pts',(1.70717378629795,2.38376996497678,-1.04927657203487));
#8024=CARTESIAN_POINT('Ctrl Pts',(1.73595988153072,2.40582462746913,-1.00096226227081));
#8025=CARTESIAN_POINT('Ctrl Pts',(1.76274746586867,2.42813330478662,-0.951326577174423));
#8026=CARTESIAN_POINT('Ctrl Pts',(1.78949886307852,2.4504118454948,-0.901757944518151));
#8027=CARTESIAN_POINT('Ctrl Pts',(1.81425661024578,2.47294346274615,-0.850871989751322));
#8028=CARTESIAN_POINT('Ctrl Pts',(1.83685166291778,2.49561014501663,-0.79892230742483));
#8029=CARTESIAN_POINT('Ctrl Pts',(1.85972419432044,2.51855518566565,-0.746334656596121));
#8030=CARTESIAN_POINT('Ctrl Pts',(1.88038006399214,2.54163834288643,-0.692657569300023));
#8031=CARTESIAN_POINT('Ctrl Pts',(1.89869012260248,2.56473221036011,-0.638182343219085));
#8032=CARTESIAN_POINT('Ctrl Pts',(1.9167745001887,2.58754143386987,-0.584378552717512));
#8033=CARTESIAN_POINT('Ctrl Pts',(1.93257038954068,2.61036080216012,-0.529796922524956));
#8034=CARTESIAN_POINT('Ctrl Pts',(1.94600287774539,2.63306717417062,-0.474735383841874));
#8035=CARTESIAN_POINT('Ctrl Pts',(1.95968680875038,2.65619858684937,-0.418643147996515));
#8036=CARTESIAN_POINT('Ctrl Pts',(1.97091779663624,2.67921241345505,-0.362053629973022));
#8037=CARTESIAN_POINT('Ctrl Pts',(1.97967164017859,2.70198279686515,-0.305288522446292));
#8038=CARTESIAN_POINT('Ctrl Pts',(1.98842548372093,2.72475318027525,-0.248523414919561));
#8039=CARTESIAN_POINT('Ctrl Pts',(1.99470232098281,2.74727983925353,-0.19158349981046));
#8040=CARTESIAN_POINT('Ctrl Pts',(1.99853290967565,2.76944575538522,-0.134785361995276));
#8041=CARTESIAN_POINT('Ctrl Pts',(1.99906986517684,2.77255287848306,-0.126823642530526));
#8042=CARTESIAN_POINT('Ctrl Pts',(1.99955883944017,2.77565293130731,-0.118864689738103));
#8043=CARTESIAN_POINT('Ctrl Pts',(2.00000000000001,2.77874561007344,-0.110909354270919));
#8044=CARTESIAN_POINT('Ctrl Pts',(2.00309415362589,2.80043663164038,-0.0551132738369698));
#8045=CARTESIAN_POINT('Ctrl Pts',(2.00386648849142,2.82249129412957,0.00112119339338623));
#8046=CARTESIAN_POINT('Ctrl Pts',(2.0022473744868,2.84479997144383,0.0575007497820639));
#8047=CARTESIAN_POINT('Ctrl Pts',(2.00063044772948,2.86707851215629,0.113804143509145));
#8048=CARTESIAN_POINT('Ctrl Pts',(1.99662830833282,2.88961012941204,0.170251546627733));
#8049=CARTESIAN_POINT('Ctrl Pts',(1.99022135678185,2.91227681168697,0.226538817587992));
#8050=CARTESIAN_POINT('Ctrl Pts',(1.98373572461087,2.93522185233572,0.2835173248316));
#8051=CARTESIAN_POINT('Ctrl Pts',(1.97478568883566,2.95830500955621,0.340330980866278));
#8052=CARTESIAN_POINT('Ctrl Pts',(1.96340505169648,2.9813988770296,0.396662939833696));
#8053=CARTESIAN_POINT('Ctrl Pts',(1.9521646868472,3.00420810053854,0.452300578019002));
#8054=CARTESIAN_POINT('Ctrl Pts',(1.9385535132055,3.02702746882794,0.507467601019676));
#8055=CARTESIAN_POINT('Ctrl Pts',(1.92265561988582,3.04973384083762,0.561868536391049));
#8056=CARTESIAN_POINT('Ctrl Pts',(1.90646013383709,3.07286525351635,0.61728780309064));
#8057=CARTESIAN_POINT('Ctrl Pts',(1.8878916956441,3.095879080122,0.671911257229776));
#8058=CARTESIAN_POINT('Ctrl Pts',(1.86709019276915,3.11864946353209,0.725448204167599));
#8059=CARTESIAN_POINT('Ctrl Pts',(1.84628868989421,3.14141984694217,0.778985151105422));
#8060=CARTESIAN_POINT('Ctrl Pts',(1.82325463286388,3.16394650592043,0.831434982710117));
#8061=CARTESIAN_POINT('Ctrl Pts',(1.79817295107574,3.1861124220521,0.882538907292086));
#8062=CARTESIAN_POINT('Ctrl Pts',(1.79465710844817,3.18921954514987,0.8897024363568));
#8063=CARTESIAN_POINT('Ctrl Pts',(1.79110109618588,3.19231959797405,0.896839578794061));
#8064=CARTESIAN_POINT('Ctrl Pts',(1.78750548470433,3.1954122767401,0.903949681684033));
#8065=CARTESIAN_POINT('Ctrl Pts',(1.76228706012363,3.21710329831304,0.953817581598165));
#8066=CARTESIAN_POINT('Ctrl Pts',(1.73483868811402,3.23915796080841,1.00290422623404));
#8067=CARTESIAN_POINT('Ctrl Pts',(1.70524671605071,3.26146663812897,1.0509207973311));
#8068=CARTESIAN_POINT('Ctrl Pts',(1.67569471954924,3.28374517883316,1.0988725032207));
#8069=CARTESIAN_POINT('Ctrl Pts',(1.64400506361456,3.30627679608043,1.14575631858279));
#8070=CARTESIAN_POINT('Ctrl Pts',(1.61031284534359,3.32894347834677,1.19129904935168));
#8071=CARTESIAN_POINT('Ctrl Pts',(1.57620686950167,3.35188851899607,1.2374010680103));
#8072=CARTESIAN_POINT('Ctrl Pts',(1.54004908313765,3.37497167621712,1.28212811953198));
#8073=CARTESIAN_POINT('Ctrl Pts',(1.50202718277948,3.39806554369109,1.32522270847443));
#8074=CARTESIAN_POINT('Ctrl Pts',(1.46447392218186,3.42087476719878,1.36778613412276));
#8075=CARTESIAN_POINT('Ctrl Pts',(1.42510278853499,3.44369413548695,1.40875659066976));
#8076=CARTESIAN_POINT('Ctrl Pts',(1.38413434137046,3.46640050749542,1.4479202360295));
#8077=CARTESIAN_POINT('Ctrl Pts',(1.34239900567359,3.48953192017566,1.48781698582912));
#8078=CARTESIAN_POINT('Ctrl Pts',(1.29900653941778,3.51254574678283,1.52583806566237));
#8079=CARTESIAN_POINT('Ctrl Pts',(1.25422343601959,3.5353161301944,1.56180167031668));
#8080=CARTESIAN_POINT('Ctrl Pts',(1.2094403326214,3.55808651360597,1.59776527497099));
#8081=CARTESIAN_POINT('Ctrl Pts',(1.16326733827567,3.5806131725857,1.63167113305201));
#8082=CARTESIAN_POINT('Ctrl Pts',(1.11599400238349,3.60277908871879,1.66338758908104));
#8083=CARTESIAN_POINT('Ctrl Pts',(1.10936742881998,3.60588621181655,1.66783346591803));
#8084=CARTESIAN_POINT('Ctrl Pts',(1.10271926064606,3.60898626464072,1.67223640644796));
#8085=CARTESIAN_POINT('Ctrl Pts',(1.09605031831594,3.61207894340676,1.67659613043341));
#8086=CARTESIAN_POINT('Ctrl Pts',(1.04927657204018,3.63376996497431,1.70717378629447));
#8087=CARTESIAN_POINT('Ctrl Pts',(1.00096226228176,3.65582462746412,1.73595988152418));
#8088=CARTESIAN_POINT('Ctrl Pts',(0.951326577191293,3.67813330477903,1.76274746585954));
#8089=CARTESIAN_POINT('Ctrl Pts',(0.901757944520491,3.70041184549381,1.78949886307784));
#8090=CARTESIAN_POINT('Ctrl Pts',(0.850871989738323,3.72294346275193,1.81425661025238));
#8091=CARTESIAN_POINT('Ctrl Pts',(0.798922307395897,3.74561014502924,1.83685166293033));
#8092=CARTESIAN_POINT('Ctrl Pts',(0.746334656569164,3.76855518567727,1.85972419433115));
#8093=CARTESIAN_POINT('Ctrl Pts',(0.692657569275196,3.79163834289702,1.88038006400118));
#8094=CARTESIAN_POINT('Ctrl Pts',(0.638182343196498,3.81473221036967,1.89869012261004));
#8095=CARTESIAN_POINT('Ctrl Pts',(0.584378552698208,3.83754143387795,1.91677450019444));
#8096=CARTESIAN_POINT('Ctrl Pts',(0.529796922509088,3.86036080216669,1.93257038954489));
#8097=CARTESIAN_POINT('Ctrl Pts',(0.474735383829518,3.88306717417569,1.94600287774836));
#8098=CARTESIAN_POINT('Ctrl Pts',(0.418643147986074,3.90619858685361,1.95968680875251));
#8099=CARTESIAN_POINT('Ctrl Pts',(0.362053629964559,3.92921241345845,1.9709177966377));
#8100=CARTESIAN_POINT('Ctrl Pts',(0.305288522439826,3.95198279686773,1.97967164017955));
#8101=CARTESIAN_POINT('Ctrl Pts',(0.248523414915094,3.97475318027701,1.9884254837214));
#8102=CARTESIAN_POINT('Ctrl Pts',(0.191583499808025,3.99727983925448,1.99470232098295));
#8103=CARTESIAN_POINT('Ctrl Pts',(0.134785361994851,4.01944575538539,1.99853290967564));
#8104=CARTESIAN_POINT('Ctrl Pts',(0.126823642530245,4.02255287848317,1.99906986517682));
#8105=CARTESIAN_POINT('Ctrl Pts',(0.118864689737964,4.02565293130737,1.99955883944014));
#8106=CARTESIAN_POINT('Ctrl Pts',(0.110909354270922,4.02874561007343,1.99999999999997));
#8107=CARTESIAN_POINT('Ctrl Pts',(0.0551132738242976,4.0504366316453,2.00309415362657));
#8108=CARTESIAN_POINT('Ctrl Pts',(-0.00112119341893398,4.07249129413957,
2.00386648849175));
#8109=CARTESIAN_POINT('Ctrl Pts',(-0.0575007498204855,4.09479997145902,
2.00224737448568));
#8110=CARTESIAN_POINT('Ctrl Pts',(-0.113804143538063,4.1170785121678,2.00063044772756));
#8111=CARTESIAN_POINT('Ctrl Pts',(-0.170251546647037,4.13961012941977,1.9966283083309));
#8112=CARTESIAN_POINT('Ctrl Pts',(-0.226538817597707,4.16227681169085,1.99022135678075));
#8113=CARTESIAN_POINT('Ctrl Pts',(-0.283517324840411,4.18522185233926,1.98373572460959));
#8114=CARTESIAN_POINT('Ctrl Pts',(-0.340330980874181,4.2083050095594,1.97478568883428));
#8115=CARTESIAN_POINT('Ctrl Pts',(-0.396662939840692,4.23139887703244,1.96340505169506));
#8116=CARTESIAN_POINT('Ctrl Pts',(-0.452300578028994,4.25420810054262,1.95216468684497));
#8117=CARTESIAN_POINT('Ctrl Pts',(-0.507467601032612,4.27702746883328,1.9385535132022));
#8118=CARTESIAN_POINT('Ctrl Pts',(-0.561868536406803,4.29973384084417,1.92265561988122));
#8119=CARTESIAN_POINT('Ctrl Pts',(-0.617287803103484,4.32286525352173,1.90646013383284));
#8120=CARTESIAN_POINT('Ctrl Pts',(-0.671911257239761,4.34587908012621,1.88789169564045));
#8121=CARTESIAN_POINT('Ctrl Pts',(-0.725448204174809,4.36864946353514,1.86709019276634));
#8122=CARTESIAN_POINT('Ctrl Pts',(-0.778985151109857,4.39141984694406,1.84628868989224));
#8123=CARTESIAN_POINT('Ctrl Pts',(-0.831434982711863,4.41394650592118,1.82325463286298));
#8124=CARTESIAN_POINT('Ctrl Pts',(-0.882538907291288,4.43611242205175,1.79817295107612));
#8125=CARTESIAN_POINT('Ctrl Pts',(-0.889702436356276,4.43921954514964,1.79465710844842));
#8126=CARTESIAN_POINT('Ctrl Pts',(-0.896839578793813,4.44231959797394,1.79110109618599));
#8127=CARTESIAN_POINT('Ctrl Pts',(-0.903949681684058,4.44541227674011,1.78750548470431));
#8128=CARTESIAN_POINT('Ctrl Pts',(-0.95381758158599,4.46710329830775,1.76228706012975));
#8129=CARTESIAN_POINT('Ctrl Pts',(-1.00290422621005,4.48915796079764,1.7348386881274));
#8130=CARTESIAN_POINT('Ctrl Pts',(-1.05092079729589,4.51146663811263,1.70524671607237));
#8131=CARTESIAN_POINT('Ctrl Pts',(-1.09887250320882,4.5337451788273,1.67569471955788));
#8132=CARTESIAN_POINT('Ctrl Pts',(-1.14575631859328,4.55627679608531,1.64400506360812));
#8133=CARTESIAN_POINT('Ctrl Pts',(-1.1912990493832,4.57894347836249,1.61031284532021));
#8134=CARTESIAN_POINT('Ctrl Pts',(-1.23740106803856,4.60188851901054,1.57620686947931));
#8135=CARTESIAN_POINT('Ctrl Pts',(-1.28212811955707,4.6249716762303,1.54004908311658));
#8136=CARTESIAN_POINT('Ctrl Pts',(-1.32522270849651,4.64806554370296,1.50202718275994));
#8137=CARTESIAN_POINT('Ctrl Pts',(-1.36778613414585,4.67087476721149,1.46447392216032));
#8138=CARTESIAN_POINT('Ctrl Pts',(-1.40875659069372,4.69369413550049,1.42510278851133));
#8139=CARTESIAN_POINT('Ctrl Pts',(-1.44792023605415,4.71640050750975,1.38413434134462));
#8140=CARTESIAN_POINT('Ctrl Pts',(-1.48781698584889,4.73953192018755,1.34239900565136));
#8141=CARTESIAN_POINT('Ctrl Pts',(-1.52583806567761,4.76254574679229,1.29900653939958));
#8142=CARTESIAN_POINT('Ctrl Pts',(-1.56180167032779,4.78531613020146,1.25422343600572));
#8143=CARTESIAN_POINT('Ctrl Pts',(-1.59776527497796,4.80808651361063,1.20944033261186));
#8144=CARTESIAN_POINT('Ctrl Pts',(-1.63167113305526,4.830613172588,1.16326733827078));
#8145=CARTESIAN_POINT('Ctrl Pts',(-1.66338758908104,4.85277908871881,1.11599400238347));
#8146=CARTESIAN_POINT('Ctrl Pts',(-1.66783346591803,4.85588621181656,1.10936742881996));
#8147=CARTESIAN_POINT('Ctrl Pts',(-1.67223640644797,4.85898626464074,1.10271926064603));
#8148=CARTESIAN_POINT('Ctrl Pts',(-1.67659613043342,4.86207894340678,1.09605031831591));
#8149=CARTESIAN_POINT('Ctrl Pts',(-1.7071737862946,4.88376996497442,1.04927657203996));
#8150=CARTESIAN_POINT('Ctrl Pts',(-1.73595988152442,4.90582462746431,1.00096226228135));
#8151=CARTESIAN_POINT('Ctrl Pts',(-1.76274746585988,4.92813330477931,0.951326577190672));
#8152=CARTESIAN_POINT('Ctrl Pts',(-1.78949886307729,4.95041184549336,0.901757944521465));
#8153=CARTESIAN_POINT('Ctrl Pts',(-1.81425661025109,4.97294346275075,0.85087198974096));
#8154=CARTESIAN_POINT('Ctrl Pts',(-1.83685166292844,4.99561014502732,0.798922307400261));
#8155=CARTESIAN_POINT('Ctrl Pts',(-1.8597241943295,5.01855518567546,0.746334656573327));
#8156=CARTESIAN_POINT('Ctrl Pts',(-1.88038006399974,5.04163834289532,0.692657569279139));
#8157=CARTESIAN_POINT('Ctrl Pts',(-1.89869012260881,5.06473221036808,0.638182343200189));
#8158=CARTESIAN_POINT('Ctrl Pts',(-1.91677450019352,5.08754143387663,0.584378552701312));
#8159=CARTESIAN_POINT('Ctrl Pts',(-1.93257038954424,5.11036080216563,0.529796922511562));
#8160=CARTESIAN_POINT('Ctrl Pts',(-1.94600287774792,5.1330671741749,0.47473538383138));
#8161=CARTESIAN_POINT('Ctrl Pts',(-1.95968680875216,5.15619858685286,0.418643147987838));
#8162=CARTESIAN_POINT('Ctrl Pts',(-1.97091779663741,5.17921241345773,0.362053629966241));
#8163=CARTESIAN_POINT('Ctrl Pts',(-1.97967164017932,5.20198279686705,0.305288522441415));
#8164=CARTESIAN_POINT('Ctrl Pts',(-1.98842548372123,5.22475318027637,0.24852341491659));
#8165=CARTESIAN_POINT('Ctrl Pts',(-1.99470232098284,5.24727983925388,0.191583499809409));
#8166=CARTESIAN_POINT('Ctrl Pts',(-1.99853290967558,5.26944575538484,0.134785361996117));
#8167=CARTESIAN_POINT('Ctrl Pts',(-1.9990698651768,5.27255287848279,0.12682364253107));
#8168=CARTESIAN_POINT('Ctrl Pts',(-1.99955883944015,5.27565293130716,0.11886468973834));
#8169=CARTESIAN_POINT('Ctrl Pts',(-2.,5.2787456100734,0.110909354270861));
#8170=CARTESIAN_POINT('Ctrl Pts',(-2.0030941536262,5.30043663164251,0.0551132738313546));
#8171=CARTESIAN_POINT('Ctrl Pts',(-2.00386648849157,5.32249129413392,-0.00112119340466367));
#8172=CARTESIAN_POINT('Ctrl Pts',(-2.00224737448632,5.34479997145046,-0.0575007497989892));
#8173=CARTESIAN_POINT('Ctrl Pts',(-2.00063044772871,5.36707851216043,-0.113804143519675));
#8174=CARTESIAN_POINT('Ctrl Pts',(-1.99662830833229,5.38961012941363,-0.170251546631835));
#8175=CARTESIAN_POINT('Ctrl Pts',(-1.99022135678213,5.41227681168596,-0.22653881758568));
#8176=CARTESIAN_POINT('Ctrl Pts',(-1.98373572461123,5.43522185233474,-0.283517324829355));
#8177=CARTESIAN_POINT('Ctrl Pts',(-1.97478568883606,5.45830500955525,-0.340330980864099));
#8178=CARTESIAN_POINT('Ctrl Pts',(-1.96340505169692,5.48139887702867,-0.39666293983159));
#8179=CARTESIAN_POINT('Ctrl Pts',(-1.95216468684977,5.50420810053341,-0.452300578006675));
#8180=CARTESIAN_POINT('Ctrl Pts',(-1.93855351321107,5.52702746881863,-0.507467600997336));
#8181=CARTESIAN_POINT('Ctrl Pts',(-1.92265561989521,5.54973384082418,-0.561868536359007));
#8182=CARTESIAN_POINT('Ctrl Pts',(-1.90646013384591,5.57286525350508,-0.617287803063998));
#8183=CARTESIAN_POINT('Ctrl Pts',(-1.88789169565188,5.59587908011291,-0.671911257208426));
#8184=CARTESIAN_POINT('Ctrl Pts',(-1.86709019277549,5.61864946352513,-0.725448204151379));
#8185=CARTESIAN_POINT('Ctrl Pts',(-1.84628868989909,5.64141984693736,-0.778985151094332));
#8186=CARTESIAN_POINT('Ctrl Pts',(-1.82325463286685,5.66394650591773,-0.831434982704001));
#8187=CARTESIAN_POINT('Ctrl Pts',(-1.79817295107646,5.68611242205145,-0.882538907290695));
#8188=CARTESIAN_POINT('Ctrl Pts',(-1.79465710844866,5.68921954514943,-0.889702436355896));
#8189=CARTESIAN_POINT('Ctrl Pts',(-1.79110109618612,5.69231959797383,-0.896839578793643));
#8190=CARTESIAN_POINT('Ctrl Pts',(-1.78750548470433,5.69541227674009,-0.903949681684095));
#8191=CARTESIAN_POINT('Ctrl Pts',(-1.76228706012609,5.7171032983109,-0.953817581593325));
#8192=CARTESIAN_POINT('Ctrl Pts',(-1.73483868811939,5.73915796080408,-1.00290422622447));
#8193=CARTESIAN_POINT('Ctrl Pts',(-1.70524671605941,5.7614666381224,-1.05092079731701));
#8194=CARTESIAN_POINT('Ctrl Pts',(-1.67569471954416,5.78374517883724,-1.09887250322985));
#8195=CARTESIAN_POINT('Ctrl Pts',(-1.64400506359364,5.80627679609541,-1.14575631861415));
#8196=CARTESIAN_POINT('Ctrl Pts',(-1.61031284530496,5.82894347837275,-1.19129904940391));
#8197=CARTESIAN_POINT('Ctrl Pts',(-1.57620686946479,5.85188851901994,-1.23740106805705));
#8198=CARTESIAN_POINT('Ctrl Pts',(-1.54004908310295,5.87497167623883,-1.28212811957342));
#8199=CARTESIAN_POINT('Ctrl Pts',(-1.50202718274738,5.89806554371058,-1.32522270851082));
#8200=CARTESIAN_POINT('Ctrl Pts',(-1.46447392215038,5.92087476721728,-1.36778613415636));
#8201=CARTESIAN_POINT('Ctrl Pts',(-1.42510278850434,5.94369413550442,-1.40875659070067));
#8202=CARTESIAN_POINT('Ctrl Pts',(-1.38413434134083,5.96640050751184,-1.44792023605782));
#8203=CARTESIAN_POINT('Ctrl Pts',(-1.34239900564825,5.98953192018921,-1.4878169858517));
#8204=CARTESIAN_POINT('Ctrl Pts',(-1.29900653939721,6.01254574679351,-1.52583806567962));
#8205=CARTESIAN_POINT('Ctrl Pts',(-1.25422343600415,6.03531613020225,-1.56180167032907));
#8206=CARTESIAN_POINT('Ctrl Pts',(-1.2094403326111,6.05808651361099,-1.59776527497852));
#8207=CARTESIAN_POINT('Ctrl Pts',(-1.1632673382709,6.08061317258793,-1.63167113305516));
#8208=CARTESIAN_POINT('Ctrl Pts',(-1.11599400238451,6.10277908871833,-1.66338758908036));
#8209=CARTESIAN_POINT('Ctrl Pts',(-1.10936742882066,6.10588621181624,-1.66783346591758));
#8210=CARTESIAN_POINT('Ctrl Pts',(-1.1027192606464,6.10898626464057,-1.67223640644774));
#8211=CARTESIAN_POINT('Ctrl Pts',(-1.09605031831594,6.11207894340677,-1.67659613043341));
#8212=CARTESIAN_POINT('Ctrl Pts',(-1.04927657203408,6.13376996497715,-1.70717378629846));
#8213=CARTESIAN_POINT('Ctrl Pts',(-1.00096226226917,6.15582462746988,-1.73595988153168));
#8214=CARTESIAN_POINT('Ctrl Pts',(-0.951326577171912,6.17813330478775,-1.76274746587001));
#8215=CARTESIAN_POINT('Ctrl Pts',(-0.901757944513397,6.20041184549692,-1.78949886308099));
#8216=CARTESIAN_POINT('Ctrl Pts',(-0.85087198974423,6.22294346274929,-1.81425661024918));
#8217=CARTESIAN_POINT('Ctrl Pts',(-0.798922307415297,6.24561014502079,-1.83685166292192));
#8218=CARTESIAN_POINT('Ctrl Pts',(-0.746334656587136,6.26855518566954,-1.85972419432402));
#8219=CARTESIAN_POINT('Ctrl Pts',(-0.692657569291611,6.29163834289003,-1.88038006399521));
#8220=CARTESIAN_POINT('Ctrl Pts',(-0.638182343211294,6.31473221036342,-1.8986901226051));
#8221=CARTESIAN_POINT('Ctrl Pts',(-0.584378552714839,6.33754143387098,-1.91677450018935));
#8222=CARTESIAN_POINT('Ctrl Pts',(-0.529796922527578,6.36036080215901,-1.93257038953981));
#8223=CARTESIAN_POINT('Ctrl Pts',(-0.474735383849875,6.38306717416733,-1.94600287774344));
#8224=CARTESIAN_POINT('Ctrl Pts',(-0.418643148002995,6.40619858684674,-1.95968680874906));
#8225=CARTESIAN_POINT('Ctrl Pts',(-0.362053629977934,6.42921241345308,-1.9709177966354));
#8226=CARTESIAN_POINT('Ctrl Pts',(-0.305288522449613,6.45198279686383,-1.97967164017809));
#8227=CARTESIAN_POINT('Ctrl Pts',(-0.248523414921292,6.47475318027459,-1.98842548372078));
#8228=CARTESIAN_POINT('Ctrl Pts',(-0.191583499810573,6.49727983925352,-1.99470232098286));
#8229=CARTESIAN_POINT('Ctrl Pts',(-0.134785361993779,6.51944575538583,-1.99853290967577));
#8230=CARTESIAN_POINT('Ctrl Pts',(-0.126823642529531,6.52255287848348,-1.99906986517692));
#8231=CARTESIAN_POINT('Ctrl Pts',(-0.118864689737606,6.52565293130753,-1.99955883944021));
#8232=CARTESIAN_POINT('Ctrl Pts',(-0.110909354270919,6.52874561007346,-2.00000000000002));
#8233=CARTESIAN_POINT('Ctrl Pts',(-0.0551132738396572,6.55043663163936,
-2.00309415362574));
#8234=CARTESIAN_POINT('Ctrl Pts',(0.00112119338795719,6.57249129412745,
-2.00386648849135));
#8235=CARTESIAN_POINT('Ctrl Pts',(0.0575007497738815,6.5947999714406,-2.00224737448704));
#8236=CARTESIAN_POINT('Ctrl Pts',(0.113804143520435,6.61707851216074,-2.00063044772938));
#8237=CARTESIAN_POINT('Ctrl Pts',(0.170251546658587,6.63961012942435,-1.99662830833074));
#8238=CARTESIAN_POINT('Ctrl Pts',(0.226538817638237,6.6622768117072,-1.99022135677613));
#8239=CARTESIAN_POINT('Ctrl Pts',(0.283517324877466,6.6852218523543,-1.9837357246042));
#8240=CARTESIAN_POINT('Ctrl Pts',(0.340330980907712,6.70830500957309,-1.9747856888284));
#8241=CARTESIAN_POINT('Ctrl Pts',(0.396662939870692,6.73139887704476,-1.96340505168901));
#8242=CARTESIAN_POINT('Ctrl Pts',(0.452300578056111,6.75420810055383,-1.95216468683862));
#8243=CARTESIAN_POINT('Ctrl Pts',(0.507467601056806,6.77702746884334,-1.93855351319579));
#8244=CARTESIAN_POINT('Ctrl Pts',(0.561868536428129,6.79973384085308,-1.92265561987499));
#8245=CARTESIAN_POINT('Ctrl Pts',(0.617287803120988,6.8228652535291,-1.90646013382708));
#8246=CARTESIAN_POINT('Ctrl Pts',(0.671911257253534,6.84587908013206,-1.88789169563546));
#8247=CARTESIAN_POINT('Ctrl Pts',(0.725448204184969,6.86864946353947,-1.86709019276243));
#8248=CARTESIAN_POINT('Ctrl Pts',(0.778985151116403,6.89141984694689,-1.84628868988941));
#8249=CARTESIAN_POINT('Ctrl Pts',(0.831434982714933,6.91394650592253,-1.8232546328615));
#8250=CARTESIAN_POINT('Ctrl Pts',(0.882538907291036,6.93611242205166,-1.79817295107629));
#8251=CARTESIAN_POINT('Ctrl Pts',(0.889702436356114,6.93921954514958,-1.79465710844855));
#8252=CARTESIAN_POINT('Ctrl Pts',(0.896839578793735,6.94231959797392,-1.79110109618609));
#8253=CARTESIAN_POINT('Ctrl Pts',(0.903949681684065,6.94541227674013,-1.78750548470436));
#8254=CARTESIAN_POINT('Ctrl Pts',(0.953817581589804,6.96710329830942,-1.7622870601279));
#8255=CARTESIAN_POINT('Ctrl Pts',(1.00290422621755,6.98915796080102,-1.7348386881233));
#8256=CARTESIAN_POINT('Ctrl Pts',(1.0509207973069,7.01146663811774,-1.70524671606568));
#8257=CARTESIAN_POINT('Ctrl Pts',(1.09887250321008,7.03374517882799,-1.67569471955678));
#8258=CARTESIAN_POINT('Ctrl Pts',(1.14575631858522,7.05627679608148,-1.64400506361347));
#8259=CARTESIAN_POINT('Ctrl Pts',(1.19129904936639,7.07894347835411,-1.61031284533278));
#8260=CARTESIAN_POINT('Ctrl Pts',(1.23740106802345,7.1018885190028,-1.57620686949137));
#8261=CARTESIAN_POINT('Ctrl Pts',(1.2821281195436,7.12497167622323,-1.54004908312799));
#8262=CARTESIAN_POINT('Ctrl Pts',(1.32522270848461,7.14806554369656,-1.50202718277058));
#8263=CARTESIAN_POINT('Ctrl Pts',(1.36778613412793,7.1708747672017,-1.46447392217686));
#8264=CARTESIAN_POINT('Ctrl Pts',(1.40875659067027,7.19369413548732,-1.42510278853431));
#8265=CARTESIAN_POINT('Ctrl Pts',(1.44792023602575,7.21640050749326,-1.38413434137446));
#8266=CARTESIAN_POINT('Ctrl Pts',(1.48781698582602,7.23953192017381,-1.34239900567713));
#8267=CARTESIAN_POINT('Ctrl Pts',(1.52583806565988,7.26254574678129,-1.29900653942082));
#8268=CARTESIAN_POINT('Ctrl Pts',(1.56180167031475,7.28531613019319,-1.25422343602206));
#8269=CARTESIAN_POINT('Ctrl Pts',(1.59776527496962,7.30808651360508,-1.2094403326233));
#8270=CARTESIAN_POINT('Ctrl Pts',(1.63167113305116,7.33061317258512,-1.16326733827696));
#8271=CARTESIAN_POINT('Ctrl Pts',(1.66338758908065,7.35277908871853,-1.11599400238413));
#8272=CARTESIAN_POINT('Ctrl Pts',(1.66783346591777,7.35588621181638,-1.10936742882042));
#8273=CARTESIAN_POINT('Ctrl Pts',(1.67223640644784,7.35898626464064,-1.10271926064629));
#8274=CARTESIAN_POINT('Ctrl Pts',(1.67659613043342,7.36207894340678,-1.09605031831597));
#8275=CARTESIAN_POINT('Ctrl Pts',(1.70717378629979,7.3837699649781,-1.04927657203209));
#8276=CARTESIAN_POINT('Ctrl Pts',(1.73595988153417,7.40582462747179,-1.00096226226504));
#8277=CARTESIAN_POINT('Ctrl Pts',(1.76274746587349,7.42813330479065,-0.951326577165512));
#8278=CARTESIAN_POINT('Ctrl Pts',(1.78949886308338,7.45041184549909,-0.901757944508564));
#8279=CARTESIAN_POINT('Ctrl Pts',(1.81425661025064,7.47294346275071,-0.85087198974103));
#8280=CARTESIAN_POINT('Ctrl Pts',(1.83685166292257,7.49561014502146,-0.798922307413823));
#8281=CARTESIAN_POINT('Ctrl Pts',(1.85972419432456,7.51855518567013,-0.746334656585818));
#8282=CARTESIAN_POINT('Ctrl Pts',(1.88038006399563,7.54163834289054,-0.692657569290468));
#8283=CARTESIAN_POINT('Ctrl Pts',(1.89869012260542,7.56473221036385,-0.638182343210334));
#8284=CARTESIAN_POINT('Ctrl Pts',(1.91677450018888,7.58754143387044,-0.584378552716151));
#8285=CARTESIAN_POINT('Ctrl Pts',(1.93257038953873,7.6103608021575,-0.529796922531237));
#8286=CARTESIAN_POINT('Ctrl Pts',(1.94600287774196,7.63306717416486,-0.474735383855908));
#8287=CARTESIAN_POINT('Ctrl Pts',(1.95968680874796,7.65619858684464,-0.418643148008195));
#8288=CARTESIAN_POINT('Ctrl Pts',(1.97091779663461,7.67921241345134,-0.362053629982299));
#8289=CARTESIAN_POINT('Ctrl Pts',(1.97967164017753,7.70198279686246,-0.305288522453109));
#8290=CARTESIAN_POINT('Ctrl Pts',(1.98842548372046,7.72475318027358,-0.248523414923918));
#8291=CARTESIAN_POINT('Ctrl Pts',(1.99470232098269,7.74727983925285,-0.191583499812325));
#8292=CARTESIAN_POINT('Ctrl Pts',(1.99853290967569,7.76944575538552,-0.134785361994661));
#8293=CARTESIAN_POINT('Ctrl Pts',(1.99906986517686,7.77255287848327,-0.126823642530115));
#8294=CARTESIAN_POINT('Ctrl Pts',(1.99955883944017,7.77565293130744,-0.11886468973791));
#8295=CARTESIAN_POINT('Ctrl Pts',(2.,7.77874561007349,-0.110909354270931));
#8296=CARTESIAN_POINT('Ctrl Pts',(2.00309415362605,7.80043663164154,-0.0551132738341087));
#8297=CARTESIAN_POINT('Ctrl Pts',(2.00386648849149,7.82249129413187,0.00112119339916694));
#8298=CARTESIAN_POINT('Ctrl Pts',(2.00224737448655,7.84479997144731,0.057500749790785));
#8299=CARTESIAN_POINT('Ctrl Pts',(2.00063044772897,7.8670785121599,0.113804143518177));
#8300=CARTESIAN_POINT('Ctrl Pts',(1.99662830833203,7.88961012941579,0.170251546637083));
#8301=CARTESIAN_POINT('Ctrl Pts',(1.99022135678076,7.91227681169085,0.22653881759762));
#8302=CARTESIAN_POINT('Ctrl Pts',(1.98373572460961,7.93522185233927,0.283517324840359));
#8303=CARTESIAN_POINT('Ctrl Pts',(1.97478568883429,7.95830500955941,0.340330980874146));
#8304=CARTESIAN_POINT('Ctrl Pts',(1.96340505169508,7.98139887703245,0.396662939840668));
#8305=CARTESIAN_POINT('Ctrl Pts',(1.95216468684763,8.00420810053727,0.452300578015884));
#8306=CARTESIAN_POINT('Ctrl Pts',(1.93855351320864,8.02702746882255,0.507467601006632));
#8307=CARTESIAN_POINT('Ctrl Pts',(1.92265561989246,8.04973384082815,0.561868536368393));
#8308=CARTESIAN_POINT('Ctrl Pts',(1.90646013384331,8.07286525350844,0.617287803071861));
#8309=CARTESIAN_POINT('Ctrl Pts',(1.88789169564955,8.09587908011566,0.6719112572148));
#8310=CARTESIAN_POINT('Ctrl Pts',(1.86709019277355,8.11864946352728,0.725448204156317));
#8311=CARTESIAN_POINT('Ctrl Pts',(1.84628868989755,8.14141984693891,0.778985151097833));
#8312=CARTESIAN_POINT('Ctrl Pts',(1.82325463286583,8.16394650591869,0.831434982706109));
#8313=CARTESIAN_POINT('Ctrl Pts',(1.79817295107606,8.18611242205183,0.882538907291475));
#8314=CARTESIAN_POINT('Ctrl Pts',(1.79465710844839,8.1892195451497,0.889702436356406));
#8315=CARTESIAN_POINT('Ctrl Pts',(1.79110109618599,8.19231959797397,0.896839578793874));
#8316=CARTESIAN_POINT('Ctrl Pts',(1.78750548470434,8.19541227674012,0.903949681684059));
#8317=CARTESIAN_POINT('Ctrl Pts',(1.7622870601238,8.21710329831291,0.953817581597852));
#8318=CARTESIAN_POINT('Ctrl Pts',(1.73483868811439,8.23915796080813,1.0029042262334));
#8319=CARTESIAN_POINT('Ctrl Pts',(1.70524671605131,8.26146663812854,1.05092079733016));
#8320=CARTESIAN_POINT('Ctrl Pts',(1.67569471954768,8.28374517883438,1.09887250322331));
#8321=CARTESIAN_POINT('Ctrl Pts',(1.64400506361051,8.30627679608333,1.14575631858882));
#8322=CARTESIAN_POINT('Ctrl Pts',(1.61031284533679,8.32894347835137,1.19129904936089));
#8323=CARTESIAN_POINT('Ctrl Pts',(1.57620686949512,8.35188851900034,1.23740106801864));
#8324=CARTESIAN_POINT('Ctrl Pts',(1.5400490831314,8.37497167622106,1.28212811953947));
#8325=CARTESIAN_POINT('Ctrl Pts',(1.50202718277361,8.39806554369468,1.3252227084811));
#8326=CARTESIAN_POINT('Ctrl Pts',(1.46447392217283,8.42087476720419,1.36778613413263));
#8327=CARTESIAN_POINT('Ctrl Pts',(1.42510278852252,8.44369413549416,1.40875659068257));
#8328=CARTESIAN_POINT('Ctrl Pts',(1.38413434135432,8.4664005075044,1.44792023604494));
#8329=CARTESIAN_POINT('Ctrl Pts',(1.34239900565957,8.48953192018319,1.48781698584163));
#8330=CARTESIAN_POINT('Ctrl Pts',(1.29900653940613,8.51254574678892,1.52583806567217));
#8331=CARTESIAN_POINT('Ctrl Pts',(1.25422343601048,8.53531613019907,1.561801670324));
#8332=CARTESIAN_POINT('Ctrl Pts',(1.20944033261483,8.55808651360922,1.59776527497583));
#8333=CARTESIAN_POINT('Ctrl Pts',(1.16326733827184,8.58061317258754,1.63167113305461));
#8334=CARTESIAN_POINT('Ctrl Pts',(1.11599400238253,8.60277908871928,1.66338758908168));
#8335=CARTESIAN_POINT('Ctrl Pts',(1.10936742881934,8.60588621181689,1.66783346591845));
#8336=CARTESIAN_POINT('Ctrl Pts',(1.10271926064574,8.60898626464091,1.67223640644817));
#8337=CARTESIAN_POINT('Ctrl Pts',(1.09605031831595,8.6120789434068,1.6765961304334));
#8338=CARTESIAN_POINT('Ctrl Pts',(1.0492765720318,8.63376996497824,1.70717378629997));
#8339=CARTESIAN_POINT('Ctrl Pts',(1.00096226226444,8.65582462747207,1.73595988153451));
#8340=CARTESIAN_POINT('Ctrl Pts',(0.951326577164588,8.67813330479107,1.76274746587397));
#8341=CARTESIAN_POINT('Ctrl Pts',(0.90175794451587,8.70041184549581,1.78949886307939));
#8342=CARTESIAN_POINT('Ctrl Pts',(0.850871989756991,8.72294346274365,1.81425661024285));
#8343=CARTESIAN_POINT('Ctrl Pts',(0.798922307438777,8.74561014501057,1.83685166291171));
#8344=CARTESIAN_POINT('Ctrl Pts',(0.746334656609139,8.76855518566006,1.85972419431526));
#8345=CARTESIAN_POINT('Ctrl Pts',(0.692657569312053,8.79163834288131,1.88038006398774));
#8346=CARTESIAN_POINT('Ctrl Pts',(0.638182343230064,8.81473221035548,1.89869012259878));
#8347=CARTESIAN_POINT('Ctrl Pts',(0.58437855273512,8.83754143386247,1.91677450018311));
#8348=CARTESIAN_POINT('Ctrl Pts',(0.529796922549362,8.86036080214996,1.93257038953378));
#8349=CARTESIAN_POINT('Ctrl Pts',(0.474735383873144,8.88306717415774,1.94600287773775));
#8350=CARTESIAN_POINT('Ctrl Pts',(0.418643148022863,8.90619858683864,1.9596868087449));
#8351=CARTESIAN_POINT('Ctrl Pts',(0.362053629994299,8.92921241344647,1.97091779663247));
#8352=CARTESIAN_POINT('Ctrl Pts',(0.305288522462434,8.95198279685869,1.97967164017607));
#8353=CARTESIAN_POINT('Ctrl Pts',(0.24852341493057,8.97475318027092,1.98842548371968));
#8354=CARTESIAN_POINT('Ctrl Pts',(0.191583499816279,8.99727983925128,1.99470232098237));
#8355=CARTESIAN_POINT('Ctrl Pts',(0.13478536199593,9.01944575538499,1.99853290967558));
#8356=CARTESIAN_POINT('Ctrl Pts',(0.126823642530953,9.02255287848291,1.99906986517679));
#8357=CARTESIAN_POINT('Ctrl Pts',(0.118864689738311,9.02565293130725,1.99955883944013));
#8358=CARTESIAN_POINT('Ctrl Pts',(0.110909354270898,9.02874561007346,1.99999999999998));
#8359=CARTESIAN_POINT('Ctrl Pts',(0.0551132738224583,9.05043663164604,2.00309415362669));
#8360=CARTESIAN_POINT('Ctrl Pts',(-0.00112119342262139,9.07249129414105,
2.00386648849181));
#8361=CARTESIAN_POINT('Ctrl Pts',(-0.0575007498260162,9.09479997146124,
2.00224737448554));
#8362=CARTESIAN_POINT('Ctrl Pts',(-0.113804143546013,9.11707851217099,2.00063044772719));
#8363=CARTESIAN_POINT('Ctrl Pts',(-0.170251546657395,9.13961012942394,1.9966283083301));
#8364=CARTESIAN_POINT('Ctrl Pts',(-0.226538817610427,9.16227681169601,1.99022135677932));
#8365=CARTESIAN_POINT('Ctrl Pts',(-0.283517324852289,9.18522185234411,1.9837357246079));
#8366=CARTESIAN_POINT('Ctrl Pts',(-0.340330980885206,9.20830500956393,1.97478568883238));
#8367=CARTESIAN_POINT('Ctrl Pts',(-0.396662939850842,9.23139887703663,1.96340505169303));
#8368=CARTESIAN_POINT('Ctrl Pts',(-0.45230057804149,9.2542081005478,1.95216468684217));
#8369=CARTESIAN_POINT('Ctrl Pts',(-0.507467601047385,9.27702746883943,1.93855351319842));
#8370=CARTESIAN_POINT('Ctrl Pts',(-0.561868536423777,9.29973384085128,1.92265561987627));
#8371=CARTESIAN_POINT('Ctrl Pts',(-0.617287803117933,9.32286525352782,1.9064601338281));
#8372=CARTESIAN_POINT('Ctrl Pts',(-0.671911257251733,9.34587908013129,1.88789169563612));
#8373=CARTESIAN_POINT('Ctrl Pts',(-0.725448204184394,9.36864946353922,1.86709019276262));
#8374=CARTESIAN_POINT('Ctrl Pts',(-0.778985151117054,9.39141984694716,1.84628868988913));
#8375=CARTESIAN_POINT('Ctrl Pts',(-0.831434982716753,9.41394650592329,1.82325463286067));
#8376=CARTESIAN_POINT('Ctrl Pts',(-0.882538907293985,9.43611242205291,1.7981729510748));
#8377=CARTESIAN_POINT('Ctrl Pts',(-0.889702436358074,9.43921954515041,1.79465710844753));
#8378=CARTESIAN_POINT('Ctrl Pts',(-0.896839578794715,9.44231959797432,1.79110109618554));
#8379=CARTESIAN_POINT('Ctrl Pts',(-0.903949681684071,9.44541227674011,1.7875054847043));
#8380=CARTESIAN_POINT('Ctrl Pts',(-0.95381758159861,9.46710329831322,1.7622870601234));
#8381=CARTESIAN_POINT('Ctrl Pts',(-1.00290422623487,9.48915796080878,1.73483868811356));
#8382=CARTESIAN_POINT('Ctrl Pts',(-1.05092079733231,9.51146663812953,1.70524671604998));
#8383=CARTESIAN_POINT('Ctrl Pts',(-1.09887250322587,9.53374517883558,1.67569471954602));
#8384=CARTESIAN_POINT('Ctrl Pts',(-1.14575631859174,9.55627679608474,1.6440050636085));
#8385=CARTESIAN_POINT('Ctrl Pts',(-1.19129904936418,9.578943478353,1.61031284533437));
#8386=CARTESIAN_POINT('Ctrl Pts',(-1.23740106802143,9.60188851900177,1.57620686949291));
#8387=CARTESIAN_POINT('Ctrl Pts',(-1.28212811954179,9.62497167622228,1.54004908312946));
#8388=CARTESIAN_POINT('Ctrl Pts',(-1.32522270848299,9.64806554369569,1.50202718277195));
#8389=CARTESIAN_POINT('Ctrl Pts',(-1.36778613412685,9.67087476720111,1.46447392217784));
#8390=CARTESIAN_POINT('Ctrl Pts',(-1.4087565906697,9.693694135487,1.42510278853486));
#8391=CARTESIAN_POINT('Ctrl Pts',(-1.44792023602563,9.7164005074932,1.38413434137453));
#8392=CARTESIAN_POINT('Ctrl Pts',(-1.48781698582588,9.73953192017373,1.34239900567723));
#8393=CARTESIAN_POINT('Ctrl Pts',(-1.52583806565969,9.76254574678119,1.29900653942098));
#8394=CARTESIAN_POINT('Ctrl Pts',(-1.56180167031453,9.78531613019306,1.25422343602228));
#8395=CARTESIAN_POINT('Ctrl Pts',(-1.59776527496938,9.80808651360493,1.20944033262357));
#8396=CARTESIAN_POINT('Ctrl Pts',(-1.63167113305088,9.83061317258494,1.16326733827729));
#8397=CARTESIAN_POINT('Ctrl Pts',(-1.66338758908036,9.85277908871833,1.11599400238452));
#8398=CARTESIAN_POINT('Ctrl Pts',(-1.66783346591758,9.85588621181624,1.10936742882067));
#8399=CARTESIAN_POINT('Ctrl Pts',(-1.67223640644775,9.85898626464057,1.1027192606464));
#8400=CARTESIAN_POINT('Ctrl Pts',(-1.67659613043342,9.86207894340678,1.09605031831594));
#8401=CARTESIAN_POINT('Ctrl Pts',(-1.70717378629812,9.88376996497691,1.04927657203461));
#8402=CARTESIAN_POINT('Ctrl Pts',(-1.73595988153104,9.90582462746939,1.00096226227027));
#8403=CARTESIAN_POINT('Ctrl Pts',(-1.7627474658691,9.928133304787,0.951326577173604));
#8404=CARTESIAN_POINT('Ctrl Pts',(-1.78949886308675,9.95041184550169,0.90175794450282));
#8405=CARTESIAN_POINT('Ctrl Pts',(-1.81425661026064,9.97294346275971,0.850871989720727));
#8406=CARTESIAN_POINT('Ctrl Pts',(-1.83685166293795,9.99561014503689,0.798922307378422));
#8407=CARTESIAN_POINT('Ctrl Pts',(-1.85972419433764,10.0185551856843,0.746334656552911));
#8408=CARTESIAN_POINT('Ctrl Pts',(-1.88038006400666,10.0416383429035,0.692657569260229));
#8409=CARTESIAN_POINT('Ctrl Pts',(-1.89869012261463,10.0647322103755,0.638182343182895));
#8410=CARTESIAN_POINT('Ctrl Pts',(-1.91677450019885,10.087541433884,0.584378552683838));
#8411=CARTESIAN_POINT('Ctrl Pts',(-1.93257038954908,10.110360802173,0.529796922493951));
#8412=CARTESIAN_POINT('Ctrl Pts',(-1.94600287775226,10.1330671741823,0.474735383813648));
#8413=CARTESIAN_POINT('Ctrl Pts',(-1.95968680875531,10.1561985868591,0.418643147972745));
#8414=CARTESIAN_POINT('Ctrl Pts',(-1.97091779663961,10.1792124134628,0.36205362995384));
#8415=CARTESIAN_POINT('Ctrl Pts',(-1.97967164018081,10.201982796871,0.305288522431753));
#8416=CARTESIAN_POINT('Ctrl Pts',(-1.98842548372202,10.2247531802792,0.248523414909664));
#8417=CARTESIAN_POINT('Ctrl Pts',(-1.99470232098315,10.2472798392556,0.191583499805278));
#8418=CARTESIAN_POINT('Ctrl Pts',(-1.99853290967567,10.2694457553855,0.13478536199476));
#8419=CARTESIAN_POINT('Ctrl Pts',(-1.99906986517685,10.2725528784832,0.126823642530179));
#8420=CARTESIAN_POINT('Ctrl Pts',(-1.99955883944017,10.2756529313074,0.118864689737915));
#8421=CARTESIAN_POINT('Ctrl Pts',(-2.,10.2787456100735,0.110909354270896));
#8422=CARTESIAN_POINT('Ctrl Pts',(-2.00309415362599,10.3004366316412,0.0551132738350213));
#8423=CARTESIAN_POINT('Ctrl Pts',(-2.00386648849147,10.3224912941311,-0.00112119339731515));
#8424=CARTESIAN_POINT('Ctrl Pts',(-2.00224737448664,10.3447999714462,-0.0575007497879437));
#8425=CARTESIAN_POINT('Ctrl Pts',(-2.00063044772864,10.3670785121657,-0.113804143532892));
#8426=CARTESIAN_POINT('Ctrl Pts',(-1.99662830832979,10.3896101294287,-0.170251546669399));
#8427=CARTESIAN_POINT('Ctrl Pts',(-1.99022135677511,10.4122768117109,-0.226538817647384));
#8428=CARTESIAN_POINT('Ctrl Pts',(-1.983735724603,10.4352218523577,-0.283517324885871));
#8429=CARTESIAN_POINT('Ctrl Pts',(-1.97478568882708,10.4583050095762,-0.340330980915366));
#8430=CARTESIAN_POINT('Ctrl Pts',(-1.96340505168762,10.4813988770476,-0.396662939877621));
#8431=CARTESIAN_POINT('Ctrl Pts',(-1.95216468683779,10.5042081005551,-0.452300578059234));
#8432=CARTESIAN_POINT('Ctrl Pts',(-1.93855351319585,10.5270274688431,-0.507467601056206));
#8433=CARTESIAN_POINT('Ctrl Pts',(-1.92265561987624,10.5497338408513,-0.561868536423899));
#8434=CARTESIAN_POINT('Ctrl Pts',(-1.90646013382819,10.5728652535277,-0.617287803117652));
#8435=CARTESIAN_POINT('Ctrl Pts',(-1.88789169563638,10.595879080131,-0.671911257251014));
#8436=CARTESIAN_POINT('Ctrl Pts',(-1.86709019276308,10.6186494635387,-0.725448204183275));
#8437=CARTESIAN_POINT('Ctrl Pts',(-1.84628868988979,10.6414198469465,-0.778985151115534));
#8438=CARTESIAN_POINT('Ctrl Pts',(-1.82325463286158,10.6639465059224,-0.831434982714827));
#8439=CARTESIAN_POINT('Ctrl Pts',(-1.79817295107597,10.6861124220519,-0.882538907291692));
#8440=CARTESIAN_POINT('Ctrl Pts',(-1.79465710844833,10.6892195451497,-0.889702436356563));
#8441=CARTESIAN_POINT('Ctrl Pts',(-1.79110109618594,10.692319597974,-0.896839578793999));
#8442=CARTESIAN_POINT('Ctrl Pts',(-1.78750548470432,10.6954122767401,-0.903949681684119));
#8443=CARTESIAN_POINT('Ctrl Pts',(-1.76228706013068,10.7171032983069,-0.953817581584232));
#8444=CARTESIAN_POINT('Ctrl Pts',(-1.7348386881294,10.739157960796,-1.00290422620656));
#8445=CARTESIAN_POINT('Ctrl Pts',(-1.70524671607559,10.7614666381102,-1.05092079729075));
#8446=CARTESIAN_POINT('Ctrl Pts',(-1.67569471957146,10.7837451788171,-1.09887250318719));
#8447=CARTESIAN_POINT('Ctrl Pts',(-1.64400506363352,10.8062767960673,-1.14575631855595));
#8448=CARTESIAN_POINT('Ctrl Pts',(-1.61031284535875,10.8289434783366,-1.19129904933118));
#8449=CARTESIAN_POINT('Ctrl Pts',(-1.57620686951628,10.8518885189866,-1.23740106799179));
#8450=CARTESIAN_POINT('Ctrl Pts',(-1.54004908315154,10.8749716762084,-1.28212811951541));
#8451=CARTESIAN_POINT('Ctrl Pts',(-1.50202718279246,10.8980655436832,-1.32522270845973));
#8452=CARTESIAN_POINT('Ctrl Pts',(-1.46447392219654,10.9208747671901,-1.36778613410698));
#8453=CARTESIAN_POINT('Ctrl Pts',(-1.4251027885515,10.9436941354775,-1.408756590653));
#8454=CARTESIAN_POINT('Ctrl Pts',(-1.38413434138884,10.9664005074852,-1.44792023601195));
#8455=CARTESIAN_POINT('Ctrl Pts',(-1.3423990056896,10.9895319201671,-1.48781698581485));
#8456=CARTESIAN_POINT('Ctrl Pts',(-1.29900653943119,11.0125457467759,-1.52583806565114));
#8457=CARTESIAN_POINT('Ctrl Pts',(-1.25422343603018,11.035316130189,-1.5618016703082));
#8458=CARTESIAN_POINT('Ctrl Pts',(-1.20944033262918,11.0580865136022,-1.59776527496527));
#8459=CARTESIAN_POINT('Ctrl Pts',(-1.1632673382804,11.0806131725835,-1.6316711330488));
#8460=CARTESIAN_POINT('Ctrl Pts',(-1.11599400238502,11.1027790887181,-1.66338758908006));
#8461=CARTESIAN_POINT('Ctrl Pts',(-1.10936742882101,11.1058862118161,-1.66783346591739));
#8462=CARTESIAN_POINT('Ctrl Pts',(-1.10271926064657,11.1089862646405,-1.67223640644766));
#8463=CARTESIAN_POINT('Ctrl Pts',(-1.09605031831595,11.1120789434068,-1.67659613043343));
#8464=CARTESIAN_POINT('Ctrl Pts',(-1.04927657204784,11.1337699649708,-1.70717378628948));
#8465=CARTESIAN_POINT('Ctrl Pts',(-1.00096226229761,11.1558246274569,-1.73595988151476));
#8466=CARTESIAN_POINT('Ctrl Pts',(-0.951326577215707,11.1781333047681,-1.76274746584638));
#8467=CARTESIAN_POINT('Ctrl Pts',(-0.901757944540899,11.2004118454848,-1.78949886306773));
#8468=CARTESIAN_POINT('Ctrl Pts',(-0.85087198975444,11.2229434627449,-1.814256610245));
#8469=CARTESIAN_POINT('Ctrl Pts',(-0.798922307407508,11.2456101450242,-1.8368516629253));
#8470=CARTESIAN_POINT('Ctrl Pts',(-0.746334656580119,11.2685551856726,-1.8597241943268));
#8471=CARTESIAN_POINT('Ctrl Pts',(-0.692657569285422,11.2916383428927,-1.88038006399746));
#8472=CARTESIAN_POINT('Ctrl Pts',(-0.638182343205964,11.3147322103657,-1.89869012260688));
#8473=CARTESIAN_POINT('Ctrl Pts',(-0.584378552711461,11.3375414338724,-1.91677450019031));
#8474=CARTESIAN_POINT('Ctrl Pts',(-0.529796922526239,11.3603608021596,-1.9325703895401));
#8475=CARTESIAN_POINT('Ctrl Pts',(-0.474735383850581,11.3830671741671,-1.94600287774326));
#8476=CARTESIAN_POINT('Ctrl Pts',(-0.418643148004073,11.4061985868463,-1.9596868087488));
#8477=CARTESIAN_POINT('Ctrl Pts',(-0.36205362997942,11.4292124134525,-1.97091779663511));
#8478=CARTESIAN_POINT('Ctrl Pts',(-0.30528852245147,11.4519827968631,-1.97967164017779));
#8479=CARTESIAN_POINT('Ctrl Pts',(-0.248523414923521,11.4747531802737,-1.98842548372048));
#8480=CARTESIAN_POINT('Ctrl Pts',(-0.191583499813202,11.4972798392525,-1.99470232098259));
#8481=CARTESIAN_POINT('Ctrl Pts',(-0.13478536199678,11.5194457553847,-1.99853290967556));
#8482=CARTESIAN_POINT('Ctrl Pts',(-0.126823642531537,11.5225528784827,-1.99906986517679));
#8483=CARTESIAN_POINT('Ctrl Pts',(-0.118864689738596,11.5256529313072,-1.99955883944015));
#8484=CARTESIAN_POINT('Ctrl Pts',(-0.110909354270918,11.5287456100735,-2.00000000000001));
#8485=CARTESIAN_POINT('Ctrl Pts',(-0.0551132738492376,11.5504366316357,
-2.00309415362522));
#8486=CARTESIAN_POINT('Ctrl Pts',(0.00112119336864007,11.5724912941199,
-2.0038664884911));
#8487=CARTESIAN_POINT('Ctrl Pts',(0.0575007497448667,11.5947999714292,-2.00224737448789));
#8488=CARTESIAN_POINT('Ctrl Pts',(0.113804143493782,11.6170785121502,-2.00063044773099));
#8489=CARTESIAN_POINT('Ctrl Pts',(0.170251546634363,11.6396101294147,-1.9966283083329));
#8490=CARTESIAN_POINT('Ctrl Pts',(0.226538817616414,11.6622768116985,-1.99022135677864));
#8491=CARTESIAN_POINT('Ctrl Pts',(0.283517324857556,11.6852218523463,-1.98373572460713));
#8492=CARTESIAN_POINT('Ctrl Pts',(0.340330980889751,11.7083050095658,-1.97478568883157));
#8493=CARTESIAN_POINT('Ctrl Pts',(0.396662939854681,11.7313988770382,-1.96340505169226));
#8494=CARTESIAN_POINT('Ctrl Pts',(0.452300578040246,11.7542081005473,-1.95216468684231));
#8495=CARTESIAN_POINT('Ctrl Pts',(0.507467601041112,11.7770274688369,-1.93855351319992));
#8496=CARTESIAN_POINT('Ctrl Pts',(0.561868536412669,11.7997338408467,-1.92265561987953));
#8497=CARTESIAN_POINT('Ctrl Pts',(0.617287803108415,11.8228652535238,-1.90646013383125));
#8498=CARTESIAN_POINT('Ctrl Pts',(0.671911257243793,11.8458790801279,-1.88789169563901));
#8499=CARTESIAN_POINT('Ctrl Pts',(0.725448204177951,11.8686494635365,-1.86709019276516));
#8500=CARTESIAN_POINT('Ctrl Pts',(0.778985151112109,11.891419846945,-1.8462886898913));
#8501=CARTESIAN_POINT('Ctrl Pts',(0.831434982713284,11.9139465059218,-1.82325463286234));
#8502=CARTESIAN_POINT('Ctrl Pts',(0.882538907291871,11.936112422052,-1.79817295107588));
#8503=CARTESIAN_POINT('Ctrl Pts',(0.889702436356676,11.9392195451498,-1.79465710844827));
#8504=CARTESIAN_POINT('Ctrl Pts',(0.896839578794011,11.942319597974,-1.79110109618594));
#8505=CARTESIAN_POINT('Ctrl Pts',(0.903949681684077,11.9454122767401,-1.78750548470435));
#8506=CARTESIAN_POINT('Ctrl Pts',(0.953817581596336,11.9671032983122,-1.7622870601246));
#8507=CARTESIAN_POINT('Ctrl Pts',(1.00290422623042,11.9891579608068,-1.73483868811609));
#8508=CARTESIAN_POINT('Ctrl Pts',(1.05092079732578,12.0114666381265,-1.70524671605404));
#8509=CARTESIAN_POINT('Ctrl Pts',(1.09887250322481,12.033745178835,-1.67569471954696));
#8510=CARTESIAN_POINT('Ctrl Pts',(1.14575631859591,12.0562767960867,-1.64400506360586));
#8511=CARTESIAN_POINT('Ctrl Pts',(1.19129904937325,12.0789434783575,-1.61031284532769));
#8512=CARTESIAN_POINT('Ctrl Pts',(1.23740106802966,12.101888519006,-1.57620686948646));
#8513=CARTESIAN_POINT('Ctrl Pts',(1.28212811954919,12.1249716762261,-1.5400490831233));
#8514=CARTESIAN_POINT('Ctrl Pts',(1.3252227084896,12.1480655436992,-1.50202718276616));
#8515=CARTESIAN_POINT('Ctrl Pts',(1.36778613413641,12.1708747672063,-1.46447392216911));
#8516=CARTESIAN_POINT('Ctrl Pts',(1.40875659068193,12.1936941354938,-1.42510278852297));
#8517=CARTESIAN_POINT('Ctrl Pts',(1.44792023604029,12.2164005075017,-1.38413434135923));
#8518=CARTESIAN_POINT('Ctrl Pts',(1.4878169858378,12.2395319201809,-1.3423990056639));
#8519=CARTESIAN_POINT('Ctrl Pts',(1.52583806566909,12.262545746787,-1.29900653940983));
#8520=CARTESIAN_POINT('Ctrl Pts',(1.5618016703216,12.2853161301975,-1.25422343601351));
#8521=CARTESIAN_POINT('Ctrl Pts',(1.59776527497412,12.3080865136081,-1.2094403326172));
#8522=CARTESIAN_POINT('Ctrl Pts',(1.63167113305352,12.3306131725868,-1.16326733827348));
#8523=CARTESIAN_POINT('Ctrl Pts',(1.66338758908114,12.3527790887189,-1.11599400238341));
#8524=CARTESIAN_POINT('Ctrl Pts',(1.6678334659181,12.3558862118166,-1.10936742881995));
#8525=CARTESIAN_POINT('Ctrl Pts',(1.67223640644802,12.3589862646408,-1.10271926064603));
#8526=CARTESIAN_POINT('Ctrl Pts',(1.67659613043343,12.3620789434068,-1.09605031831597));
#8527=CARTESIAN_POINT('Ctrl Pts',(1.70717378629813,12.3837699649769,-1.04927657203466));
#8528=CARTESIAN_POINT('Ctrl Pts',(1.73595988153105,12.4058246274694,-1.00096226227032));
#8529=CARTESIAN_POINT('Ctrl Pts',(1.76274746586913,12.428133304787,-0.95132657717363));
#8530=CARTESIAN_POINT('Ctrl Pts',(1.78949886307494,12.4504118454918,-0.901757944524793));
#8531=CARTESIAN_POINT('Ctrl Pts',(1.81425661023879,12.4729434627398,-0.850871989765756));
#8532=CARTESIAN_POINT('Ctrl Pts',(1.83685166290801,12.4956101450068,-0.798922307447371));
#8533=CARTESIAN_POINT('Ctrl Pts',(1.85972419431202,12.5185551856565,-0.746334656617319));
#8534=CARTESIAN_POINT('Ctrl Pts',(1.88038006398497,12.541638342878,-0.692657569319742));
#8535=CARTESIAN_POINT('Ctrl Pts',(1.8986901225964,12.5647322103524,-0.638182343237275));
#8536=CARTESIAN_POINT('Ctrl Pts',(1.91677450018556,12.5875414338653,-0.584378552728654));
#8537=CARTESIAN_POINT('Ctrl Pts',(1.93257038953987,12.6103608021586,-0.529796922528835));
#8538=CARTESIAN_POINT('Ctrl Pts',(1.94600287774627,12.6330671741721,-0.474735383838342));
#8539=CARTESIAN_POINT('Ctrl Pts',(1.95968680875091,12.6561985868504,-0.418643147994041));
#8540=CARTESIAN_POINT('Ctrl Pts',(1.9709177966365,12.6792124134557,-0.36205362997159));
#8541=CARTESIAN_POINT('Ctrl Pts',(1.97967164017866,12.7019827968653,-0.305288522445932));
#8542=CARTESIAN_POINT('Ctrl Pts',(1.98842548372083,12.724753180275,-0.248523414920275));
#8543=CARTESIAN_POINT('Ctrl Pts',(1.99470232098261,12.7472798392529,-0.191583499812266));
#8544=CARTESIAN_POINT('Ctrl Pts',(1.99853290967546,12.7694457553842,-0.134785361998167));
#8545=CARTESIAN_POINT('Ctrl Pts',(1.99906986517673,12.7725528784824,-0.126823642532455));
#8546=CARTESIAN_POINT('Ctrl Pts',(1.99955883944012,12.775652931307,-0.118864689739083));
#8547=CARTESIAN_POINT('Ctrl Pts',(2.00000000000001,12.7787456100735,-0.110909354270942));
#8548=CARTESIAN_POINT('Ctrl Pts',(2.00309415362581,12.8004366316398,-0.0551132738386595));
#8549=CARTESIAN_POINT('Ctrl Pts',(2.00386648849138,12.8224912941283,0.00112119338997931));
#8550=CARTESIAN_POINT('Ctrl Pts',(2.00224737448696,12.8447999714419,0.0575007497769627));
#8551=CARTESIAN_POINT('Ctrl Pts',(2.00063044773012,12.8670785121497,0.113804143492278));
#8552=CARTESIAN_POINT('Ctrl Pts',(1.99662830833494,12.8896101294007,0.170251546599096));
#8553=CARTESIAN_POINT('Ctrl Pts',(1.99022135678646,12.9122768116708,0.22653881754767));
#8554=CARTESIAN_POINT('Ctrl Pts',(1.98373572461622,12.935221852321,0.283517324795138));
#8555=CARTESIAN_POINT('Ctrl Pts',(1.97478568884141,12.958305009543,0.340330980833699));
#8556=CARTESIAN_POINT('Ctrl Pts',(1.96340505170229,12.9813988770179,0.396662939804991));
#8557=CARTESIAN_POINT('Ctrl Pts',(1.95216468685348,13.0042081005275,0.45230057799216));
#8558=CARTESIAN_POINT('Ctrl Pts',(1.93855351321208,13.0270274688176,0.507467600994751));
#8559=CARTESIAN_POINT('Ctrl Pts',(1.92265561989256,13.049733840828,0.561868536368022));
#8560=CARTESIAN_POINT('Ctrl Pts',(1.90646013384314,13.0728652535087,0.617287803072458));
#8561=CARTESIAN_POINT('Ctrl Pts',(1.88789169564903,13.0958790801163,0.671911257216334));
#8562=CARTESIAN_POINT('Ctrl Pts',(1.8670901927726,13.1186494635283,0.725448204158746));
#8563=CARTESIAN_POINT('Ctrl Pts',(1.84628868989617,13.1414198469403,0.77898515110116));
#8564=CARTESIAN_POINT('Ctrl Pts',(1.82325463286394,13.1639465059205,0.831434982710294));
#8565=CARTESIAN_POINT('Ctrl Pts',(1.79817295107358,13.186112422054,0.882538907296488));
#8566=CARTESIAN_POINT('Ctrl Pts',(1.79465710844671,13.1892195451511,0.889702436359735));
#8567=CARTESIAN_POINT('Ctrl Pts',(1.79110109618515,13.1923195979747,0.896839578795523));
#8568=CARTESIAN_POINT('Ctrl Pts',(1.78750548470433,13.1954122767401,0.903949681684049));
#8569=CARTESIAN_POINT('Ctrl Pts',(1.76228706012136,13.217103298315,0.95381758160267));
#8570=CARTESIAN_POINT('Ctrl Pts',(1.73483868810907,13.2391579608124,1.00290422624289));
#8571=CARTESIAN_POINT('Ctrl Pts',(1.70524671604273,13.261466638135,1.05092079734406));
#8572=CARTESIAN_POINT('Ctrl Pts',(1.67569471954095,13.2837451788392,1.09887250323334));
#8573=CARTESIAN_POINT('Ctrl Pts',(1.64400506360599,13.3062767960864,1.14575631859508));
#8574=CARTESIAN_POINT('Ctrl Pts',(1.61031284533477,13.3289434783527,1.1912990493636));
#8575=CARTESIAN_POINT('Ctrl Pts',(1.57620686949313,13.3518885190016,1.23740106802114));
#8576=CARTESIAN_POINT('Ctrl Pts',(1.54004908312944,13.3749716762223,1.28212811954181));
#8577=CARTESIAN_POINT('Ctrl Pts',(1.5020271827717,13.3980655436958,1.32522270848326));
#8578=CARTESIAN_POINT('Ctrl Pts',(1.46447392217234,13.4208747672044,1.36778613413307));
#8579=CARTESIAN_POINT('Ctrl Pts',(1.42510278852357,13.4436941354935,1.40875659068142));
#8580=CARTESIAN_POINT('Ctrl Pts',(1.38413434135706,13.4664005075029,1.44792023604233));
#8581=CARTESIAN_POINT('Ctrl Pts',(1.34239900566176,13.489531920182,1.48781698583969));
#8582=CARTESIAN_POINT('Ctrl Pts',(1.29900653940771,13.5125457467881,1.52583806567085));
#8583=CARTESIAN_POINT('Ctrl Pts',(1.25422343601143,13.5353161301986,1.56180167032324));
#8584=CARTESIAN_POINT('Ctrl Pts',(1.20944033261515,13.5580865136091,1.59776527497563));
#8585=CARTESIAN_POINT('Ctrl Pts',(1.16326733827152,13.5806131725877,1.63167113305488));
#8586=CARTESIAN_POINT('Ctrl Pts',(1.11599400238149,13.6027790887198,1.66338758908239));
#8587=CARTESIAN_POINT('Ctrl Pts',(1.10936742881865,13.6058862118172,1.66783346591892));
#8588=CARTESIAN_POINT('Ctrl Pts',(1.1027192606454,13.6089862646411,1.6722364064484));
#8589=CARTESIAN_POINT('Ctrl Pts',(1.09605031831597,13.6120789434068,1.67659613043339));
#8590=CARTESIAN_POINT('Ctrl Pts',(1.04927657204321,13.6337699649729,1.7071737862925));
#8591=CARTESIAN_POINT('Ctrl Pts',(1.00096226228807,13.6558246274613,1.73595988152044));
#8592=CARTESIAN_POINT('Ctrl Pts',(0.951326577201009,13.6781333047747,1.76274746585431));
#8593=CARTESIAN_POINT('Ctrl Pts',(0.901757944547673,13.7004118454817,1.78949886306355));
#8594=CARTESIAN_POINT('Ctrl Pts',(0.850871989783864,13.7229434627318,1.81425661023042));
#8595=CARTESIAN_POINT('Ctrl Pts',(0.798922307460442,13.7456101450011,1.83685166290228));
#8596=CARTESIAN_POINT('Ctrl Pts',(0.746334656629352,13.7685551856513,1.85972419430719));
#8597=CARTESIAN_POINT('Ctrl Pts',(0.692657569330676,13.7916383428733,1.88038006398094));
#8598=CARTESIAN_POINT('Ctrl Pts',(0.638182343247026,13.8147322103483,1.89869012259308));
#8599=CARTESIAN_POINT('Ctrl Pts',(0.584378552748106,13.837541433857,1.91677450017928));
#8600=CARTESIAN_POINT('Ctrl Pts',(0.52979692255822,13.8603608021463,1.93257038953147));
#8601=CARTESIAN_POINT('Ctrl Pts',(0.474735383877795,13.8830671741558,1.94600287773661));
#8602=CARTESIAN_POINT('Ctrl Pts',(0.418643148026858,13.906198586837,1.95968680874406));
#8603=CARTESIAN_POINT('Ctrl Pts',(0.362053629997598,13.9292124134452,1.97091779663188));
#8604=CARTESIAN_POINT('Ctrl Pts',(0.305288522465042,13.9519827968577,1.97967164017568));
#8605=CARTESIAN_POINT('Ctrl Pts',(0.248523414932487,13.9747531802702,1.98842548371947));
#8606=CARTESIAN_POINT('Ctrl Pts',(0.191583499817506,13.9972798392508,1.99470232098228));
#8607=CARTESIAN_POINT('Ctrl Pts',(0.134785361996449,14.0194457553848,1.99853290967556));
#8608=CARTESIAN_POINT('Ctrl Pts',(0.126823642531306,14.0225528784828,1.99906986517678));
#8609=CARTESIAN_POINT('Ctrl Pts',(0.118864689738491,14.0256529313072,1.99955883944013));
#8610=CARTESIAN_POINT('Ctrl Pts',(0.110909354270912,14.0287456100735,1.99999999999999));
#8611=CARTESIAN_POINT('Ctrl Pts',(0.0551132738272201,14.0504366316442,2.00309415362644));
#8612=CARTESIAN_POINT('Ctrl Pts',(-0.00112119341301478,14.0724912941373,
2.00386648849169));
#8613=CARTESIAN_POINT('Ctrl Pts',(-0.0575007498115822,14.0947999714556,
2.00224737448596));
#8614=CARTESIAN_POINT('Ctrl Pts',(-0.113804143535633,14.1170785121669,2.0006304477279));
#8615=CARTESIAN_POINT('Ctrl Pts',(-0.170251546651125,14.1396101294215,1.99662830833074));
#8616=CARTESIAN_POINT('Ctrl Pts',(-0.226538817608238,14.1622768116952,1.99022135677956));
#8617=CARTESIAN_POINT('Ctrl Pts',(-0.283517324850062,14.1852218523432,1.9837357246082));
#8618=CARTESIAN_POINT('Ctrl Pts',(-0.340330980882965,14.2083050095631,1.97478568883275));
#8619=CARTESIAN_POINT('Ctrl Pts',(-0.396662939848583,14.2313988770357,1.96340505169347));
#8620=CARTESIAN_POINT('Ctrl Pts',(-0.452300578033097,14.2542081005444,1.95216468684391));
#8621=CARTESIAN_POINT('Ctrl Pts',(-0.507467601032979,14.2770274688335,1.93855351320199));
#8622=CARTESIAN_POINT('Ctrl Pts',(-0.561868536403543,14.2997338408429,1.92265561988216));
#8623=CARTESIAN_POINT('Ctrl Pts',(-0.617287803100842,14.3228652535207,1.90646013383371));
#8624=CARTESIAN_POINT('Ctrl Pts',(-0.671911257237724,14.3458790801254,1.88789169564117));
#8625=CARTESIAN_POINT('Ctrl Pts',(-0.725448204173397,14.3686494635346,1.86709019276687));
#8626=CARTESIAN_POINT('Ctrl Pts',(-0.778985151109067,14.3914198469438,1.84628868989257));
#8627=CARTESIAN_POINT('Ctrl Pts',(-0.831434982711695,14.4139465059212,1.82325463286305));
#8628=CARTESIAN_POINT('Ctrl Pts',(-0.882538907291681,14.436112422052,1.79817295107591));
#8629=CARTESIAN_POINT('Ctrl Pts',(-0.889702436356552,14.4392195451498,1.79465710844826));
#8630=CARTESIAN_POINT('Ctrl Pts',(-0.896839578793936,14.4423195979741,1.79110109618591));
#8631=CARTESIAN_POINT('Ctrl Pts',(-0.903949681684057,14.4454122767402,1.78750548470429));
#8632=CARTESIAN_POINT('Ctrl Pts',(-0.953817581601736,14.4671032983147,1.7622870601218));
#8633=CARTESIAN_POINT('Ctrl Pts',(-1.00290422624106,14.4891579608116,1.73483868811007));
#8634=CARTESIAN_POINT('Ctrl Pts',(-1.05092079734141,14.5114666381338,1.70524671604434));
#8635=CARTESIAN_POINT('Ctrl Pts',(-1.09887250323354,14.5337451788393,1.67569471954091));
#8636=CARTESIAN_POINT('Ctrl Pts',(-1.14575631859805,14.5562767960879,1.64400506360401));
#8637=CARTESIAN_POINT('Ctrl Pts',(-1.19129904936917,14.5789434783555,1.61031284533064));
#8638=CARTESIAN_POINT('Ctrl Pts',(-1.23740106802587,14.6018885190041,1.57620686948938));
#8639=CARTESIAN_POINT('Ctrl Pts',(-1.28212811954568,14.6249716762243,1.54004908312616));
#8640=CARTESIAN_POINT('Ctrl Pts',(-1.32522270848637,14.6480655436975,1.50202718276894));
#8641=CARTESIAN_POINT('Ctrl Pts',(-1.36778613413622,14.6708747672062,1.46447392216936));
#8642=CARTESIAN_POINT('Ctrl Pts',(-1.40875659068459,14.6936941354953,1.42510278852042));
#8643=CARTESIAN_POINT('Ctrl Pts',(-1.44792023604552,14.7164005075047,1.38413434135369));
#8644=CARTESIAN_POINT('Ctrl Pts',(-1.48781698584175,14.7395319201833,1.34239900565937));
#8645=CARTESIAN_POINT('Ctrl Pts',(-1.52583806567186,14.7625457467887,1.29900653940642));
#8646=CARTESIAN_POINT('Ctrl Pts',(-1.56180167032331,14.7853161301986,1.2542234360113));
#8647=CARTESIAN_POINT('Ctrl Pts',(-1.59776527497476,14.8080865136085,1.20944033261618));
#8648=CARTESIAN_POINT('Ctrl Pts',(-1.63167113305322,14.8306131725866,1.16326733827374));
#8649=CARTESIAN_POINT('Ctrl Pts',(-1.66338758908002,14.8527790887181,1.11599400238499));
#8650=CARTESIAN_POINT('Ctrl Pts',(-1.66783346591735,14.8558862118161,1.10936742882098));
#8651=CARTESIAN_POINT('Ctrl Pts',(-1.67223640644763,14.8589862646405,1.10271926064654));
#8652=CARTESIAN_POINT('Ctrl Pts',(-1.67659613043341,14.8620789434068,1.09605031831592));
#8653=CARTESIAN_POINT('Ctrl Pts',(-1.70717378629289,14.8837699649732,1.04927657204259));
#8654=CARTESIAN_POINT('Ctrl Pts',(-1.73595988152119,14.9058246274618,1.00096226228679));
#8655=CARTESIAN_POINT('Ctrl Pts',(-1.76274746585537,14.9281333047756,0.951326577199046));
#8656=CARTESIAN_POINT('Ctrl Pts',(-1.78949886307631,14.9504118454923,0.901757944523873));
#8657=CARTESIAN_POINT('Ctrl Pts',(-1.81425661025313,14.9729434627525,0.850871989737085));
#8658=CARTESIAN_POINT('Ctrl Pts',(-1.83685166293298,14.9956101450319,0.798922307389847));
#8659=CARTESIAN_POINT('Ctrl Pts',(-1.85972419433329,15.0185551856796,0.746334656563815));
#8660=CARTESIAN_POINT('Ctrl Pts',(-1.88038006400286,15.041638342899,0.692657569270616));
#8661=CARTESIAN_POINT('Ctrl Pts',(-1.89869012261134,15.0647322103713,0.638182343192682));
#8662=CARTESIAN_POINT('Ctrl Pts',(-1.9167745001939,15.0875414338774,0.584378552699522));
#8663=CARTESIAN_POINT('Ctrl Pts',(-1.93257038954294,15.110360802164,0.529796922515685));
#8664=CARTESIAN_POINT('Ctrl Pts',(-1.94600287774547,15.1330671741708,0.474735383841463));
#8665=CARTESIAN_POINT('Ctrl Pts',(-1.95968680875032,15.1561985868493,0.418643147996668));
#8666=CARTESIAN_POINT('Ctrl Pts',(-1.97091779663606,15.1792124134548,0.362053629973788));
#8667=CARTESIAN_POINT('Ctrl Pts',(-1.97967164017836,15.2019827968646,0.305288522447653));
#8668=CARTESIAN_POINT('Ctrl Pts',(-1.98842548372065,15.2247531802745,0.248523414921518));
#8669=CARTESIAN_POINT('Ctrl Pts',(-1.99470232098253,15.2472798392525,0.191583499813044));
#8670=CARTESIAN_POINT('Ctrl Pts',(-1.99853290967543,15.269445755384,0.134785361998419));
#8671=CARTESIAN_POINT('Ctrl Pts',(-1.9990698651767,15.2725528784823,0.126823642532606));
#8672=CARTESIAN_POINT('Ctrl Pts',(-1.9995588394401,15.2756529313069,0.118864689739133));
#8673=CARTESIAN_POINT('Ctrl Pts',(-2.,15.2787456100735,0.110909354270892));
#8674=CARTESIAN_POINT('Ctrl Pts',(-2.0030941536263,15.3004366316433,0.0551132738295713));
#8675=CARTESIAN_POINT('Ctrl Pts',(-2.00386648849161,15.3224912941354,-0.0011211934082543));
#8676=CARTESIAN_POINT('Ctrl Pts',(-2.00224737448615,15.3447999714527,-0.0575007498044029));
#8677=CARTESIAN_POINT('Ctrl Pts',(-2.00063044772843,15.3670785121621,-0.113804143523693));
#8678=CARTESIAN_POINT('Ctrl Pts',(-1.99662830833203,15.3896101294147,-0.170251546634409));
#8679=CARTESIAN_POINT('Ctrl Pts',(-1.99022135678199,15.4122768116865,-0.226538817586818));
#8680=CARTESIAN_POINT('Ctrl Pts',(-1.98373572461104,15.4352218523353,-0.28351732483059));
#8681=CARTESIAN_POINT('Ctrl Pts',(-1.97478568883582,15.4583050095559,-0.340330980865487));
#8682=CARTESIAN_POINT('Ctrl Pts',(-1.96340505169662,15.4813988770293,-0.396662939833066));
#8683=CARTESIAN_POINT('Ctrl Pts',(-1.95216468684707,15.5042081005389,-0.452300578019836));
#8684=CARTESIAN_POINT('Ctrl Pts',(-1.93855351320496,15.5270274688289,-0.507467601021982));
#8685=CARTESIAN_POINT('Ctrl Pts',(-1.92265561988476,15.5497338408392,-0.561868536394774));
#8686=CARTESIAN_POINT('Ctrl Pts',(-1.90646013383607,15.5728652535177,-0.61728780309387));
#8687=CARTESIAN_POINT('Ctrl Pts',(-1.88789169564315,15.5958790801231,-0.671911257232479));
#8688=CARTESIAN_POINT('Ctrl Pts',(-1.86709019276833,15.618649463533,-0.725448204169802));
#8689=CARTESIAN_POINT('Ctrl Pts',(-1.84628868989351,15.6414198469429,-0.778985151107124));
#8690=CARTESIAN_POINT('Ctrl Pts',(-1.82325463286332,15.6639465059209,-0.831434982711367));
#8691=CARTESIAN_POINT('Ctrl Pts',(-1.79817295107539,15.6861124220524,-0.882538907292868));
#8692=CARTESIAN_POINT('Ctrl Pts',(-1.79465710844794,15.6892195451501,-0.889702436357341));
#8693=CARTESIAN_POINT('Ctrl Pts',(-1.79110109618575,15.6923195979742,-0.896839578794375));
#8694=CARTESIAN_POINT('Ctrl Pts',(-1.78750548470433,15.6954122767401,-0.90394968168411));
#8695=CARTESIAN_POINT('Ctrl Pts',(-1.76228694372129,15.7171033984337,-0.953817811776782));
#8696=CARTESIAN_POINT('Ctrl Pts',(-1.7348384346849,15.7391581644147,-1.00290467937114));
#8697=CARTESIAN_POINT('Ctrl Pts',(-1.70524630628172,15.7614669470439,-1.05092146223084));
#8698=CARTESIAN_POINT('Ctrl Pts',(-1.67569381899318,15.7837458452052,-1.09887392262047));
#8699=CARTESIAN_POINT('Ctrl Pts',(-1.64400360450942,15.8062778274659,-1.14575845707494));
#8700=CARTESIAN_POINT('Ctrl Pts',(-1.6103107669867,15.8289448765748,-1.19130185872078));
#8701=CARTESIAN_POINT('Ctrl Pts',(-1.57500230505964,15.8526988462403,-1.23902913790753));
#8702=CARTESIAN_POINT('Ctrl Pts',(-1.53749452927016,15.876600854243,-1.28528257992073));
#8703=CARTESIAN_POINT('Ctrl Pts',(-1.49799656462519,15.9005094948716,-1.32977711562351));
#8704=CARTESIAN_POINT('Ctrl Pts',(-1.46031104530288,15.9233210383646,-1.3722299280668));
#8705=CARTESIAN_POINT('Ctrl Pts',(-1.42081463632739,15.9461382987637,-1.41308123426202));
#8706=CARTESIAN_POINT('Ctrl Pts',(-1.37972921806466,15.9688381759537,-1.45211851089488));
#8707=CARTESIAN_POINT('Ctrl Pts',(-1.33864416295559,15.9915378524997,-1.49115544247757));
#8708=CARTESIAN_POINT('Ctrl Pts',(-1.29597073421029,16.0141198611299,-1.52837796258682));
#8709=CARTESIAN_POINT('Ctrl Pts',(-1.25196176236387,16.0364652934131,-1.56361524373601));
#8710=CARTESIAN_POINT('Ctrl Pts',(-1.20788630186401,16.058844485124,-1.5989057612885));
#8711=CARTESIAN_POINT('Ctrl Pts',(-1.16247193926722,16.0809861259264,-1.63220477934516));
#8712=CARTESIAN_POINT('Ctrl Pts',(-1.11599400092916,16.1027790894007,-1.66338759005681));
#8713=CARTESIAN_POINT('Ctrl Pts',(-1.10936742784726,16.1058862122702,-1.66783346656228));
#8714=CARTESIAN_POINT('Ctrl Pts',(-1.10271926015816,16.108986264867,-1.67223640676696));
#8715=CARTESIAN_POINT('Ctrl Pts',(-1.09605031831592,16.1120789434068,-1.67659613043346));
#8716=CARTESIAN_POINT('Ctrl Pts',(-1.04927657203949,16.1337699649747,-1.70717378629496));
#8717=CARTESIAN_POINT('Ctrl Pts',(-1.00096226228034,16.1558246274648,-1.73595988152507));
#8718=CARTESIAN_POINT('Ctrl Pts',(-0.951326577189098,16.17813330478,-1.76274746586078));
#8719=CARTESIAN_POINT('Ctrl Pts',(-0.901757944534647,16.2004118454875,-1.78949886307018));
#8720=CARTESIAN_POINT('Ctrl Pts',(-0.850871989769685,16.2229434627381,-1.81425661023715));
#8721=CARTESIAN_POINT('Ctrl Pts',(-0.798922307445119,16.2456101450078,-1.83685166290899));
#8722=CARTESIAN_POINT('Ctrl Pts',(-0.746334656615035,16.2685551856575,-1.85972419431294));
#8723=CARTESIAN_POINT('Ctrl Pts',(-0.69265756931742,16.291638342879,-1.88038006398583));
#8724=CARTESIAN_POINT('Ctrl Pts',(-0.638182343234895,16.3147322103534,-1.89869012259721));
#8725=CARTESIAN_POINT('Ctrl Pts',(-0.584378552734248,16.3375414338629,-1.91677450018361));
#8726=CARTESIAN_POINT('Ctrl Pts',(-0.52979692254261,16.3603608021528,-1.93257038953586));
#8727=CARTESIAN_POINT('Ctrl Pts',(-0.474735383860447,16.383067174163,-1.9460028777409));
#8728=CARTESIAN_POINT('Ctrl Pts',(-0.41864314801215,16.406198586843,-1.95968680874718));
#8729=CARTESIAN_POINT('Ctrl Pts',(-0.362053629985638,16.42921241345,-1.97091779663406));
#8730=CARTESIAN_POINT('Ctrl Pts',(-0.305288522455835,16.4519827968614,-1.97967164017715));
#8731=CARTESIAN_POINT('Ctrl Pts',(-0.248523414926033,16.4747531802727,-1.98842548372025));
#8732=CARTESIAN_POINT('Ctrl Pts',(-0.191583499813838,16.4972798392523,-1.99470232098261));
#8733=CARTESIAN_POINT('Ctrl Pts',(-0.134785361995554,16.5194457553852,-1.99853290967566));
#8734=CARTESIAN_POINT('Ctrl Pts',(-0.126823642530709,16.522552878483,-1.99906986517686));
#8735=CARTESIAN_POINT('Ctrl Pts',(-0.118864689738204,16.5256529313073,-1.99955883944019));
#8736=CARTESIAN_POINT('Ctrl Pts',(-0.110909354270924,16.5287456100735,-2.00000000000003));
#8737=CARTESIAN_POINT('Ctrl Pts',(-0.0551132738242786,16.5504366316454,
-2.00309415362662));
#8738=CARTESIAN_POINT('Ctrl Pts',(0.00112119341897333,16.5724912941397,
-2.00386648849178));
#8739=CARTESIAN_POINT('Ctrl Pts',(0.0575007498205267,16.5947999714591,-2.00224737448572));
#8740=CARTESIAN_POINT('Ctrl Pts',(0.113804143545222,16.6170785121707,-2.00063044772738));
#8741=CARTESIAN_POINT('Ctrl Pts',(0.170251546661352,16.6396101294255,-1.99662830832989));
#8742=CARTESIAN_POINT('Ctrl Pts',(0.226538817619078,16.6622768116995,-1.99022135677833));
#8743=CARTESIAN_POINT('Ctrl Pts',(0.283517324860016,16.6852218523473,-1.98373572460676));
#8744=CARTESIAN_POINT('Ctrl Pts',(0.340330980892024,16.7083050095667,-1.97478568883116));
#8745=CARTESIAN_POINT('Ctrl Pts',(0.396662939856765,16.7313988770391,-1.96340505169182));
#8746=CARTESIAN_POINT('Ctrl Pts',(0.452300578040149,16.7542081005473,-1.95216468684225));
#8747=CARTESIAN_POINT('Ctrl Pts',(0.507467601038886,16.7770274688359,-1.93855351320042));
#8748=CARTESIAN_POINT('Ctrl Pts',(0.56186853640834,16.7997338408448,-1.92265561988078));
#8749=CARTESIAN_POINT('Ctrl Pts',(0.617287803104898,16.8228652535224,-1.9064601338324));
#8750=CARTESIAN_POINT('Ctrl Pts',(0.671911257241057,16.8458790801268,-1.88789169564));
#8751=CARTESIAN_POINT('Ctrl Pts',(0.725448204175984,16.8686494635356,-1.86709019276591));
#8752=CARTESIAN_POINT('Ctrl Pts',(0.778985151110912,16.8914198469445,-1.84628868989182));
#8753=CARTESIAN_POINT('Ctrl Pts',(0.831434982712801,16.9139465059216,-1.82325463286257));
#8754=CARTESIAN_POINT('Ctrl Pts',(0.882538907292112,16.9361124220521,-1.79817295107574));
#8755=CARTESIAN_POINT('Ctrl Pts',(0.889702436356832,16.9392195451499,-1.79465710844817));
#8756=CARTESIAN_POINT('Ctrl Pts',(0.89683957879411,16.942319597974,-1.79110109618587));
#8757=CARTESIAN_POINT('Ctrl Pts',(0.903949681684087,16.9454122767401,-1.78750548470432));
#8758=CARTESIAN_POINT('Ctrl Pts',(0.953817581597555,16.9671032983128,-1.76228706012394));
#8759=CARTESIAN_POINT('Ctrl Pts',(1.00290422623283,16.9891579608078,-1.73483868811471));
#8760=CARTESIAN_POINT('Ctrl Pts',(1.05092079732929,17.0114666381281,-1.70524671605184));
#8761=CARTESIAN_POINT('Ctrl Pts',(1.09887250324054,17.0337451788424,-1.67569471953709));
#8762=CARTESIAN_POINT('Ctrl Pts',(1.14575631862329,17.0562767960999,-1.64400506358722));
#8763=CARTESIAN_POINT('Ctrl Pts',(1.19129904941155,17.0789434783766,-1.61031284529931));
#8764=CARTESIAN_POINT('Ctrl Pts',(1.23740106806408,17.1018885190235,-1.57620686945925));
#8765=CARTESIAN_POINT('Ctrl Pts',(1.28212811957984,17.1249716762422,-1.5400490830976));
#8766=CARTESIAN_POINT('Ctrl Pts',(1.32522270851665,17.1480655437137,-1.50202718274225));
#8767=CARTESIAN_POINT('Ctrl Pts',(1.36778613416616,17.1708747672226,-1.46447392214146));
#8768=CARTESIAN_POINT('Ctrl Pts',(1.40875659071413,17.193694135512,-1.42510278849127));
#8769=CARTESIAN_POINT('Ctrl Pts',(1.44792023607454,17.2164005075216,-1.38413434132337));
#8770=CARTESIAN_POINT('Ctrl Pts',(1.4878169858654,17.2395319201974,-1.34239900563293));
#8771=CARTESIAN_POINT('Ctrl Pts',(1.52583806569053,17.2625457468003,-1.29900653938427));
#8772=CARTESIAN_POINT('Ctrl Pts',(1.56180167033742,17.2853161302076,-1.25422343599379));
#8773=CARTESIAN_POINT('Ctrl Pts',(1.59776527498432,17.3080865136148,-1.20944033260332));
#8774=CARTESIAN_POINT('Ctrl Pts',(1.63167113305864,17.3306131725904,-1.16326733826587));
#8775=CARTESIAN_POINT('Ctrl Pts',(1.66338758908179,17.3527790887194,-1.11599400238241));
#8776=CARTESIAN_POINT('Ctrl Pts',(1.66783346591852,17.3558862118169,-1.10936742881929));
#8777=CARTESIAN_POINT('Ctrl Pts',(1.6722364064482,17.3589862646409,-1.10271926064573));
#8778=CARTESIAN_POINT('Ctrl Pts',(1.6765961304334,17.3620789434068,-1.09605031831599));
#8779=CARTESIAN_POINT('Ctrl Pts',(1.70717378629827,17.3837699649771,-1.04927657203438));
#8780=CARTESIAN_POINT('Ctrl Pts',(1.73595988153134,17.4058246274697,-1.00096226226976));
#8781=CARTESIAN_POINT('Ctrl Pts',(1.76274746586953,17.4281333047874,-0.951326577172805));
#8782=CARTESIAN_POINT('Ctrl Pts',(1.78949886307612,17.4504118454929,-0.901757944522451));
#8783=CARTESIAN_POINT('Ctrl Pts',(1.81425661024061,17.4729434627415,-0.850871989761866));
#8784=CARTESIAN_POINT('Ctrl Pts',(1.83685166291036,17.4956101450092,-0.798922307441834));
#8785=CARTESIAN_POINT('Ctrl Pts',(1.8597241943142,17.5185551856589,-0.746334656611749));
#8786=CARTESIAN_POINT('Ctrl Pts',(1.88038006398696,17.5416383428804,-0.692657569314163));
#8787=CARTESIAN_POINT('Ctrl Pts',(1.89869012259822,17.5647322103548,-0.638182343231689));
#8788=CARTESIAN_POINT('Ctrl Pts',(1.9167745001822,17.5875414338613,-0.584378552737978));
#8789=CARTESIAN_POINT('Ctrl Pts',(1.93257038953261,17.6103608021483,-0.529796922553466));
#8790=CARTESIAN_POINT('Ctrl Pts',(1.94600287773644,17.6330671741555,-0.474735383878508));
#8791=CARTESIAN_POINT('Ctrl Pts',(1.95968680874409,17.656198586837,-0.418643148026851));
#8792=CARTESIAN_POINT('Ctrl Pts',(1.97091779663205,17.6792124134455,-0.362053629996861));
#8793=CARTESIAN_POINT('Ctrl Pts',(1.97967164017591,17.7019827968583,-0.305288522463581));
#8794=CARTESIAN_POINT('Ctrl Pts',(1.98842548371977,17.7247531802711,-0.248523414930299));
#8795=CARTESIAN_POINT('Ctrl Pts',(1.9947023209826,17.747279839252,-0.191583499814546));
#8796=CARTESIAN_POINT('Ctrl Pts',(1.99853290967582,17.7694457553863,-0.134785361992776));
#8797=CARTESIAN_POINT('Ctrl Pts',(1.99906986517694,17.7725528784838,-0.126823642528859));
#8798=CARTESIAN_POINT('Ctrl Pts',(1.99955883944021,17.7756529313077,-0.118864689737281));
#8799=CARTESIAN_POINT('Ctrl Pts',(2.,17.7787456100735,-0.110909354270934));
#8800=CARTESIAN_POINT('Ctrl Pts',(2.003094153626,17.8004366316412,-0.0551132738349501));
#8801=CARTESIAN_POINT('Ctrl Pts',(2.00386648849147,17.8224912941312,0.00112119339748048));
#8802=CARTESIAN_POINT('Ctrl Pts',(2.00224737448663,17.8447999714463,0.0575007497882499));
#8803=CARTESIAN_POINT('Ctrl Pts',(2.00063044772936,17.8670785121557,0.113804143507444));
#8804=CARTESIAN_POINT('Ctrl Pts',(1.99662830833342,17.8896101294083,0.170251546618121));
#8805=CARTESIAN_POINT('Ctrl Pts',(1.99022135678385,17.91227681168,0.226538817570541));
#8806=CARTESIAN_POINT('Ctrl Pts',(1.98373572461321,17.9352218523293,0.283517324815695));
#8807=CARTESIAN_POINT('Ctrl Pts',(1.97478568883819,17.9583050095504,0.340330980851915));
#8808=CARTESIAN_POINT('Ctrl Pts',(1.96340505169907,17.9813988770244,0.396662939820889));
#8809=CARTESIAN_POINT('Ctrl Pts',(1.95216468685023,18.0042081005331,0.452300578005842));
#8810=CARTESIAN_POINT('Ctrl Pts',(1.93855351320902,18.0270274688224,0.507467601006192));
#8811=CARTESIAN_POINT('Ctrl Pts',(1.92265561988986,18.0497338408319,0.561868536377263));
#8812=CARTESIAN_POINT('Ctrl Pts',(1.90646013384083,18.0728652535116,0.617287803079352));
#8813=CARTESIAN_POINT('Ctrl Pts',(1.88789169564731,18.0958790801183,0.671911257220936));
#8814=CARTESIAN_POINT('Ctrl Pts',(1.86709019277166,18.1186494635294,0.725448204161157));
#8815=CARTESIAN_POINT('Ctrl Pts',(1.846288689896,18.1414198469404,0.778985151101378));
#8816=CARTESIAN_POINT('Ctrl Pts',(1.82325463286474,18.1639465059197,0.831434982708388));
#8817=CARTESIAN_POINT('Ctrl Pts',(1.79817295107552,18.1861124220523,0.882538907292541));
#8818=CARTESIAN_POINT('Ctrl Pts',(1.79465710844803,18.18921954515,0.889702436357106));
#8819=CARTESIAN_POINT('Ctrl Pts',(1.79110109618581,18.1923195979741,0.896839578794223));
#8820=CARTESIAN_POINT('Ctrl Pts',(1.78750548470433,18.1954122767401,0.903949681684052));
#8821=CARTESIAN_POINT('Ctrl Pts',(1.76228706013497,18.2171032983033,0.953817581575735));
#8822=CARTESIAN_POINT('Ctrl Pts',(1.73483868813874,18.2391579607885,1.00290422618985));
#8823=CARTESIAN_POINT('Ctrl Pts',(1.70524671609067,18.2614666380988,1.05092079726627));
#8824=CARTESIAN_POINT('Ctrl Pts',(1.6756947195693,18.2837451788193,1.09887250319222));
#8825=CARTESIAN_POINT('Ctrl Pts',(1.64400506361153,18.3062767960832,1.14575631858921));
#8826=CARTESIAN_POINT('Ctrl Pts',(1.61031284531455,18.3289434783663,1.19129904939094));
#8827=CARTESIAN_POINT('Ctrl Pts',(1.57620686947382,18.3518885190141,1.23740106804561));
#8828=CARTESIAN_POINT('Ctrl Pts',(1.54004908311129,18.3749716762336,1.28212811956348));
#8829=CARTESIAN_POINT('Ctrl Pts',(1.50202718275492,18.398065543706,1.32522270850227));
#8830=CARTESIAN_POINT('Ctrl Pts',(1.46447392215565,18.4208747672142,1.36778613415087));
#8831=CARTESIAN_POINT('Ctrl Pts',(1.42510278850714,18.4436941355029,1.408756590698));
#8832=CARTESIAN_POINT('Ctrl Pts',(1.3841343413409,18.4664005075118,1.44792023605776));
#8833=CARTESIAN_POINT('Ctrl Pts',(1.34239900564798,18.4895319201894,1.48781698585197));
#8834=CARTESIAN_POINT('Ctrl Pts',(1.29900653939657,18.5125457467939,1.52583806568019));
#8835=CARTESIAN_POINT('Ctrl Pts',(1.25422343600313,18.5353161302028,1.5618016703299));
#8836=CARTESIAN_POINT('Ctrl Pts',(1.20944033260969,18.5580865136117,1.59776527497961));
#8837=CARTESIAN_POINT('Ctrl Pts',(1.16326733826908,18.5806131725888,1.63167113305647));
#8838=CARTESIAN_POINT('Ctrl Pts',(1.11599400238223,18.6027790887194,1.66338758908188));
#8839=CARTESIAN_POINT('Ctrl Pts',(1.10936742881915,18.605886211817,1.66783346591857));
#8840=CARTESIAN_POINT('Ctrl Pts',(1.10271926064563,18.608986264641,1.67223640644824));
#8841=CARTESIAN_POINT('Ctrl Pts',(1.09605031831596,18.6120789434068,1.67659613043339));
#8842=CARTESIAN_POINT('Ctrl Pts',(1.04927657203943,18.6337699649747,1.70717378629498));
#8843=CARTESIAN_POINT('Ctrl Pts',(1.00096226228026,18.6558246274649,1.73595988152509));
#8844=CARTESIAN_POINT('Ctrl Pts',(0.951326577188937,18.6781333047801,1.76274746586083));
#8845=CARTESIAN_POINT('Ctrl Pts',(0.901757944528287,18.7004118454903,1.78949886307358));
#8846=CARTESIAN_POINT('Ctrl Pts',(0.850871989756818,18.7229434627438,1.81425661024339));
#8847=CARTESIAN_POINT('Ctrl Pts',(0.798922307425478,18.7456101450164,1.83685166291751));
#8848=CARTESIAN_POINT('Ctrl Pts',(0.746334656596687,18.7685551856654,1.85972419432023));
#8849=CARTESIAN_POINT('Ctrl Pts',(0.692657569300505,18.7916383428862,1.88038006399197));
#8850=CARTESIAN_POINT('Ctrl Pts',(0.638182343219492,18.81473221036,1.89869012260234));
#8851=CARTESIAN_POINT('Ctrl Pts',(0.584378552729531,18.8375414338648,1.91677450018467));
#8852=CARTESIAN_POINT('Ctrl Pts',(0.529796922548891,18.8603608021501,1.93257038953376));
#8853=CARTESIAN_POINT('Ctrl Pts',(0.474735383877914,18.8830671741558,1.94600287773659));
#8854=CARTESIAN_POINT('Ctrl Pts',(0.418643148026724,18.9061985868371,1.9596868087441));
#8855=CARTESIAN_POINT('Ctrl Pts',(0.362053629997216,18.9292124134453,1.97091779663196));
#8856=CARTESIAN_POINT('Ctrl Pts',(0.30528852246438,18.9519827968579,1.97967164017578));
#8857=CARTESIAN_POINT('Ctrl Pts',(0.248523414931543,18.9747531802706,1.9884254837196));
#8858=CARTESIAN_POINT('Ctrl Pts',(0.191583499816295,18.9972798392513,1.9947023209824));
#8859=CARTESIAN_POINT('Ctrl Pts',(0.134785361994945,19.0194457553854,1.99853290967565));
#8860=CARTESIAN_POINT('Ctrl Pts',(0.126823642530299,19.0225528784832,1.99906986517683));
#8861=CARTESIAN_POINT('Ctrl Pts',(0.118864689737992,19.0256529313074,1.99955883944015));
#8862=CARTESIAN_POINT('Ctrl Pts',(0.110909354270916,19.0287456100735,1.99999999999998));
#8863=CARTESIAN_POINT('Ctrl Pts',(0.0551132738329355,19.050436631642,2.00309415362612));
#8864=CARTESIAN_POINT('Ctrl Pts',(-0.00112119340150097,19.0724912941328,
2.00386648849152));
#8865=CARTESIAN_POINT('Ctrl Pts',(-0.0575007497943028,19.0947999714487,
2.00224737448645));
#8866=CARTESIAN_POINT('Ctrl Pts',(-0.113804143521595,19.1170785121613,2.00063044772879));
#8867=CARTESIAN_POINT('Ctrl Pts',(-0.170251546640372,19.1396101294171,1.99662830833176));
#8868=CARTESIAN_POINT('Ctrl Pts',(-0.226538817600756,19.1622768116922,1.99022135678042));
#8869=CARTESIAN_POINT('Ctrl Pts',(-0.283517324843176,19.1852218523405,1.98373572460921));
#8870=CARTESIAN_POINT('Ctrl Pts',(-0.340330980876671,19.2083050095605,1.97478568883386));
#8871=CARTESIAN_POINT('Ctrl Pts',(-0.396662939842893,19.2313988770334,1.96340505169463));
#8872=CARTESIAN_POINT('Ctrl Pts',(-0.452300578032891,19.2542081005443,1.95216468684413));
#8873=CARTESIAN_POINT('Ctrl Pts',(-0.507467601038136,19.2770274688356,1.93855351320081));
#8874=CARTESIAN_POINT('Ctrl Pts',(-0.561868536413931,19.2997338408472,1.92265561987913));
#8875=CARTESIAN_POINT('Ctrl Pts',(-0.617287803109304,19.3228652535242,1.90646013383092));
#8876=CARTESIAN_POINT('Ctrl Pts',(-0.671911257244324,19.3458790801282,1.88789169563878));
#8877=CARTESIAN_POINT('Ctrl Pts',(-0.725448204178154,19.3686494635366,1.86709019276504));
#8878=CARTESIAN_POINT('Ctrl Pts',(-0.778985151111984,19.3914198469451,1.8462886898913));
#8879=CARTESIAN_POINT('Ctrl Pts',(-0.831434982712839,19.4139465059217,1.82325463286249));
#8880=CARTESIAN_POINT('Ctrl Pts',(-0.882538907291128,19.4361124220518,1.7981729510762));
#8881=CARTESIAN_POINT('Ctrl Pts',(-0.889702436356173,19.4392195451497,1.79465710844847));
#8882=CARTESIAN_POINT('Ctrl Pts',(-0.896839578793776,19.442319597974,1.79110109618601));
#8883=CARTESIAN_POINT('Ctrl Pts',(-0.903949681684074,19.4454122767402,1.7875054847043));
#8884=CARTESIAN_POINT('Ctrl Pts',(-0.95381758160981,19.4671032983182,1.76228706011775));
#8885=CARTESIAN_POINT('Ctrl Pts',(-1.00290422625695,19.4891579608188,1.73483868810121));
#8886=CARTESIAN_POINT('Ctrl Pts',(-1.05092079736472,19.5114666381446,1.70524671603001));
#8887=CARTESIAN_POINT('Ctrl Pts',(-1.09887250323535,19.5337451788404,1.67569471953893));
#8888=CARTESIAN_POINT('Ctrl Pts',(-1.14575631857925,19.5562767960789,1.6440050636163));
#8889=CARTESIAN_POINT('Ctrl Pts',(-1.19129904933102,19.5789434783365,1.6103128453589));
#8890=CARTESIAN_POINT('Ctrl Pts',(-1.23740106799155,19.6018885189865,1.57620686951649));
#8891=CARTESIAN_POINT('Ctrl Pts',(-1.28212811951509,19.6249716762083,1.54004908315182));
#8892=CARTESIAN_POINT('Ctrl Pts',(-1.32522270845931,19.648065543683,1.50202718279284));
#8893=CARTESIAN_POINT('Ctrl Pts',(-1.36778613411482,19.6708747671943,1.46447392218964));
#8894=CARTESIAN_POINT('Ctrl Pts',(-1.40875659066852,19.6936941354862,1.4251027885366));
#8895=CARTESIAN_POINT('Ctrl Pts',(-1.44792023603437,19.7164005074983,1.38413434136538));
#8896=CARTESIAN_POINT('Ctrl Pts',(-1.48781698583262,19.7395319201778,1.34239900566963));
#8897=CARTESIAN_POINT('Ctrl Pts',(-1.52583806566465,19.7625457467843,1.29900653941504));
#8898=CARTESIAN_POINT('Ctrl Pts',(-1.56180167031782,19.7853161301951,1.25422343601817));
#8899=CARTESIAN_POINT('Ctrl Pts',(-1.59776527497099,19.808086513606,1.2094403326213));
#8900=CARTESIAN_POINT('Ctrl Pts',(-1.63167113305097,19.830613172585,1.16326733827702));
#8901=CARTESIAN_POINT('Ctrl Pts',(-1.66338758907914,19.8527790887175,1.11599400238632));
#8902=CARTESIAN_POINT('Ctrl Pts',(-1.66783346591677,19.8558862118157,1.10936742882188));
#8903=CARTESIAN_POINT('Ctrl Pts',(-1.67223640644734,19.8589862646403,1.10271926064701));
#8904=CARTESIAN_POINT('Ctrl Pts',(-1.67659613043341,19.8620789434068,1.09605031831594));
#8905=CARTESIAN_POINT('Ctrl Pts',(-1.7071737862944,19.8837699649743,1.04927657204031));
#8906=CARTESIAN_POINT('Ctrl Pts',(-1.73595988152403,19.905824627464,1.00096226228204));
#8907=CARTESIAN_POINT('Ctrl Pts',(-1.76274746585934,19.9281333047789,0.951326577191711));
#8908=CARTESIAN_POINT('Ctrl Pts',(-1.78949886307829,19.9504118454942,0.901757944519727));
#8909=CARTESIAN_POINT('Ctrl Pts',(-1.81425661025339,19.9729434627528,0.850871989736333));
#8910=CARTESIAN_POINT('Ctrl Pts',(-1.83685166293178,19.9956101450307,0.798922307392625));
#8911=CARTESIAN_POINT('Ctrl Pts',(-1.85972419433239,20.0185551856786,0.746334656566127));
#8912=CARTESIAN_POINT('Ctrl Pts',(-1.88038006400222,20.0416383428983,0.692657569272394));
#8913=CARTESIAN_POINT('Ctrl Pts',(-1.89869012261092,20.0647322103708,0.638182343193955));
#8914=CARTESIAN_POINT('Ctrl Pts',(-1.91677450019524,20.087541433879,0.584378552695657));
#8915=CARTESIAN_POINT('Ctrl Pts',(-1.93257038954561,20.1103608021678,0.529796922506548));
#8916=CARTESIAN_POINT('Ctrl Pts',(-1.94600287774902,20.1330671741768,0.474735383826951));
#8917=CARTESIAN_POINT('Ctrl Pts',(-1.959686808753,20.1561985868545,0.418643147983894));
#8918=CARTESIAN_POINT('Ctrl Pts',(-1.97091779663804,20.1792124134592,0.362053629962793));
#8919=CARTESIAN_POINT('Ctrl Pts',(-1.97967164017977,20.2019827968683,0.305288522438494));
#8920=CARTESIAN_POINT('Ctrl Pts',(-1.98842548372151,20.2247531802774,0.248523414914194));
#8921=CARTESIAN_POINT('Ctrl Pts',(-1.994702320983,20.2472798392547,0.191583499807577));
#8922=CARTESIAN_POINT('Ctrl Pts',(-1.99853290967566,20.2694457553854,0.134785361994836));
#8923=CARTESIAN_POINT('Ctrl Pts',(-1.99906986517684,20.2725528784832,0.126823642530228));
#8924=CARTESIAN_POINT('Ctrl Pts',(-1.99955883944016,20.2756529313074,0.118864689737925));
#8925=CARTESIAN_POINT('Ctrl Pts',(-1.99999999999999,20.2787456100735,0.110909354270875));
#8926=CARTESIAN_POINT('Ctrl Pts',(-2.00309415362675,20.3004366316465,0.0551132738212203));
#8927=CARTESIAN_POINT('Ctrl Pts',(-2.00386648849184,20.322491294142,-0.00112119342512291));
#8928=CARTESIAN_POINT('Ctrl Pts',(-2.00224737448543,20.3447999714627,-0.057500749829767));
#8929=CARTESIAN_POINT('Ctrl Pts',(-2.0006304477273,20.3670785121679,-0.113804143538167));
#8930=CARTESIAN_POINT('Ctrl Pts',(-1.99662830833143,20.3896101294162,-0.170251546637865));
#8931=CARTESIAN_POINT('Ctrl Pts',(-1.99022135678284,20.4122768116835,-0.226538817579384));
#8932=CARTESIAN_POINT('Ctrl Pts',(-1.98373572461206,20.4352218523325,-0.283517324823514));
#8933=CARTESIAN_POINT('Ctrl Pts',(-1.97478568883698,20.4583050095532,-0.340330980858763));
#8934=CARTESIAN_POINT('Ctrl Pts',(-1.9634050516979,20.4813988770268,-0.396662939826711));
#8935=CARTESIAN_POINT('Ctrl Pts',(-1.95216468684893,20.5042081005355,-0.452300578011471));
#8936=CARTESIAN_POINT('Ctrl Pts',(-1.9385535132076,20.5270274688246,-0.50746760101163));
#8937=CARTESIAN_POINT('Ctrl Pts',(-1.92265561988833,20.5497338408341,-0.561868536382517));
#8938=CARTESIAN_POINT('Ctrl Pts',(-1.90646013383956,20.5728652535133,-0.617287803083201));
#8939=CARTESIAN_POINT('Ctrl Pts',(-1.88789169564641,20.5958790801194,-0.671911257223431));
#8940=CARTESIAN_POINT('Ctrl Pts',(-1.86709019277123,20.6186494635299,-0.725448204162321));
#8941=CARTESIAN_POINT('Ctrl Pts',(-1.84628868989605,20.6414198469404,-0.778985151101207));
#8942=CARTESIAN_POINT('Ctrl Pts',(-1.8232546328654,20.6639465059191,-0.831434982706896));
#8943=CARTESIAN_POINT('Ctrl Pts',(-1.79817295107689,20.6861124220512,-0.882538907289802));
#8944=CARTESIAN_POINT('Ctrl Pts',(-1.79465710844896,20.6892195451493,-0.889702436355293));
#8945=CARTESIAN_POINT('Ctrl Pts',(-1.79110109618628,20.6923195979738,-0.896839578793339));
#8946=CARTESIAN_POINT('Ctrl Pts',(-1.78750548470434,20.6954122767402,-0.903949681684084));
#8947=CARTESIAN_POINT('Ctrl Pts',(-1.76228706012711,20.7171032983101,-0.953817581591305));
#8948=CARTESIAN_POINT('Ctrl Pts',(-1.73483868812163,20.7391579608024,-1.00290422622048));
#8949=CARTESIAN_POINT('Ctrl Pts',(-1.70524671606301,20.7614666381198,-1.05092079731117));
#8950=CARTESIAN_POINT('Ctrl Pts',(-1.67569471953583,20.7837451788437,-1.09887250324374));
#8951=CARTESIAN_POINT('Ctrl Pts',(-1.64400506357161,20.8062767961112,-1.14575631864694));
#8952=CARTESIAN_POINT('Ctrl Pts',(-1.61031284526767,20.8289434783979,-1.19129904945433));
#8953=CARTESIAN_POINT('Ctrl Pts',(-1.57620686942888,20.8518885190433,-1.23740106810258));
#8954=CARTESIAN_POINT('Ctrl Pts',(-1.54004908306881,20.8749716762603,-1.28212811961424));
#8955=CARTESIAN_POINT('Ctrl Pts',(-1.5020271827154,20.8980655437301,-1.3252227085471));
#8956=CARTESIAN_POINT('Ctrl Pts',(-1.46447392211193,20.9208747672401,-1.3677861341979));
#8957=CARTESIAN_POINT('Ctrl Pts',(-1.42510278845897,20.9436941355305,-1.40875659074693));
#8958=CARTESIAN_POINT('Ctrl Pts',(-1.38413434128816,20.9664005075411,-1.44792023610822));
#8959=CARTESIAN_POINT('Ctrl Pts',(-1.34239900560239,20.9895319202138,-1.48781698589268));
#8960=CARTESIAN_POINT('Ctrl Pts',(-1.2990065393589,21.0125457468135,-1.52583806571186));
#8961=CARTESIAN_POINT('Ctrl Pts',(-1.25422343597402,21.0353161302176,-1.56180167035333));
#8962=CARTESIAN_POINT('Ctrl Pts',(-1.20944033258914,21.0580865136218,-1.59776527499479));
#8963=CARTESIAN_POINT('Ctrl Pts',(-1.16326733825769,21.0806131725942,-1.63167113306424));
#8964=CARTESIAN_POINT('Ctrl Pts',(-1.11599400238053,21.1027790887202,-1.66338758908307));
#8965=CARTESIAN_POINT('Ctrl Pts',(-1.109367428818,21.1058862118175,-1.66783346591938));
#8966=CARTESIAN_POINT('Ctrl Pts',(-1.10271926064508,21.1089862646412,-1.67223640644865));
#8967=CARTESIAN_POINT('Ctrl Pts',(-1.09605031831596,21.1120789434068,-1.67659613043345));
#8968=CARTESIAN_POINT('Ctrl Pts',(-1.04927635614639,21.1337700650937,-1.70717392743191));
#8969=CARTESIAN_POINT('Ctrl Pts',(-1.00096181624318,21.1558248310677,-1.73596014723423));
#8970=CARTESIAN_POINT('Ctrl Pts',(-0.95132588988029,21.1781336136898,-1.76274783679009));
#8971=CARTESIAN_POINT('Ctrl Pts',(-0.901757245312855,21.2004121566235,-1.78949921547233));
#8972=CARTESIAN_POINT('Ctrl Pts',(-0.850871279746339,21.2229437755687,-1.814256943256));
#8973=CARTESIAN_POINT('Ctrl Pts',(-0.79892158787343,21.2456104589712,-1.83685197588009));
#8974=CARTESIAN_POINT('Ctrl Pts',(-0.746333987087704,21.2685554747151,-1.85972446101981));
#8975=CARTESIAN_POINT('Ctrl Pts',(-0.692656953597621,21.2916386061407,-1.88038028879146));
#8976=CARTESIAN_POINT('Ctrl Pts',(-0.638181784183411,21.314732447354,-1.89869031050386));
#8977=CARTESIAN_POINT('Ctrl Pts',(-0.584377988360444,21.3375416709098,-1.91677467224742));
#8978=CARTESIAN_POINT('Ctrl Pts',(-0.529796353858963,21.3603610388166,-1.93257054541442));
#8979=CARTESIAN_POINT('Ctrl Pts',(-0.474734811919399,21.383067410021,-1.94600301726812));
#8980=CARTESIAN_POINT('Ctrl Pts',(-0.418642668014323,21.406198782596,-1.95968690837756));
#8981=CARTESIAN_POINT('Ctrl Pts',(-0.362053244712395,21.4292125690608,-1.97091786454334));
#8982=CARTESIAN_POINT('Ctrl Pts',(-0.305288233051566,21.4519829129511,-1.97967168480661));
#8983=CARTESIAN_POINT('Ctrl Pts',(-0.248523221390737,21.4747532568414,-1.98842550506989));
#8984=CARTESIAN_POINT('Ctrl Pts',(-0.191583403285161,21.4972798769234,-1.99470232749285));
#8985=CARTESIAN_POINT('Ctrl Pts',(-0.134785361988912,21.5194457553878,-1.99853290967608));
#8986=CARTESIAN_POINT('Ctrl Pts',(-0.126823642526288,21.5225528784848,-1.9990698651771));
#8987=CARTESIAN_POINT('Ctrl Pts',(-0.118864689735969,21.5256529313082,-1.99955883944028));
#8988=CARTESIAN_POINT('Ctrl Pts',(-0.110909354270907,21.5287456100735,-2.));
#8989=CARTESIAN_POINT('Ctrl Pts',(-0.0551132738402241,21.5504366316392,
-2.00309415362571));
#8990=CARTESIAN_POINT('Ctrl Pts',(0.00112119338679578,21.572491294127,-2.00386648849132));
#8991=CARTESIAN_POINT('Ctrl Pts',(0.0575007497721895,21.59479997144,-2.00224737448708));
#8992=CARTESIAN_POINT('Ctrl Pts',(0.113804143497728,21.6170785121518,-2.00063044773009));
#8993=CARTESIAN_POINT('Ctrl Pts',(0.170251546614775,21.6396101294069,-1.99662830833388));
#8994=CARTESIAN_POINT('Ctrl Pts',(0.226538817573559,21.6622768116812,-1.9902213567835));
#8995=CARTESIAN_POINT('Ctrl Pts',(0.283517324818125,21.6852218523303,-1.98373572461284));
#8996=CARTESIAN_POINT('Ctrl Pts',(0.340330980853702,21.7083050095511,-1.97478568883787));
#8997=CARTESIAN_POINT('Ctrl Pts',(0.39666293982207,21.7313988770249,-1.96340505169883));
#8998=CARTESIAN_POINT('Ctrl Pts',(0.452300578005598,21.7542081005331,-1.95216468685026));
#8999=CARTESIAN_POINT('Ctrl Pts',(0.50746760100459,21.7770274688217,-1.9385535132094));
#9000=CARTESIAN_POINT('Ctrl Pts',(0.561868536374285,21.7997338408307,-1.92265561989074));
#9001=CARTESIAN_POINT('Ctrl Pts',(0.617287803076197,21.8228652535103,-1.90646013384186));
#9002=CARTESIAN_POINT('Ctrl Pts',(0.671911257217691,21.845879080117,-1.88789169564849));
#9003=CARTESIAN_POINT('Ctrl Pts',(0.725448204157765,21.868649463528,-1.86709019277301));
#9004=CARTESIAN_POINT('Ctrl Pts',(0.778985151097843,21.891419846939,-1.84628868989752));
#9005=CARTESIAN_POINT('Ctrl Pts',(0.83143498270472,21.9139465059182,-1.82325463286644));
#9006=CARTESIAN_POINT('Ctrl Pts',(0.882538907288783,21.9361124220507,-1.7981729510774));
#9007=CARTESIAN_POINT('Ctrl Pts',(0.889702436354614,21.939219545149,-1.79465710844931));
#9008=CARTESIAN_POINT('Ctrl Pts',(0.896839578792973,21.9423195979737,-1.79110109618647));
#9009=CARTESIAN_POINT('Ctrl Pts',(0.903949681684045,21.9454122767402,-1.78750548470437));
#9010=CARTESIAN_POINT('Ctrl Pts',(0.953817581608164,21.9671032983175,-1.76228706011861));
#9011=CARTESIAN_POINT('Ctrl Pts',(1.00290422625371,21.9891579608173,-1.73483868810305));
#9012=CARTESIAN_POINT('Ctrl Pts',(1.05092079735995,22.0114666381424,-1.70524671603297));
#9013=CARTESIAN_POINT('Ctrl Pts',(1.09887250325821,22.033745178851,-1.67569471952504));
#9014=CARTESIAN_POINT('Ctrl Pts',(1.14575631862848,22.0562767961026,-1.64400506358312));
#9015=CARTESIAN_POINT('Ctrl Pts',(1.19129904940493,22.0789434783733,-1.61031284530423));
#9016=CARTESIAN_POINT('Ctrl Pts',(1.23740106805828,22.1018885190206,-1.57620686946387));
#9017=CARTESIAN_POINT('Ctrl Pts',(1.28212811957486,22.1249716762396,-1.54004908310181));
#9018=CARTESIAN_POINT('Ctrl Pts',(1.32522270851242,22.1480655437115,-1.50202718274601));
#9019=CARTESIAN_POINT('Ctrl Pts',(1.36778613416513,22.1708747672221,-1.4644739221426));
#9020=CARTESIAN_POINT('Ctrl Pts',(1.40875659071607,22.1936941355131,-1.42510278848953));
#9021=CARTESIAN_POINT('Ctrl Pts',(1.44792023607921,22.2164005075243,-1.3841343413185));
#9022=CARTESIAN_POINT('Ctrl Pts',(1.4878169858694,22.2395319201999,-1.34239900562848));
#9023=CARTESIAN_POINT('Ctrl Pts',(1.52583806569387,22.2625457468024,-1.29900653938033));
#9024=CARTESIAN_POINT('Ctrl Pts',(1.56180167034017,22.2853161302094,-1.25422343599037));
#9025=CARTESIAN_POINT('Ctrl Pts',(1.59776527498648,22.3080865136163,-1.20944033260042));
#9026=CARTESIAN_POINT('Ctrl Pts',(1.63167113306028,22.3306131725915,-1.16326733826354));
#9027=CARTESIAN_POINT('Ctrl Pts',(1.66338758908297,22.3527790887203,-1.11599400238064));
#9028=CARTESIAN_POINT('Ctrl Pts',(1.6678334659193,22.3558862118176,-1.10936742881809));
#9029=CARTESIAN_POINT('Ctrl Pts',(1.6722364064486,22.3589862646413,-1.10271926064512));
#9030=CARTESIAN_POINT('Ctrl Pts',(1.67659613043341,22.3620789434069,-1.09605031831596));
#9031=CARTESIAN_POINT('Ctrl Pts',(1.70717378630092,22.383769964979,-1.04927657203033));
#9032=CARTESIAN_POINT('Ctrl Pts',(1.73595988153634,22.4058246274736,-1.00096226226136));
#9033=CARTESIAN_POINT('Ctrl Pts',(1.76274746587652,22.4281333047933,-0.951326577159854));
#9034=CARTESIAN_POINT('Ctrl Pts',(1.78949886308967,22.4504118455046,-0.901757944496487));
#9035=CARTESIAN_POINT('Ctrl Pts',(1.81425661025967,22.4729434627591,-0.850871989722196));
#9036=CARTESIAN_POINT('Ctrl Pts',(1.83685166293377,22.4956101450328,-0.798922307388034));
#9037=CARTESIAN_POINT('Ctrl Pts',(1.85972419433401,22.5185551856805,-0.746334656562013));
#9038=CARTESIAN_POINT('Ctrl Pts',(1.88038006400352,22.5416383428998,-0.692657569268785));
#9039=CARTESIAN_POINT('Ctrl Pts',(1.89869012261195,22.5647322103721,-0.638182343190864));
#9040=CARTESIAN_POINT('Ctrl Pts',(1.91677450019458,22.5875414338784,-0.584378552697299));
#9041=CARTESIAN_POINT('Ctrl Pts',(1.93257038954368,22.6103608021651,-0.52979692251304));
#9042=CARTESIAN_POINT('Ctrl Pts',(1.94600287774621,22.6330671741721,-0.474735383838417));
#9043=CARTESIAN_POINT('Ctrl Pts',(1.95968680875091,22.6561985868505,-0.418643147993864));
#9044=CARTESIAN_POINT('Ctrl Pts',(1.97091779663654,22.6792124134558,-0.362053629971188));
#9045=CARTESIAN_POINT('Ctrl Pts',(1.97967164017873,22.7019827968656,-0.305288522445268));
#9046=CARTESIAN_POINT('Ctrl Pts',(1.98842548372092,22.7247531802754,-0.248523414919351));
#9047=CARTESIAN_POINT('Ctrl Pts',(1.99470232098272,22.7472798392533,-0.191583499811085));
#9048=CARTESIAN_POINT('Ctrl Pts',(1.99853290967555,22.7694457553847,-0.134785361996723));
#9049=CARTESIAN_POINT('Ctrl Pts',(1.99906986517678,22.7725528784828,-0.126823642531481));
#9050=CARTESIAN_POINT('Ctrl Pts',(1.99955883944014,22.7756529313072,-0.118864689738578));
#9051=CARTESIAN_POINT('Ctrl Pts',(2.,22.7787456100735,-0.110909354270901));
#9052=CARTESIAN_POINT('Ctrl Pts',(2.00309415362582,22.8004366316399,-0.0551132738382789));
#9053=CARTESIAN_POINT('Ctrl Pts',(2.00386648849139,22.8224912941286,0.00112119339068031));
#9054=CARTESIAN_POINT('Ctrl Pts',(2.00224737448693,22.8447999714423,0.0575007497779818));
#9055=CARTESIAN_POINT('Ctrl Pts',(2.00063044773006,22.8670785121501,0.11380414349335));
#9056=CARTESIAN_POINT('Ctrl Pts',(1.99662830833485,22.8896101294011,0.17025154660023));
#9057=CARTESIAN_POINT('Ctrl Pts',(1.99022135678632,22.9122768116713,0.226538817548881));
#9058=CARTESIAN_POINT('Ctrl Pts',(1.98373572461611,22.9352218523213,0.283517324795811));
#9059=CARTESIAN_POINT('Ctrl Pts',(1.97478568884138,22.958305009543,0.340330980833825));
#9060=CARTESIAN_POINT('Ctrl Pts',(1.96340505170238,22.9813988770177,0.396662939804617));
#9061=CARTESIAN_POINT('Ctrl Pts',(1.95216468685371,23.0042081005271,0.452300577991144));
#9062=CARTESIAN_POINT('Ctrl Pts',(1.93855351321251,23.027027468817,0.507467600993079));
#9063=CARTESIAN_POINT('Ctrl Pts',(1.92265561989324,23.0497338408271,0.561868536365727));
#9064=CARTESIAN_POINT('Ctrl Pts',(1.90646013384401,23.0728652535076,0.617287803069753));
#9065=CARTESIAN_POINT('Ctrl Pts',(1.88789169565015,23.0958790801151,0.671911257213199));
#9066=CARTESIAN_POINT('Ctrl Pts',(1.86709019277399,23.1186494635269,0.725448204155213));
#9067=CARTESIAN_POINT('Ctrl Pts',(1.84628868989783,23.1414198469387,0.778985151097228));
#9068=CARTESIAN_POINT('Ctrl Pts',(1.82325463286591,23.1639465059187,0.831434982705977));
#9069=CARTESIAN_POINT('Ctrl Pts',(1.79817295107589,23.1861124220521,0.88253890729181));
#9070=CARTESIAN_POINT('Ctrl Pts',(1.79465710844828,23.1892195451499,0.88970243635662));
#9071=CARTESIAN_POINT('Ctrl Pts',(1.79110109618594,23.1923195979741,0.896839578793966));
#9072=CARTESIAN_POINT('Ctrl Pts',(1.78750548470435,23.1954122767402,0.903949681684032));
#9073=CARTESIAN_POINT('Ctrl Pts',(1.76228706012777,23.2171032983096,0.953817581590012));
#9074=CARTESIAN_POINT('Ctrl Pts',(1.73483868812302,23.2391579608013,1.00290422621798));
#9075=CARTESIAN_POINT('Ctrl Pts',(1.70524671606526,23.2614666381181,1.05092079730752));
#9076=CARTESIAN_POINT('Ctrl Pts',(1.6756947195636,23.2837451788229,1.09887250319891));
#9077=CARTESIAN_POINT('Ctrl Pts',(1.64400506362857,23.3062767960707,1.14575631856278));
#9078=CARTESIAN_POINT('Ctrl Pts',(1.61031284535712,23.3289434783377,1.19129904933341));
#9079=CARTESIAN_POINT('Ctrl Pts',(1.57620686951458,23.3518885189878,1.23740106799398));
#9080=CARTESIAN_POINT('Ctrl Pts',(1.54004908314973,23.3749716762096,1.28212811951758));
#9081=CARTESIAN_POINT('Ctrl Pts',(1.5020271827906,23.3980655436844,1.32522270846184));
#9082=CARTESIAN_POINT('Ctrl Pts',(1.46447392219389,23.4208747671917,1.36778613410986));
#9083=CARTESIAN_POINT('Ctrl Pts',(1.42510278854796,23.4436941354796,1.40875659065662));
#9084=CARTESIAN_POINT('Ctrl Pts',(1.38413434138436,23.4664005074878,1.44792023601622));
#9085=CARTESIAN_POINT('Ctrl Pts',(1.34239900568539,23.4895319201694,1.48781698581861));
#9086=CARTESIAN_POINT('Ctrl Pts',(1.29900653942732,23.5125457467779,1.52583806565439));
#9087=CARTESIAN_POINT('Ctrl Pts',(1.25422343602664,23.5353161301909,1.56180167031102));
#9088=CARTESIAN_POINT('Ctrl Pts',(1.20944033262596,23.5580865136038,1.59776527496766));
#9089=CARTESIAN_POINT('Ctrl Pts',(1.1632673382776,23.5806131725848,1.63167113305074));
#9090=CARTESIAN_POINT('Ctrl Pts',(1.11599400238262,23.6027790887192,1.66338758908162));
#9091=CARTESIAN_POINT('Ctrl Pts',(1.10936742881941,23.6058862118168,1.6678334659184));
#9092=CARTESIAN_POINT('Ctrl Pts',(1.10271926064578,23.6089862646409,1.67223640644814));
#9093=CARTESIAN_POINT('Ctrl Pts',(1.09605031831596,23.6120789434068,1.67659613043339));
#9094=CARTESIAN_POINT('Ctrl Pts',(1.0492765720368,23.6337699649759,1.70717378629669));
#9095=CARTESIAN_POINT('Ctrl Pts',(1.00096226227484,23.6558246274673,1.73595988152832));
#9096=CARTESIAN_POINT('Ctrl Pts',(0.951326577180585,23.6781333047839,1.76274746586534));
#9097=CARTESIAN_POINT('Ctrl Pts',(0.901757944510291,23.7004118454984,1.78949886308298));
#9098=CARTESIAN_POINT('Ctrl Pts',(0.850871989728759,23.7229434627562,1.81425661025687));
#9099=CARTESIAN_POINT('Ctrl Pts',(0.798922307386955,23.7456101450332,1.83685166293425));
#9100=CARTESIAN_POINT('Ctrl Pts',(0.746334656561049,23.7685551856808,1.8597241943344));
#9101=CARTESIAN_POINT('Ctrl Pts',(0.692657569267959,23.7916383429002,1.88038006400383));
#9102=CARTESIAN_POINT('Ctrl Pts',(0.638182343190171,23.8147322103724,1.89869012261219));
#9103=CARTESIAN_POINT('Ctrl Pts',(0.584378552694931,23.8375414338794,1.91677450019536));
#9104=CARTESIAN_POINT('Ctrl Pts',(0.529796922509002,23.8603608021668,1.93257038954484));
#9105=CARTESIAN_POINT('Ctrl Pts',(0.474735383832642,23.8830671741745,1.94600287774763));
#9106=CARTESIAN_POINT('Ctrl Pts',(0.418643147989125,23.9061985868524,1.95968680875189));
#9107=CARTESIAN_POINT('Ctrl Pts',(0.362053629967556,23.9292124134573,1.97091779663716));
#9108=CARTESIAN_POINT('Ctrl Pts',(0.305288522442711,23.9519827968666,1.97967164017911));
#9109=CARTESIAN_POINT('Ctrl Pts',(0.248523414917863,23.974753180276,1.98842548372106));
#9110=CARTESIAN_POINT('Ctrl Pts',(0.191583499810712,23.9972798392535,1.9947023209827));
#9111=CARTESIAN_POINT('Ctrl Pts',(0.13478536199745,24.0194457553844,1.99853290967547));
#9112=CARTESIAN_POINT('Ctrl Pts',(0.126823642531985,24.0225528784826,1.99906986517672));
#9113=CARTESIAN_POINT('Ctrl Pts',(0.118864689738828,24.0256529313071,1.9995588394401));
#9114=CARTESIAN_POINT('Ctrl Pts',(0.110909354270918,24.0287456100735,1.99999999999998));
#9115=CARTESIAN_POINT('Ctrl Pts',(0.0551130162975314,24.0504367317603,2.00309416790767));
#9116=CARTESIAN_POINT('Ctrl Pts',(-0.00112171253166826,24.0724914977342,
2.00386649558389));
#9117=CARTESIAN_POINT('Ctrl Pts',(-0.0575015304798811,24.0948002803561,
2.00224735206656));
#9118=CARTESIAN_POINT('Ctrl Pts',(-0.113805823015011,24.1170791785251,2.00063037752543));
#9119=CARTESIAN_POINT('Ctrl Pts',(-0.170254128158742,24.1396111607935,1.99662811395759));
#9120=CARTESIAN_POINT('Ctrl Pts',(-0.2265422897397,24.1622782099103,1.99022096155788));
#9121=CARTESIAN_POINT('Ctrl Pts',(-0.283520500950918,24.1852231396404,1.98373526239061));
#9122=CARTESIAN_POINT('Ctrl Pts',(-0.340333856155103,24.2083061819791,1.97478518482606));
#9123=CARTESIAN_POINT('Ctrl Pts',(-0.396665514397027,24.2313999324986,1.96340453156067));
#9124=CARTESIAN_POINT('Ctrl Pts',(-0.452303137861108,24.2542091562259,1.95216409375152));
#9125=CARTESIAN_POINT('Ctrl Pts',(-0.507470141472793,24.2770285228212,1.93855284808134));
#9126=CARTESIAN_POINT('Ctrl Pts',(-0.561871053025202,24.2997348912542,1.92265488443379));
#9127=CARTESIAN_POINT('Ctrl Pts',(-0.61728987625894,24.3228661253192,1.90645944924681));
#9128=CARTESIAN_POINT('Ctrl Pts',(-0.671912894410742,24.3458797731456,1.88789109964264));
#9129=CARTESIAN_POINT('Ctrl Pts',(-0.725449419744559,24.3686499805425,1.86708972046256));
#9130=CARTESIAN_POINT('Ctrl Pts',(-0.778985945078376,24.3914201879394,1.84628834128247));
#9131=CARTESIAN_POINT('Ctrl Pts',(-0.831435369486437,24.4139466736816,1.82325444303487));
#9132=CARTESIAN_POINT('Ctrl Pts',(-0.882538907289412,24.436112422051,1.79817295107701));
#9133=CARTESIAN_POINT('Ctrl Pts',(-0.889702436355033,24.4392195451492,1.79465710844901));
#9134=CARTESIAN_POINT('Ctrl Pts',(-0.896839578793186,24.4423195979737,1.79110109618628));
#9135=CARTESIAN_POINT('Ctrl Pts',(-0.903949681684042,24.4454122767402,1.78750548470429));
#9136=CARTESIAN_POINT('Ctrl Pts',(-0.953817581595852,24.4671032983121,1.76228706012477));
#9137=CARTESIAN_POINT('Ctrl Pts',(-1.00290422622947,24.4891579608064,1.73483868811654));
#9138=CARTESIAN_POINT('Ctrl Pts',(-1.05092079732441,24.5114666381259,1.7052467160548));
#9139=CARTESIAN_POINT('Ctrl Pts',(-1.09887250319947,24.5337451788233,1.67569471956254));
#9140=CARTESIAN_POINT('Ctrl Pts',(-1.14575631854775,24.5562767960636,1.64400506363834));
#9141=CARTESIAN_POINT('Ctrl Pts',(-1.19129904930367,24.578943478323,1.61031284537906));
#9142=CARTESIAN_POINT('Ctrl Pts',(-1.23740106796711,24.6018885189741,1.57620686953571));
#9143=CARTESIAN_POINT('Ctrl Pts',(-1.28212811949352,24.6249716761971,1.54004908316981));
#9144=CARTESIAN_POINT('Ctrl Pts',(-1.32522270844045,24.648065543673,1.50202718280942));
#9145=CARTESIAN_POINT('Ctrl Pts',(-1.36778613409947,24.6708747671859,1.46447392220408));
#9146=CARTESIAN_POINT('Ctrl Pts',(-1.4087565906565,24.6936941354794,1.42510278854858));
#9147=CARTESIAN_POINT('Ctrl Pts',(-1.44792023602544,24.7164005074931,1.38413434137467));
#9148=CARTESIAN_POINT('Ctrl Pts',(-1.48781698582565,24.7395319201737,1.34239900567742));
#9149=CARTESIAN_POINT('Ctrl Pts',(-1.52583806565949,24.7625457467811,1.29900653942118));
#9150=CARTESIAN_POINT('Ctrl Pts',(-1.56180167031431,24.7853161301929,1.25422343602251));
#9151=CARTESIAN_POINT('Ctrl Pts',(-1.59776527496913,24.8080865136048,1.20944033262385));
#9152=CARTESIAN_POINT('Ctrl Pts',(-1.63167113305059,24.8306131725848,1.16326733827763));
#9153=CARTESIAN_POINT('Ctrl Pts',(-1.66338758908004,24.8527790887181,1.11599400238492));
#9154=CARTESIAN_POINT('Ctrl Pts',(-1.66783346591736,24.8558862118161,1.10936742882094));
#9155=CARTESIAN_POINT('Ctrl Pts',(-1.67223640644764,24.8589862646405,1.10271926064652));
#9156=CARTESIAN_POINT('Ctrl Pts',(-1.6765961304334,24.8620789434068,1.09605031831592));
#9157=CARTESIAN_POINT('Ctrl Pts',(-1.7071737863027,24.8837699649802,1.04927657202758));
#9158=CARTESIAN_POINT('Ctrl Pts',(-1.73595988153965,24.905824627476,1.00096226225577));
#9159=CARTESIAN_POINT('Ctrl Pts',(-1.76274746588115,24.9281333047971,0.951326577151247));
#9160=CARTESIAN_POINT('Ctrl Pts',(-1.78949886308653,24.9504118455021,0.901757944501721));
#9161=CARTESIAN_POINT('Ctrl Pts',(-1.81425661024985,24.9729434627502,0.850871989742079));
#9162=CARTESIAN_POINT('Ctrl Pts',(-1.83685166291854,24.9956101450174,0.798922307423065));
#9163=CARTESIAN_POINT('Ctrl Pts',(-1.85972419432098,25.0185551856663,0.746334656594723));
#9164=CARTESIAN_POINT('Ctrl Pts',(-1.88038006399248,25.0416383428869,0.692657569299052));
#9165=CARTESIAN_POINT('Ctrl Pts',(-1.89869012260265,25.0647322103604,0.638182343218542));
#9166=CARTESIAN_POINT('Ctrl Pts',(-1.91677450018681,25.0875414338675,0.584378552723056));
#9167=CARTESIAN_POINT('Ctrl Pts',(-1.93257038953726,25.1103608021552,0.529796922536758));
#9168=CARTESIAN_POINT('Ctrl Pts',(-1.94600287774096,25.1330671741632,0.474735383859972));
#9169=CARTESIAN_POINT('Ctrl Pts',(-1.95968680874709,25.156198586843,0.418643148012222));
#9170=CARTESIAN_POINT('Ctrl Pts',(-1.97091779663386,25.1792124134497,0.362053629986285));
#9171=CARTESIAN_POINT('Ctrl Pts',(-1.97967164017691,25.2019827968609,0.305288522457018));
#9172=CARTESIAN_POINT('Ctrl Pts',(-1.98842548371996,25.224753180272,0.248523414927751));
#9173=CARTESIAN_POINT('Ctrl Pts',(-1.99470232098232,25.2472798392513,0.191583499816204));
#9174=CARTESIAN_POINT('Ctrl Pts',(-1.99853290967542,25.269445755384,0.134785361998493));
#9175=CARTESIAN_POINT('Ctrl Pts',(-1.9990698651767,25.2725528784823,0.126823642532641));
#9176=CARTESIAN_POINT('Ctrl Pts',(-1.9995588394401,25.2756529313069,0.118864689739151));
#9177=CARTESIAN_POINT('Ctrl Pts',(-2.,25.2787456100735,0.110909354270877));
#9178=CARTESIAN_POINT('Ctrl Pts',(-2.00309415362697,25.300436631648,0.0551132738174295));
#9179=CARTESIAN_POINT('Ctrl Pts',(-2.00386648849195,25.322491294145,-0.00112119343270661));
#9180=CARTESIAN_POINT('Ctrl Pts',(-2.00224737448511,25.3447999714672,-0.0575007498411724));
#9181=CARTESIAN_POINT('Ctrl Pts',(-2.00063044772582,25.367078512184,-0.113804143578793));
#9182=CARTESIAN_POINT('Ctrl Pts',(-1.9966283083263,25.3896101294441,-0.170251546707902));
#9183=CARTESIAN_POINT('Ctrl Pts',(-1.99022135677158,25.4122768117234,-0.22653881767843));
#9184=CARTESIAN_POINT('Ctrl Pts',(-1.98373572459887,25.4352218523693,-0.283517324914314));
#9185=CARTESIAN_POINT('Ctrl Pts',(-1.97478568882256,25.4583050095867,-0.34033098094112));
#9186=CARTESIAN_POINT('Ctrl Pts',(-1.96340505168295,25.4813988770571,-0.396662939900708));
#9187=CARTESIAN_POINT('Ctrl Pts',(-1.95216468683355,25.5042081005624,-0.452300578076878));
#9188=CARTESIAN_POINT('Ctrl Pts',(-1.93855351319249,25.5270274688482,-0.50746760106841));
#9189=CARTESIAN_POINT('Ctrl Pts',(-1.92265561987421,25.5497338408542,-0.561868536430838));
#9190=CARTESIAN_POINT('Ctrl Pts',(-1.9064601338263,25.5728652535301,-0.617287803123396));
#9191=CARTESIAN_POINT('Ctrl Pts',(-1.8878916956347,25.5958790801329,-0.671911257255631));
#9192=CARTESIAN_POINT('Ctrl Pts',(-1.86709019276172,25.6186494635402,-0.725448204186784));
#9193=CARTESIAN_POINT('Ctrl Pts',(-1.84628868988873,25.6414198469475,-0.77898515111794));
#9194=CARTESIAN_POINT('Ctrl Pts',(-1.82325463286093,25.663946505923,-0.831434982716144));
#9195=CARTESIAN_POINT('Ctrl Pts',(-1.79817295107583,25.686112422052,-0.882538907291945));
#9196=CARTESIAN_POINT('Ctrl Pts',(-1.79465710844823,25.6892195451498,-0.889702436356714));
#9197=CARTESIAN_POINT('Ctrl Pts',(-1.79110109618591,25.692319597974,-0.896839578794057));
#9198=CARTESIAN_POINT('Ctrl Pts',(-1.78750548470433,25.6954122767401,-0.903949681684092));
#9199=CARTESIAN_POINT('Ctrl Pts',(-1.7622870601227,25.7171032983138,-0.953817581600028));
#9200=CARTESIAN_POINT('Ctrl Pts',(-1.73483868811199,25.7391579608101,-1.00290422623769));
#9201=CARTESIAN_POINT('Ctrl Pts',(-1.70524671604744,25.7614666381315,-1.05092079733642));
#9202=CARTESIAN_POINT('Ctrl Pts',(-1.67569471954384,25.7837451788372,-1.09887250322914));
#9203=CARTESIAN_POINT('Ctrl Pts',(-1.64400506360674,25.806276796086,-1.14575631859421));
#9204=CARTESIAN_POINT('Ctrl Pts',(-1.61031284533311,25.8289434783539,-1.19129904936587));
#9205=CARTESIAN_POINT('Ctrl Pts',(-1.57620686949147,25.8518885190027,-1.23740106802327));
#9206=CARTESIAN_POINT('Ctrl Pts',(-1.54004908312781,25.8749716762233,-1.28212811954378));
#9207=CARTESIAN_POINT('Ctrl Pts',(-1.5020271827701,25.8980655436969,-1.3252227084851));
#9208=CARTESIAN_POINT('Ctrl Pts',(-1.46447392217107,25.9208747672052,-1.36778613413441));
#9209=CARTESIAN_POINT('Ctrl Pts',(-1.42510278852273,25.943694135494,-1.40875659068227));
#9210=CARTESIAN_POINT('Ctrl Pts',(-1.38413434135664,25.9664005075031,-1.44792023604275));
#9211=CARTESIAN_POINT('Ctrl Pts',(-1.34239900566126,25.9895319201823,-1.48781698584017));
#9212=CARTESIAN_POINT('Ctrl Pts',(-1.29900653940712,26.0125457467884,-1.52583806567139));
#9213=CARTESIAN_POINT('Ctrl Pts',(-1.25422343601075,26.035316130199,-1.56180167032382));
#9214=CARTESIAN_POINT('Ctrl Pts',(-1.20944033261438,26.0580865136095,-1.59776527497625));
#9215=CARTESIAN_POINT('Ctrl Pts',(-1.16326733827057,26.0806131725882,-1.63167113305559));
#9216=CARTESIAN_POINT('Ctrl Pts',(-1.11599400238044,26.1027790887203,-1.66338758908314));
#9217=CARTESIAN_POINT('Ctrl Pts',(-1.10936742881793,26.1058862118175,-1.66783346591944));
#9218=CARTESIAN_POINT('Ctrl Pts',(-1.10271926064503,26.1089862646412,-1.67223640644869));
#9219=CARTESIAN_POINT('Ctrl Pts',(-1.09605031831595,26.1120789434068,-1.67659613043346));
#9220=CARTESIAN_POINT('Ctrl Pts',(-1.04927657203578,26.1337699649764,-1.7071737862974));
#9221=CARTESIAN_POINT('Ctrl Pts',(-1.00096226227268,26.1558246274683,-1.73595988152965));
#9222=CARTESIAN_POINT('Ctrl Pts',(-0.951326577177282,26.1781333047854,-1.76274746586717));
#9223=CARTESIAN_POINT('Ctrl Pts',(-0.901757944517214,26.2004118454953,-1.78949886307917));
#9224=CARTESIAN_POINT('Ctrl Pts',(-0.850871989746337,26.2229434627484,-1.8142566102483));
#9225=CARTESIAN_POINT('Ctrl Pts',(-0.798922307415678,26.2456101450206,-1.8368516629218));
#9226=CARTESIAN_POINT('Ctrl Pts',(-0.74633465658777,26.2685551856693,-1.8597241943238));
#9227=CARTESIAN_POINT('Ctrl Pts',(-0.692657569292552,26.2916383428896,-1.8803800639949));
#9228=CARTESIAN_POINT('Ctrl Pts',(-0.638182343212506,26.3147322103629,-1.89869012260473));
#9229=CARTESIAN_POINT('Ctrl Pts',(-0.584378552725403,26.3375414338665,-1.91677450018587));
#9230=CARTESIAN_POINT('Ctrl Pts',(-0.529796922547766,26.3603608021506,-1.93257038953402));
#9231=CARTESIAN_POINT('Ctrl Pts',(-0.474735383879798,26.383067174155,-1.94600287773618));
#9232=CARTESIAN_POINT('Ctrl Pts',(-0.418643148028719,26.4061985868363,-1.95968680874373));
#9233=CARTESIAN_POINT('Ctrl Pts',(-0.362053629999354,26.4292124134444,-1.97091779663162));
#9234=CARTESIAN_POINT('Ctrl Pts',(-0.305288522466675,26.451982796857,-1.97967164017548));
#9235=CARTESIAN_POINT('Ctrl Pts',(-0.248523414933991,26.4747531802696,-1.98842548371934));
#9236=CARTESIAN_POINT('Ctrl Pts',(-0.191583499818795,26.4972798392503,-1.99470232098221));
#9237=CARTESIAN_POINT('Ctrl Pts',(-0.13478536199757,26.5194457553844,-1.99853290967552));
#9238=CARTESIAN_POINT('Ctrl Pts',(-0.126823642532062,26.5225528784825,-1.99906986517677));
#9239=CARTESIAN_POINT('Ctrl Pts',(-0.118864689738849,26.5256529313071,-1.99955883944015));
#9240=CARTESIAN_POINT('Ctrl Pts',(-0.110909354270907,26.5287456100735,-2.00000000000003));
#9241=CARTESIAN_POINT('Ctrl Pts',(-0.0551132738153703,26.5504366316488,
-2.00309415362711));
#9242=CARTESIAN_POINT('Ctrl Pts',(0.00112119343692078,26.5724912941467,
-2.00386648849203));
#9243=CARTESIAN_POINT('Ctrl Pts',(0.0575007498475077,26.5947999714698,-2.00224737448494));
#9244=CARTESIAN_POINT('Ctrl Pts',(0.113804143574996,26.6170785121825,-2.00063044772577));
#9245=CARTESIAN_POINT('Ctrl Pts',(0.170251546693887,26.6396101294386,-1.99662830832721));
#9246=CARTESIAN_POINT('Ctrl Pts',(0.22653881765432,26.6622768117137,-1.99022135677433));
#9247=CARTESIAN_POINT('Ctrl Pts',(0.283517324892532,26.6852218523605,-1.98373572460205));
#9248=CARTESIAN_POINT('Ctrl Pts',(0.3403309809217,26.7083050095789,-1.97478568882598));
#9249=CARTESIAN_POINT('Ctrl Pts',(0.396662939883625,26.7313988770501,-1.96340505168641));
#9250=CARTESIAN_POINT('Ctrl Pts',(0.452300578058839,26.754208100555,-1.9521646868377));
#9251=CARTESIAN_POINT('Ctrl Pts',(0.507467601049452,26.7770274688404,-1.93855351319744));
#9252=CARTESIAN_POINT('Ctrl Pts',(0.561868536411038,26.799733840846,-1.92265561988001));
#9253=CARTESIAN_POINT('Ctrl Pts',(0.617287803107586,26.8228652535235,-1.90646013383155));
#9254=CARTESIAN_POINT('Ctrl Pts',(0.671911257243766,26.845879080128,-1.88789169563905));
#9255=CARTESIAN_POINT('Ctrl Pts',(0.725448204178672,26.8686494635369,-1.86709019276489));
#9256=CARTESIAN_POINT('Ctrl Pts',(0.778985151113583,26.8914198469457,-1.84628868989072));
#9257=CARTESIAN_POINT('Ctrl Pts',(0.831434982715474,26.9139465059228,-1.82325463286138));
#9258=CARTESIAN_POINT('Ctrl Pts',(0.882538907294795,26.9361124220533,-1.79817295107445));
#9259=CARTESIAN_POINT('Ctrl Pts',(0.889702436358604,26.9392195451507,-1.79465710844732));
#9260=CARTESIAN_POINT('Ctrl Pts',(0.896839578794966,26.9423195979745,-1.79110109618546));
#9261=CARTESIAN_POINT('Ctrl Pts',(0.903949681684054,26.9454122767402,-1.78750548470436));
#9262=CARTESIAN_POINT('Ctrl Pts',(0.953817581590833,26.9671032983099,-1.76228706012734));
#9263=CARTESIAN_POINT('Ctrl Pts',(1.0029042262196,26.989157960802,-1.73483868812211));
#9264=CARTESIAN_POINT('Ctrl Pts',(1.05092079730992,27.0114666381192,-1.70524671606377));
#9265=CARTESIAN_POINT('Ctrl Pts',(1.09887250322323,27.0337451788342,-1.67569471954849));
#9266=CARTESIAN_POINT('Ctrl Pts',(1.14575631860802,27.0562767960925,-1.64400506359792));
#9267=CARTESIAN_POINT('Ctrl Pts',(1.19129904939823,27.07894347837,-1.61031284530915));
#9268=CARTESIAN_POINT('Ctrl Pts',(1.23740106805221,27.1018885190175,-1.5762068694686));
#9269=CARTESIAN_POINT('Ctrl Pts',(1.28212811956941,27.1249716762368,-1.54004908310631));
#9270=CARTESIAN_POINT('Ctrl Pts',(1.32522270850755,27.1480655437089,-1.50202718275025));
#9271=CARTESIAN_POINT('Ctrl Pts',(1.36778613415706,27.1708747672177,-1.46447392214992));
#9272=CARTESIAN_POINT('Ctrl Pts',(1.40875659070502,27.1936941355069,-1.42510278850023));
#9273=CARTESIAN_POINT('Ctrl Pts',(1.44792023606551,27.2164005075163,-1.38413434133279));
#9274=CARTESIAN_POINT('Ctrl Pts',(1.48781698585827,27.2395319201932,-1.34239900564092));
#9275=CARTESIAN_POINT('Ctrl Pts',(1.52583806568516,27.262545746797,-1.29900653939066));
#9276=CARTESIAN_POINT('Ctrl Pts',(1.56180167033367,27.2853161302052,-1.25422343599845));
#9277=CARTESIAN_POINT('Ctrl Pts',(1.59776527498217,27.3080865136134,-1.20944033260624));
#9278=CARTESIAN_POINT('Ctrl Pts',(1.63167113305793,27.3306131725898,-1.16326733826698));
#9279=CARTESIAN_POINT('Ctrl Pts',(1.66338758908235,27.3527790887197,-1.11599400238156));
#9280=CARTESIAN_POINT('Ctrl Pts',(1.6678334659189,27.3558862118172,-1.1093674288187));
#9281=CARTESIAN_POINT('Ctrl Pts',(1.6722364064484,27.3589862646411,-1.10271926064542));
#9282=CARTESIAN_POINT('Ctrl Pts',(1.67659613043341,27.3620789434068,-1.09605031831596));
#9283=CARTESIAN_POINT('Ctrl Pts',(1.70717378629165,27.3837699649724,-1.04927657204452));
#9284=CARTESIAN_POINT('Ctrl Pts',(1.73595988151885,27.4058246274601,-1.00096226229075));
#9285=CARTESIAN_POINT('Ctrl Pts',(1.76274746585211,27.4281333047729,-0.951326577205113));
#9286=CARTESIAN_POINT('Ctrl Pts',(1.78949886307212,27.4504118454887,-0.901757944532073));
#9287=CARTESIAN_POINT('Ctrl Pts',(1.81425661024819,27.472943462748,-0.850871989747507));
#9288=CARTESIAN_POINT('Ctrl Pts',(1.83685166292746,27.4956101450264,-0.798922307402572));
#9289=CARTESIAN_POINT('Ctrl Pts',(1.85972419432879,27.5185551856747,-0.746334656575189));
#9290=CARTESIAN_POINT('Ctrl Pts',(1.88038006399926,27.5416383428948,-0.692657569280544));
#9291=CARTESIAN_POINT('Ctrl Pts',(1.8986901226085,27.5647322103678,-0.638182343201152));
#9292=CARTESIAN_POINT('Ctrl Pts',(1.91677450019326,27.5875414338763,-0.58437855270225));
#9293=CARTESIAN_POINT('Ctrl Pts',(1.93257038954402,27.6103608021654,-0.529796922512431));
#9294=CARTESIAN_POINT('Ctrl Pts',(1.94600287774773,27.6330671741746,-0.474735383832203));
#9295=CARTESIAN_POINT('Ctrl Pts',(1.95968680875216,27.6561985868529,-0.418643147987978));
#9296=CARTESIAN_POINT('Ctrl Pts',(1.97091779663755,27.6792124134581,-0.362053629965651));
#9297=CARTESIAN_POINT('Ctrl Pts',(1.97967164017953,27.7019827968677,-0.305288522440102));
#9298=CARTESIAN_POINT('Ctrl Pts',(1.98842548372151,27.7247531802773,-0.248523414914553));
#9299=CARTESIAN_POINT('Ctrl Pts',(1.99470232098313,27.7472798392551,-0.191583499806667));
#9300=CARTESIAN_POINT('Ctrl Pts',(1.99853290967581,27.7694457553863,-0.13478536199265));
#9301=CARTESIAN_POINT('Ctrl Pts',(1.99906986517693,27.7725528784838,-0.126823642528799));
#9302=CARTESIAN_POINT('Ctrl Pts',(1.9995588394402,27.7756529313077,-0.118864689737254));
#9303=CARTESIAN_POINT('Ctrl Pts',(1.99999999999999,27.7787456100735,-0.110909354270966));
#9304=CARTESIAN_POINT('Ctrl Pts',(2.00309415362701,27.8004366316483,-0.0551132738167583));
#9305=CARTESIAN_POINT('Ctrl Pts',(2.00386648849197,27.8224912941456,0.00112119343414613));
#9306=CARTESIAN_POINT('Ctrl Pts',(2.00224737448504,27.8447999714681,0.0575007498433761));
#9307=CARTESIAN_POINT('Ctrl Pts',(2.00063044772619,27.8670785121781,0.113804143563829));
#9308=CARTESIAN_POINT('Ctrl Pts',(1.99662830832856,27.8896101294313,0.170251546675671));
#9309=CARTESIAN_POINT('Ctrl Pts',(1.99022135677719,27.9122768117036,0.226538817629131));
#9310=CARTESIAN_POINT('Ctrl Pts',(1.98373572460543,27.935221852351,0.283517324869203));
#9311=CARTESIAN_POINT('Ctrl Pts',(1.97478568882973,27.9583050095701,0.340330980900261));
#9312=CARTESIAN_POINT('Ctrl Pts',(1.96340505169036,27.9813988770421,0.396662939864062));
#9313=CARTESIAN_POINT('Ctrl Pts',(1.95216468683788,28.0042081005558,0.452300578060788));
#9314=CARTESIAN_POINT('Ctrl Pts',(1.93855351319197,28.02702746885,0.507467601072668));
#9315=CARTESIAN_POINT('Ctrl Pts',(1.9226556198672,28.0497338408643,0.561868536454782));
#9316=CARTESIAN_POINT('Ctrl Pts',(1.9064601338198,28.0728652535385,0.617287803143049));
#9317=CARTESIAN_POINT('Ctrl Pts',(1.88789169562905,28.0958790801396,0.671911257271115));
#9318=CARTESIAN_POINT('Ctrl Pts',(1.86709019275729,28.1186494635452,0.725448204198153));
#9319=CARTESIAN_POINT('Ctrl Pts',(1.84628868988553,28.1414198469507,0.778985151125196));
#9320=CARTESIAN_POINT('Ctrl Pts',(1.82325463285926,28.1639465059246,0.831434982719507));
#9321=CARTESIAN_POINT('Ctrl Pts',(1.79817295107597,28.186112422052,0.882538907291619));
#9322=CARTESIAN_POINT('Ctrl Pts',(1.79465710844833,28.1892195451498,0.889702436356488));
#9323=CARTESIAN_POINT('Ctrl Pts',(1.79110109618595,28.1923195979741,0.896839578793933));
#9324=CARTESIAN_POINT('Ctrl Pts',(1.78750548470432,28.1954122767402,0.903949681684058));
#9325=CARTESIAN_POINT('Ctrl Pts',(1.76228706011533,28.2171032983203,0.953817581614572));
#9326=CARTESIAN_POINT('Ctrl Pts',(1.73483868809596,28.239157960823,1.00290422626632));
#9327=CARTESIAN_POINT('Ctrl Pts',(1.70524671602152,28.2614666381511,1.05092079737846));
#9328=CARTESIAN_POINT('Ctrl Pts',(1.67569471951602,28.2837451788574,1.0988725032716));
#9329=CARTESIAN_POINT('Ctrl Pts',(1.64400506357697,28.3062767961068,1.14575631863696));
#9330=CARTESIAN_POINT('Ctrl Pts',(1.61031284530134,28.3289434783753,1.19129904940878));
#9331=CARTESIAN_POINT('Ctrl Pts',(1.57620686946125,28.3518885190223,1.23740106806151));
#9332=CARTESIAN_POINT('Ctrl Pts',(1.54004908309952,28.3749716762411,1.2821281195775));
#9333=CARTESIAN_POINT('Ctrl Pts',(1.50202718274414,28.3980655437126,1.32522270851447));
#9334=CARTESIAN_POINT('Ctrl Pts',(1.46447392213801,28.4208747672248,1.36778613417015));
#9335=CARTESIAN_POINT('Ctrl Pts',(1.42510278848197,28.4436941355174,1.40875659072383));
#9336=CARTESIAN_POINT('Ctrl Pts',(1.38413434130772,28.4664005075303,1.44792023608946));
#9337=CARTESIAN_POINT('Ctrl Pts',(1.34239900561962,28.4895319202046,1.48781698587723));
#9338=CARTESIAN_POINT('Ctrl Pts',(1.29900653937359,28.5125457468058,1.52583806569944));
#9339=CARTESIAN_POINT('Ctrl Pts',(1.25422343598591,28.5353161302116,1.56180167034371));
#9340=CARTESIAN_POINT('Ctrl Pts',(1.20944033259823,28.5580865136173,1.59776527498798));
#9341=CARTESIAN_POINT('Ctrl Pts',(1.16326733826385,28.5806131725913,1.63167113305991));
#9342=CARTESIAN_POINT('Ctrl Pts',(1.11599400238352,28.6027790887188,1.663387589081));
#9343=CARTESIAN_POINT('Ctrl Pts',(1.10936742882001,28.6058862118166,1.66783346591799));
#9344=CARTESIAN_POINT('Ctrl Pts',(1.10271926064605,28.6089862646408,1.67223640644795));
#9345=CARTESIAN_POINT('Ctrl Pts',(1.09605031831593,28.6120789434068,1.6765961304334));
#9346=CARTESIAN_POINT('Ctrl Pts',(1.04927657203313,28.6337699649776,1.70717378629907));
#9347=CARTESIAN_POINT('Ctrl Pts',(1.00096226226722,28.6558246274708,1.73595988153284));
#9348=CARTESIAN_POINT('Ctrl Pts',(0.951326577168889,28.6781333047891,1.76274746587164));
#9349=CARTESIAN_POINT('Ctrl Pts',(0.901757944496797,28.7004118455044,1.78949886308983));
#9350=CARTESIAN_POINT('Ctrl Pts',(0.850871989713288,28.722943462763,1.81425661026415));
#9351=CARTESIAN_POINT('Ctrl Pts',(0.798922307369564,28.7456101450408,1.83685166294178));
#9352=CARTESIAN_POINT('Ctrl Pts',(0.746334656544358,28.768555185688,1.85972419434104));
#9353=CARTESIAN_POINT('Ctrl Pts',(0.692657569252057,28.791638342907,1.88038006400964));
#9354=CARTESIAN_POINT('Ctrl Pts',(0.638182343175099,28.8147322103788,1.89869012261724));
#9355=CARTESIAN_POINT('Ctrl Pts',(0.584378552670652,28.8375414338896,1.91677450020303));
#9356=CARTESIAN_POINT('Ctrl Pts',(0.529796922475223,28.8603608021809,1.93257038955436));
#9357=CARTESIAN_POINT('Ctrl Pts',(0.474735383789332,28.8830671741923,1.94600287775817));
#9358=CARTESIAN_POINT('Ctrl Pts',(0.418643147951686,28.9061985868677,1.95968680875969));
#9359=CARTESIAN_POINT('Ctrl Pts',(0.36205362993619,28.92921241347,1.97091779664273));
#9360=CARTESIAN_POINT('Ctrl Pts',(0.305288522417528,28.9519827968767,1.97967164018299));
#9361=CARTESIAN_POINT('Ctrl Pts',(0.248523414898871,28.9747531802835,1.98842548372325));
#9362=CARTESIAN_POINT('Ctrl Pts',(0.191583499797966,28.9972798392585,1.99470232098375));
#9363=CARTESIAN_POINT('Ctrl Pts',(0.134785361990913,29.019445755387,1.99853290967592));
#9364=CARTESIAN_POINT('Ctrl Pts',(0.126823642527627,29.0225528784843,1.99906986517699));
#9365=CARTESIAN_POINT('Ctrl Pts',(0.118864689736634,29.0256529313079,1.99955883944022));
#9366=CARTESIAN_POINT('Ctrl Pts',(0.11090935427091,29.0287456100735,1.99999999999998));
#9367=CARTESIAN_POINT('Ctrl Pts',(0.0551132738422961,29.0504366316384,2.00309415362558));
#9368=CARTESIAN_POINT('Ctrl Pts',(-0.0011211933826387,29.0724912941254,
2.00386648849128));
#9369=CARTESIAN_POINT('Ctrl Pts',(-0.0575007497658943,29.0947999714375,
2.00224737448728));
#9370=CARTESIAN_POINT('Ctrl Pts',(-0.113804143507052,29.1170785121555,2.00063044773001));
#9371=CARTESIAN_POINT('Ctrl Pts',(-0.170251546639818,29.1396101294169,1.99662830833218));
#9372=CARTESIAN_POINT('Ctrl Pts',(-0.226538817614126,29.1622768116975,1.99022135677887));
#9373=CARTESIAN_POINT('Ctrl Pts',(-0.283517324855257,29.1852218523454,1.98373572460742));
#9374=CARTESIAN_POINT('Ctrl Pts',(-0.340330980887393,29.2083050095649,1.97478568883195));
#9375=CARTESIAN_POINT('Ctrl Pts',(-0.396662939852275,29.2313988770373,1.96340505169272));
#9376=CARTESIAN_POINT('Ctrl Pts',(-0.452300578039161,29.2542081005469,1.95216468684257));
#9377=CARTESIAN_POINT('Ctrl Pts',(-0.507467601041344,29.277027468837,1.93855351319987));
#9378=CARTESIAN_POINT('Ctrl Pts',(-0.561868536414166,29.2997338408473,1.92265561987906));
#9379=CARTESIAN_POINT('Ctrl Pts',(-0.617287803109159,29.3228652535242,1.90646013383096));
#9380=CARTESIAN_POINT('Ctrl Pts',(-0.671911257243838,29.345879080128,1.88789169563894));
#9381=CARTESIAN_POINT('Ctrl Pts',(-0.725448204177296,29.3686494635363,1.86709019276537));
#9382=CARTESIAN_POINT('Ctrl Pts',(-0.778985151110758,29.3914198469445,1.8462886898918));
#9383=CARTESIAN_POINT('Ctrl Pts',(-0.831434982711271,29.413946505921,1.82325463286319));
#9384=CARTESIAN_POINT('Ctrl Pts',(-0.88253890728924,29.4361124220509,1.79817295107712));
#9385=CARTESIAN_POINT('Ctrl Pts',(-0.889702436354912,29.4392195451491,1.7946571084491));
#9386=CARTESIAN_POINT('Ctrl Pts',(-0.896839578793133,29.4423195979737,1.79110109618633));
#9387=CARTESIAN_POINT('Ctrl Pts',(-0.903949681684058,29.4454122767402,1.7875054847043));
#9388=CARTESIAN_POINT('Ctrl Pts',(-0.953817581583688,29.4671032983068,1.76228706013093));
#9389=CARTESIAN_POINT('Ctrl Pts',(-1.00290422620548,29.4891579607957,1.73483868812999));
#9390=CARTESIAN_POINT('Ctrl Pts',(-1.0509207972892,29.5114666381096,1.70524671607653));
#9391=CARTESIAN_POINT('Ctrl Pts',(-1.09887250321126,29.5337451788284,1.67569471955667));
#9392=CARTESIAN_POINT('Ctrl Pts',(-1.1457563186045,29.5562767960907,1.64400506360072));
#9393=CARTESIAN_POINT('Ctrl Pts',(-1.19129904940263,29.5789434783722,1.61031284530589));
#9394=CARTESIAN_POINT('Ctrl Pts',(-1.23740106805556,29.6018885190193,1.57620686946592));
#9395=CARTESIAN_POINT('Ctrl Pts',(-1.28212811957172,29.624971676238,1.54004908310434));
#9396=CARTESIAN_POINT('Ctrl Pts',(-1.32522270850892,29.6480655437097,1.50202718274903));
#9397=CARTESIAN_POINT('Ctrl Pts',(-1.36778613415132,29.6708747672146,1.46447392215491));
#9398=CARTESIAN_POINT('Ctrl Pts',(-1.40875659069272,29.6936941355001,1.42510278851201));
#9399=CARTESIAN_POINT('Ctrl Pts',(-1.44792023604725,29.7164005075058,1.38413434135187));
#9400=CARTESIAN_POINT('Ctrl Pts',(-1.48781698584261,29.7395319201838,1.34239900565837));
#9401=CARTESIAN_POINT('Ctrl Pts',(-1.52583806567193,29.7625457467888,1.29900653940629));
#9402=CARTESIAN_POINT('Ctrl Pts',(-1.56180167032266,29.7853161301982,1.25422343601211));
#9403=CARTESIAN_POINT('Ctrl Pts',(-1.5977652749734,29.8080865136077,1.20944033261793));
#9404=CARTESIAN_POINT('Ctrl Pts',(-1.63167113305121,29.8306131725853,1.1632673382765));
#9405=CARTESIAN_POINT('Ctrl Pts',(-1.66338758907747,29.8527790887163,1.11599400238878));
#9406=CARTESIAN_POINT('Ctrl Pts',(-1.66783346591567,29.8558862118149,1.10936742882351));
#9407=CARTESIAN_POINT('Ctrl Pts',(-1.6722364064468,29.8589862646399,1.1027192606478));
#9408=CARTESIAN_POINT('Ctrl Pts',(-1.67659613043341,29.8620789434068,1.09605031831591));
#9409=CARTESIAN_POINT('Ctrl Pts',(-1.70717378629565,29.8837699649752,1.04927657203835));
#9410=CARTESIAN_POINT('Ctrl Pts',(-1.73595988152635,29.9058246274658,1.0009622622781));
#9411=CARTESIAN_POINT('Ctrl Pts',(-1.76274746586258,29.9281333047816,0.951326577185667));
#9412=CARTESIAN_POINT('Ctrl Pts',(-1.78949886307415,29.9504118454909,0.901757944526982));
#9413=CARTESIAN_POINT('Ctrl Pts',(-1.81425661024294,29.9729434627434,0.850871989757554));
#9414=CARTESIAN_POINT('Ctrl Pts',(-1.83685166291622,29.9956101450151,0.798922307428386));
#9415=CARTESIAN_POINT('Ctrl Pts',(-1.85972419431906,30.0185551856642,0.746334656599543));
#9416=CARTESIAN_POINT('Ctrl Pts',(-1.88038006399093,30.041638342885,0.692657569303313));
#9417=CARTESIAN_POINT('Ctrl Pts',(-1.89869012260142,30.0647322103588,0.638182343222221));
#9418=CARTESIAN_POINT('Ctrl Pts',(-1.91677450018729,30.087541433868,0.584378552721979));
#9419=CARTESIAN_POINT('Ctrl Pts',(-1.93257038953904,30.1103608021577,0.529796922530749));
#9420=CARTESIAN_POINT('Ctrl Pts',(-1.94600287774362,30.1330671741677,0.474735383849046));
#9421=CARTESIAN_POINT('Ctrl Pts',(-1.95968680874906,30.1561985868468,0.418643148002788));
#9422=CARTESIAN_POINT('Ctrl Pts',(-1.97091779663529,30.1792124134529,0.362053629978264));
#9423=CARTESIAN_POINT('Ctrl Pts',(-1.97967164017791,30.2019827968635,0.305288522450557));
#9424=CARTESIAN_POINT('Ctrl Pts',(-1.98842548372053,30.224753180274,0.248523414922854));
#9425=CARTESIAN_POINT('Ctrl Pts',(-1.9947023209826,30.2472798392526,0.191583499812823));
#9426=CARTESIAN_POINT('Ctrl Pts',(-1.99853290967555,30.2694457553847,0.134785361996615));
#9427=CARTESIAN_POINT('Ctrl Pts',(-1.99906986517678,30.2725528784827,0.126823642531405));
#9428=CARTESIAN_POINT('Ctrl Pts',(-1.99955883944014,30.2756529313072,0.118864689738512));
#9429=CARTESIAN_POINT('Ctrl Pts',(-2.,30.2787456100735,0.110909354270867));
#9430=CARTESIAN_POINT('Ctrl Pts',(-2.00309415362522,30.3004366316358,0.0551132738489099));
#9431=CARTESIAN_POINT('Ctrl Pts',(-2.00386648849109,30.3224912941201,-0.00112119336928378));
#9432=CARTESIAN_POINT('Ctrl Pts',(-2.00224737448784,30.3447999714295,-0.0575007497458005));
#9433=CARTESIAN_POINT('Ctrl Pts',(-2.00063044773086,30.3670785121513,-0.113804143496728));
#9434=CARTESIAN_POINT('Ctrl Pts',(-1.99662830833251,30.3896101294167,-0.170251546639406));
#9435=CARTESIAN_POINT('Ctrl Pts',(-1.99022135677783,30.4122768117013,-0.226538817623492));
#9436=CARTESIAN_POINT('Ctrl Pts',(-1.98373572460613,30.4352218523491,-0.283517324864499));
#9437=CARTESIAN_POINT('Ctrl Pts',(-1.9747856888304,30.4583050095686,-0.340330980896505));
#9438=CARTESIAN_POINT('Ctrl Pts',(-1.96340505169093,30.4813988770409,-0.396662939861262));
#9439=CARTESIAN_POINT('Ctrl Pts',(-1.95216468684122,30.5042081005491,-0.452300578044649));
#9440=CARTESIAN_POINT('Ctrl Pts',(-1.93855351319925,30.5270274688378,-0.507467601043391));
#9441=CARTESIAN_POINT('Ctrl Pts',(-1.92265561987947,30.5497338408467,-0.56186853641284));
#9442=CARTESIAN_POINT('Ctrl Pts',(-1.90646013383095,30.5728652535243,-0.617287803109421));
#9443=CARTESIAN_POINT('Ctrl Pts',(-1.88789169563839,30.5958790801287,-0.671911257245612));
#9444=CARTESIAN_POINT('Ctrl Pts',(-1.86709019276414,30.6186494635376,-0.72544820418056));
#9445=CARTESIAN_POINT('Ctrl Pts',(-1.84628868988989,30.6414198469465,-0.778985151115508));
#9446=CARTESIAN_POINT('Ctrl Pts',(-1.82325463286048,30.6639465059236,-0.831434982717405));
#9447=CARTESIAN_POINT('Ctrl Pts',(-1.79817295107351,30.6861124220541,-0.882538907296667));
#9448=CARTESIAN_POINT('Ctrl Pts',(-1.79465710844667,30.6892195451513,-0.889702436359856));
#9449=CARTESIAN_POINT('Ctrl Pts',(-1.79110109618512,30.6923195979748,-0.896839578795616));
#9450=CARTESIAN_POINT('Ctrl Pts',(-1.78750548470434,30.6954122767402,-0.903949681684073));
#9451=CARTESIAN_POINT('Ctrl Pts',(-1.76228706012981,30.7171032983078,-0.953817581585953));
#9452=CARTESIAN_POINT('Ctrl Pts',(-1.73483868812747,30.7391579607977,-1.00290422621001));
#9453=CARTESIAN_POINT('Ctrl Pts',(-1.70524671607249,30.7614666381126,-1.05092079729578));
#9454=CARTESIAN_POINT('Ctrl Pts',(-1.67569471956773,30.78374517882,-1.09887250319292));
#9455=CARTESIAN_POINT('Ctrl Pts',(-1.64400506362909,30.8062767960705,-1.14575631856236));
#9456=CARTESIAN_POINT('Ctrl Pts',(-1.61031284535356,30.8289434783402,-1.19129904933821));
#9457=CARTESIAN_POINT('Ctrl Pts',(-1.57620686951104,30.8518885189901,-1.23740106799845));
#9458=CARTESIAN_POINT('Ctrl Pts',(-1.54004908314627,30.8749716762118,-1.2821281195217));
#9459=CARTESIAN_POINT('Ctrl Pts',(-1.50202718278721,30.8980655436865,-1.32522270846567));
#9460=CARTESIAN_POINT('Ctrl Pts',(-1.46447392219183,30.920874767193,-1.36778613411196));
#9461=CARTESIAN_POINT('Ctrl Pts',(-1.42510278854742,30.9436941354799,-1.40875659065708));
#9462=CARTESIAN_POINT('Ctrl Pts',(-1.38413434138545,30.9664005074872,-1.44792023601518));
#9463=CARTESIAN_POINT('Ctrl Pts',(-1.34239900568604,30.9895319201691,-1.48781698581805));
#9464=CARTESIAN_POINT('Ctrl Pts',(-1.29900653942741,31.0125457467779,-1.52583806565434));
#9465=CARTESIAN_POINT('Ctrl Pts',(-1.25422343602621,31.0353161301911,-1.56180167031137));
#9466=CARTESIAN_POINT('Ctrl Pts',(-1.20944033262501,31.0580865136043,-1.59776527496841));
#9467=CARTESIAN_POINT('Ctrl Pts',(-1.16326733827608,31.0806131725856,-1.63167113305186));
#9468=CARTESIAN_POINT('Ctrl Pts',(-1.11599400238054,31.1027790887202,-1.66338758908304));
#9469=CARTESIAN_POINT('Ctrl Pts',(-1.10936742881802,31.1058862118175,-1.66783346591935));
#9470=CARTESIAN_POINT('Ctrl Pts',(-1.10271926064508,31.1089862646412,-1.67223640644862));
#9471=CARTESIAN_POINT('Ctrl Pts',(-1.09605031831596,31.1120789434068,-1.67659613043341));
#9472=CARTESIAN_POINT('Ctrl Pts',(-1.0492765720558,31.1337699649671,-1.70717378628425));
#9473=CARTESIAN_POINT('Ctrl Pts',(-1.00096226231408,31.1558246274494,-1.73595988150493));
#9474=CARTESIAN_POINT('Ctrl Pts',(-0.951326577241099,31.1781333047567,-1.76274746583267));
#9475=CARTESIAN_POINT('Ctrl Pts',(-0.901757944563462,31.2004118454748,-1.78949886305646));
#9476=CARTESIAN_POINT('Ctrl Pts',(-0.850871989773915,31.2229434627363,-1.81425661023596));
#9477=CARTESIAN_POINT('Ctrl Pts',(-0.798922307423776,31.2456101450171,-1.83685166291821));
#9478=CARTESIAN_POINT('Ctrl Pts',(-0.746334656595517,31.2685551856659,-1.85972419432064));
#9479=CARTESIAN_POINT('Ctrl Pts',(-0.692657569299935,31.2916383428865,-1.88038006399213));
#9480=CARTESIAN_POINT('Ctrl Pts',(-0.638182343219465,31.31473221036,-1.89869012260232));
#9481=CARTESIAN_POINT('Ctrl Pts',(-0.584378552727823,31.3375414338655,-1.91677450018521));
#9482=CARTESIAN_POINT('Ctrl Pts',(-0.529796922545472,31.3603608021516,-1.93257038953474));
#9483=CARTESIAN_POINT('Ctrl Pts',(-0.474735383872727,31.3830671741579,-1.94600287773785));
#9484=CARTESIAN_POINT('Ctrl Pts',(-0.41864314802318,31.4061985868385,-1.95968680874481));
#9485=CARTESIAN_POINT('Ctrl Pts',(-0.36205362999544,31.429212413446,-1.97091779663224));
#9486=CARTESIAN_POINT('Ctrl Pts',(-0.305288522464344,31.451982796858,-1.97967164017579));
#9487=CARTESIAN_POINT('Ctrl Pts',(-0.248523414933249,31.4747531802699,-1.98842548371934));
#9488=CARTESIAN_POINT('Ctrl Pts',(-0.19158349981977,31.4972798392499,-1.99470232098204));
#9489=CARTESIAN_POINT('Ctrl Pts',(-0.134785362000163,31.5194457553834,-1.99853290967532));
#9490=CARTESIAN_POINT('Ctrl Pts',(-0.126823642533793,31.5225528784818,-1.99906986517664));
#9491=CARTESIAN_POINT('Ctrl Pts',(-0.118864689739719,31.5256529313067,-1.99955883944008));
#9492=CARTESIAN_POINT('Ctrl Pts',(-0.110909354270916,31.5287456100735,-2.00000000000001));
#9493=CARTESIAN_POINT('Ctrl Pts',(-0.0551132738398505,31.5504366316393,
-2.00309415362574));
#9494=CARTESIAN_POINT('Ctrl Pts',(0.00112119338755449,31.5724912941273,
-2.00386648849135));
#9495=CARTESIAN_POINT('Ctrl Pts',(0.0575007497732957,31.5947999714404,-2.00224737448707));
#9496=CARTESIAN_POINT('Ctrl Pts',(0.113804143504013,31.6170785121543,-2.00063044772989));
#9497=CARTESIAN_POINT('Ctrl Pts',(0.170251546626252,31.6396101294115,-1.99662830833307));
#9498=CARTESIAN_POINT('Ctrl Pts',(0.226538817590147,31.6622768116879,-1.99022135678163));
#9499=CARTESIAN_POINT('Ctrl Pts',(0.283517324833422,31.6852218523365,-1.98373572461064));
#9500=CARTESIAN_POINT('Ctrl Pts',(0.340330980867798,31.7083050095569,-1.97478568883542));
#9501=CARTESIAN_POINT('Ctrl Pts',(0.396662939834899,31.7313988770301,-1.96340505169626));
#9502=CARTESIAN_POINT('Ctrl Pts',(0.452300578015339,31.7542081005371,-1.95216468684793));
#9503=CARTESIAN_POINT('Ctrl Pts',(0.507467601011179,31.7770274688245,-1.93855351320761));
#9504=CARTESIAN_POINT('Ctrl Pts',(0.561868536377917,31.7997338408322,-1.92265561988969));
#9505=CARTESIAN_POINT('Ctrl Pts',(0.617287803079549,31.8228652535117,-1.90646013384078));
#9506=CARTESIAN_POINT('Ctrl Pts',(0.671911257220686,31.8458790801182,-1.88789169564743));
#9507=CARTESIAN_POINT('Ctrl Pts',(0.725448204160488,31.8686494635291,-1.86709019277195));
#9508=CARTESIAN_POINT('Ctrl Pts',(0.778985151100286,31.89141984694,-1.84628868989648));
#9509=CARTESIAN_POINT('Ctrl Pts',(0.83143498270685,31.9139465059191,-1.82325463286546));
#9510=CARTESIAN_POINT('Ctrl Pts',(0.882538907290595,31.9361124220515,-1.79817295107651));
#9511=CARTESIAN_POINT('Ctrl Pts',(0.889702436355825,31.9392195451495,-1.7946571084487));
#9512=CARTESIAN_POINT('Ctrl Pts',(0.89683957879358,31.9423195979739,-1.79110109618616));
#9513=CARTESIAN_POINT('Ctrl Pts',(0.90394968168406,31.9454122767402,-1.78750548470436));
#9514=CARTESIAN_POINT('Ctrl Pts',(0.953817581579516,31.967103298305,-1.7622870601331));
#9515=CARTESIAN_POINT('Ctrl Pts',(1.0029042261973,31.989157960792,-1.73483868813461));
#9516=CARTESIAN_POINT('Ctrl Pts',(1.0509207972772,32.011466638104,-1.70524671608398));
#9517=CARTESIAN_POINT('Ctrl Pts',(1.09887250319299,32.0337451788198,-1.67569471956845));
#9518=CARTESIAN_POINT('Ctrl Pts',(1.14575631858028,32.056276796079,-1.64400506361739));
#9519=CARTESIAN_POINT('Ctrl Pts',(1.19129904937289,32.0789434783574,-1.61031284532795));
#9520=CARTESIAN_POINT('Ctrl Pts',(1.23740106802881,32.1018885190056,-1.5762068694871));
#9521=CARTESIAN_POINT('Ctrl Pts',(1.28212811954792,32.1249716762256,-1.54004908312433));
#9522=CARTESIAN_POINT('Ctrl Pts',(1.32522270848791,32.1480655436984,-1.50202718276764));
#9523=CARTESIAN_POINT('Ctrl Pts',(1.36778613413943,32.170874767208,-1.46447392216653));
#9524=CARTESIAN_POINT('Ctrl Pts',(1.40875659068932,32.1936941354981,-1.4251027885159));
#9525=CARTESIAN_POINT('Ctrl Pts',(1.44792023605164,32.2164005075084,-1.38413434134735));
#9526=CARTESIAN_POINT('Ctrl Pts',(1.48781698584602,32.2395319201859,-1.34239900565462));
#9527=CARTESIAN_POINT('Ctrl Pts',(1.52583806567441,32.2625457467904,-1.29900653940341));
#9528=CARTESIAN_POINT('Ctrl Pts',(1.56180167032433,32.2853161301994,-1.25422343601012));
#9529=CARTESIAN_POINT('Ctrl Pts',(1.59776527497424,32.3080865136083,-1.20944033261684));
#9530=CARTESIAN_POINT('Ctrl Pts',(1.63167113305132,32.3306131725855,-1.16326733827636));
#9531=CARTESIAN_POINT('Ctrl Pts',(1.66338758907691,32.352779088716,-1.1159940023897));
#9532=CARTESIAN_POINT('Ctrl Pts',(1.6678334659153,32.3558862118148,-1.10936742882416));
#9533=CARTESIAN_POINT('Ctrl Pts',(1.67223640644662,32.3589862646399,-1.10271926064816));
#9534=CARTESIAN_POINT('Ctrl Pts',(1.67659613043341,32.3620789434069,-1.09605031831599));
#9535=CARTESIAN_POINT('Ctrl Pts',(1.70717378628998,32.3837699649712,-1.04927657204709));
#9536=CARTESIAN_POINT('Ctrl Pts',(1.73595988151573,32.4058246274578,-1.00096226229599));
#9537=CARTESIAN_POINT('Ctrl Pts',(1.76274746584775,32.4281333047693,-0.951326577213187));
#9538=CARTESIAN_POINT('Ctrl Pts',(1.78949886306025,32.4504118454787,-0.901757944554595));
#9539=CARTESIAN_POINT('Ctrl Pts',(1.81425661022999,32.4729434627313,-0.850871989785215));
#9540=CARTESIAN_POINT('Ctrl Pts',(1.83685166290423,32.4956101450031,-0.798922307455973));
#9541=CARTESIAN_POINT('Ctrl Pts',(1.8597241943091,32.5185551856534,-0.746334656624628));
#9542=CARTESIAN_POINT('Ctrl Pts',(1.88038006398273,32.5416383428755,-0.692657569325824));
#9543=CARTESIAN_POINT('Ctrl Pts',(1.89869012259478,32.5647322103505,-0.638182343241963));
#9544=CARTESIAN_POINT('Ctrl Pts',(1.91677450017834,32.5875414338561,-0.584378552750432));
#9545=CARTESIAN_POINT('Ctrl Pts',(1.93257038952854,32.6103608021422,-0.529796922568127));
#9546=CARTESIAN_POINT('Ctrl Pts',(1.94600287773232,32.6330671741486,-0.474735383895403));
#9547=CARTESIAN_POINT('Ctrl Pts',(1.95968680874129,32.6561985868315,-0.418643148040505));
#9548=CARTESIAN_POINT('Ctrl Pts',(1.97091779663025,32.6792124134413,-0.362053630007222));
#9549=CARTESIAN_POINT('Ctrl Pts',(1.97967164017484,32.7019827968555,-0.305288522470557));
#9550=CARTESIAN_POINT('Ctrl Pts',(1.98842548371943,32.7247531802696,-0.248523414933892));
#9551=CARTESIAN_POINT('Ctrl Pts',(1.99470232098267,32.7472798392519,-0.191583499814767));
#9552=CARTESIAN_POINT('Ctrl Pts',(1.99853290967603,32.7694457553875,-0.134785361989606));
#9553=CARTESIAN_POINT('Ctrl Pts',(1.99906986517707,32.7725528784846,-0.126823642526751));
#9554=CARTESIAN_POINT('Ctrl Pts',(1.99955883944027,32.7756529313081,-0.118864689736211));
#9555=CARTESIAN_POINT('Ctrl Pts',(2.,32.7787456100735,-0.110909354270917));
#9556=CARTESIAN_POINT('Ctrl Pts',(2.00309415362607,32.8004366316417,-0.0551132738337146));
#9557=CARTESIAN_POINT('Ctrl Pts',(2.00386648849151,32.8224912941322,0.00112119339992733));
#9558=CARTESIAN_POINT('Ctrl Pts',(2.00224737448652,32.8447999714478,0.0575007497919306));
#9559=CARTESIAN_POINT('Ctrl Pts',(2.00063044772872,32.8670785121631,0.113804143526022));
#9560=CARTESIAN_POINT('Ctrl Pts',(1.99662830833099,32.8896101294217,0.170251546651625));
#9561=CARTESIAN_POINT('Ctrl Pts',(1.99022135677835,32.9122768116995,0.226538817618813));
#9562=CARTESIAN_POINT('Ctrl Pts',(1.9837357246068,32.9352218523472,0.283517324859671));
#9563=CARTESIAN_POINT('Ctrl Pts',(1.97478568883126,32.9583050095666,0.34033098089147));
#9564=CARTESIAN_POINT('Ctrl Pts',(1.96340505169196,32.9813988770389,0.396662939856094));
#9565=CARTESIAN_POINT('Ctrl Pts',(1.95216468684278,33.0042081005464,0.452300578037654));
#9566=CARTESIAN_POINT('Ctrl Pts',(1.93855351320149,33.0270274688343,0.50746760103459));
#9567=CARTESIAN_POINT('Ctrl Pts',(1.92265561988254,33.0497338408424,0.56186853640232));
#9568=CARTESIAN_POINT('Ctrl Pts',(1.90646013383411,33.0728652535203,0.617287803099664));
#9569=CARTESIAN_POINT('Ctrl Pts',(1.88789169564162,33.095879080125,0.671911257236546));
#9570=CARTESIAN_POINT('Ctrl Pts',(1.86709019276736,33.1186494635342,0.725448204172222));
#9571=CARTESIAN_POINT('Ctrl Pts',(1.8462886898931,33.1414198469433,0.7789851511079));
#9572=CARTESIAN_POINT('Ctrl Pts',(1.82325463286361,33.1639465059207,0.831434982710542));
#9573=CARTESIAN_POINT('Ctrl Pts',(1.79817295107649,33.1861124220515,0.882538907290563));
#9574=CARTESIAN_POINT('Ctrl Pts',(1.79465710844868,33.1892195451495,0.889702436355792));
#9575=CARTESIAN_POINT('Ctrl Pts',(1.79110109618616,33.1923195979739,0.896839578793529));
#9576=CARTESIAN_POINT('Ctrl Pts',(1.78750548470435,33.1954122767402,0.903949681684009));
#9577=CARTESIAN_POINT('Ctrl Pts',(1.76228706012904,33.2171032983085,0.953817581587484));
#9578=CARTESIAN_POINT('Ctrl Pts',(1.73483868812578,33.2391579607991,1.00290422621303));
#9579=CARTESIAN_POINT('Ctrl Pts',(1.7052467160697,33.2614666381147,1.0509207973003));
#9580=CARTESIAN_POINT('Ctrl Pts',(1.67569471954817,33.2837451788346,1.09887250322439));
#9581=CARTESIAN_POINT('Ctrl Pts',(1.64400506359036,33.306276796098,1.14575631861951));
#9582=CARTESIAN_POINT('Ctrl Pts',(1.61031284529353,33.3289434783805,1.19129904941936));
#9583=CARTESIAN_POINT('Ctrl Pts',(1.57620686945373,33.3518885190272,1.23740106807108));
#9584=CARTESIAN_POINT('Ctrl Pts',(1.54004908309237,33.3749716762455,1.28212811958608));
#9585=CARTESIAN_POINT('Ctrl Pts',(1.5020271827374,33.3980655437167,1.32522270852215));
#9586=CARTESIAN_POINT('Ctrl Pts',(1.46447392213645,33.4208747672256,1.36778613417152));
#9587=CARTESIAN_POINT('Ctrl Pts',(1.42510278848614,33.4436941355149,1.40875659071932));
#9588=CARTESIAN_POINT('Ctrl Pts',(1.38413434131808,33.4664005075245,1.44792023607959));
#9589=CARTESIAN_POINT('Ctrl Pts',(1.34239900562838,33.4895319201999,1.48781698586946));
#9590=CARTESIAN_POINT('Ctrl Pts',(1.2990065393805,33.5125457468022,1.52583806569369));
#9591=CARTESIAN_POINT('Ctrl Pts',(1.25422343599088,33.535316130209,1.56180167033975));
#9592=CARTESIAN_POINT('Ctrl Pts',(1.20944033260126,33.5580865136158,1.59776527498582));
#9593=CARTESIAN_POINT('Ctrl Pts',(1.16326733826477,33.5806131725909,1.63167113305938));
#9594=CARTESIAN_POINT('Ctrl Pts',(1.11599400238226,33.6027790887194,1.66338758908187));
#9595=CARTESIAN_POINT('Ctrl Pts',(1.10936742881915,33.605886211817,1.66783346591858));
#9596=CARTESIAN_POINT('Ctrl Pts',(1.10271926064564,33.6089862646409,1.67223640644824));
#9597=CARTESIAN_POINT('Ctrl Pts',(1.09605031831594,33.6120789434068,1.67659613043342));
#9598=CARTESIAN_POINT('Ctrl Pts',(1.04927657202145,33.633769964983,1.70717378630673));
#9599=CARTESIAN_POINT('Ctrl Pts',(1.00096226224306,33.6558246274818,1.73595988154725));
#9600=CARTESIAN_POINT('Ctrl Pts',(0.951326577131669,33.6781333048059,1.76274746589174));
#9601=CARTESIAN_POINT('Ctrl Pts',(0.9017579444866,33.7004118455088,1.78949886309399));
#9602=CARTESIAN_POINT('Ctrl Pts',(0.850871989731664,33.7229434627548,1.81425661025458));
#9603=CARTESIAN_POINT('Ctrl Pts',(0.798922307417563,33.7456101450198,1.83685166292093));
#9604=CARTESIAN_POINT('Ctrl Pts',(0.74633465658928,33.7685551856686,1.85972419432316));
#9605=CARTESIAN_POINT('Ctrl Pts',(0.692657569293636,33.7916383428892,1.88038006399447));
#9606=CARTESIAN_POINT('Ctrl Pts',(0.638182343213203,33.8147322103626,1.89869012260445));
#9607=CARTESIAN_POINT('Ctrl Pts',(0.584378552714243,33.8375414338713,1.9167745001896));
#9608=CARTESIAN_POINT('Ctrl Pts',(0.529796922524388,33.8603608021604,1.93257038954074));
#9609=CARTESIAN_POINT('Ctrl Pts',(0.474735383844064,33.8830671741698,1.94600287774484));
#9610=CARTESIAN_POINT('Ctrl Pts',(0.41864314799823,33.9061985868487,1.95968680875001));
#9611=CARTESIAN_POINT('Ctrl Pts',(0.362053629974232,33.9292124134546,1.97091779663601));
#9612=CARTESIAN_POINT('Ctrl Pts',(0.305288522446999,33.9519827968649,1.97967164017845));
#9613=CARTESIAN_POINT('Ctrl Pts',(0.248523414919767,33.9747531802752,1.98842548372089));
#9614=CARTESIAN_POINT('Ctrl Pts',(0.191583499810152,33.9972798392537,1.99470232098282));
#9615=CARTESIAN_POINT('Ctrl Pts',(0.134785361994467,34.0194457553856,1.99853290967567));
#9616=CARTESIAN_POINT('Ctrl Pts',(0.126823642529998,34.0225528784833,1.99906986517684));
#9617=CARTESIAN_POINT('Ctrl Pts',(0.118864689737823,34.0256529313075,1.99955883944015));
#9618=CARTESIAN_POINT('Ctrl Pts',(0.110909354270907,34.0287456100735,1.99999999999998));
#9619=CARTESIAN_POINT('Ctrl Pts',(0.0551132738170328,34.0504366316482,2.003094153627));
#9620=CARTESIAN_POINT('Ctrl Pts',(-0.00112119343355195,34.0724912941454,
2.00386648849196));
#9621=CARTESIAN_POINT('Ctrl Pts',(-0.0575007498424811,34.0947999714678,
2.00224737448507));
#9622=CARTESIAN_POINT('Ctrl Pts',(-0.113804143559823,34.1170785121765,2.00063044772634));
#9623=CARTESIAN_POINT('Ctrl Pts',(-0.17025154666847,34.1396101294284,1.99662830832909));
#9624=CARTESIAN_POINT('Ctrl Pts',(-0.226538817618813,34.1622768116994,1.99022135677838));
#9625=CARTESIAN_POINT('Ctrl Pts',(-0.283517324859929,34.1852218523472,1.9837357246068));
#9626=CARTESIAN_POINT('Ctrl Pts',(-0.340330980892099,34.2083050095668,1.97478568883116));
#9627=CARTESIAN_POINT('Ctrl Pts',(-0.396662939856971,34.2313988770392,1.96340505169179));
#9628=CARTESIAN_POINT('Ctrl Pts',(-0.452300578027502,34.2542081005421,1.95216468684481));
#9629=CARTESIAN_POINT('Ctrl Pts',(-0.507467601013651,34.2770274688255,1.93855351320665));
#9630=CARTESIAN_POINT('Ctrl Pts',(-0.561868536370906,34.2997338408293,1.92265561989172));
#9631=CARTESIAN_POINT('Ctrl Pts',(-0.617287803074319,34.3228652535095,1.9064601338425));
#9632=CARTESIAN_POINT('Ctrl Pts',(-0.671911257217177,34.3458790801167,1.88789169564869));
#9633=CARTESIAN_POINT('Ctrl Pts',(-0.725448204158619,34.3686494635283,1.86709019277263));
#9634=CARTESIAN_POINT('Ctrl Pts',(-0.778985151100058,34.3914198469399,1.84628868989658));
#9635=CARTESIAN_POINT('Ctrl Pts',(-0.831434982708242,34.4139465059197,1.82325463286483));
#9636=CARTESIAN_POINT('Ctrl Pts',(-0.88253890729354,34.4361124220528,1.79817295107501));
#9637=CARTESIAN_POINT('Ctrl Pts',(-0.88970243635778,34.4392195451504,1.79465710844767));
#9638=CARTESIAN_POINT('Ctrl Pts',(-0.896839578794564,34.4423195979743,1.79110109618562));
#9639=CARTESIAN_POINT('Ctrl Pts',(-0.903949681684068,34.4454122767402,1.78750548470431));
#9640=CARTESIAN_POINT('Ctrl Pts',(-0.953817581595336,34.4671032983119,1.76228706012506));
#9641=CARTESIAN_POINT('Ctrl Pts',(-1.00290422622842,34.489157960806,1.73483868811717));
#9642=CARTESIAN_POINT('Ctrl Pts',(-1.05092079732283,34.5114666381252,1.70524671605581));
#9643=CARTESIAN_POINT('Ctrl Pts',(-1.09887250321489,34.5337451788305,1.67569471955315));
#9644=CARTESIAN_POINT('Ctrl Pts',(-1.14575631857937,34.5562767960788,1.64400506361705));
#9645=CARTESIAN_POINT('Ctrl Pts',(-1.19129904935051,34.5789434783463,1.61031284534447));
#9646=CARTESIAN_POINT('Ctrl Pts',(-1.237401068009,34.6018885189955,1.57620686950271));
#9647=CARTESIAN_POINT('Ctrl Pts',(-1.28212811953057,34.6249716762165,1.54004908313884));
#9648=CARTESIAN_POINT('Ctrl Pts',(-1.32522270847289,34.6480655436903,1.50202718278086));
#9649=CARTESIAN_POINT('Ctrl Pts',(-1.36778613412684,34.670874767201,1.46447392217835));
#9650=CARTESIAN_POINT('Ctrl Pts',(-1.4087565906791,34.6936941354922,1.42510278852607));
#9651=CARTESIAN_POINT('Ctrl Pts',(-1.44792023604355,34.7164005075036,1.38413434135578));
#9652=CARTESIAN_POINT('Ctrl Pts',(-1.48781698583993,34.7395319201822,1.34239900566143));
#9653=CARTESIAN_POINT('Ctrl Pts',(-1.52583806567025,34.7625457467878,1.29900653940836));
#9654=CARTESIAN_POINT('Ctrl Pts',(-1.56180167032184,34.7853161301977,1.25422343601316));
#9655=CARTESIAN_POINT('Ctrl Pts',(-1.59776527497344,34.8080865136077,1.20944033261796));
#9656=CARTESIAN_POINT('Ctrl Pts',(-1.63167113305207,34.8306131725858,1.16326733827539));
#9657=CARTESIAN_POINT('Ctrl Pts',(-1.66338758907898,34.8527790887174,1.11599400238656));
#9658=CARTESIAN_POINT('Ctrl Pts',(-1.66783346591667,34.8558862118156,1.10936742882202));
#9659=CARTESIAN_POINT('Ctrl Pts',(-1.67223640644732,34.8589862646403,1.10271926064705));
#9660=CARTESIAN_POINT('Ctrl Pts',(-1.67659613043344,34.8620789434068,1.0960503183159));
#9661=CARTESIAN_POINT('Ctrl Pts',(-1.70717378628652,34.8837699649687,1.04927657205235));
#9662=CARTESIAN_POINT('Ctrl Pts',(-1.73595988150919,34.9058246274527,1.00096226230697));
#9663=CARTESIAN_POINT('Ctrl Pts',(-1.76274746583861,34.9281333047616,0.951326577230139));
#9664=CARTESIAN_POINT('Ctrl Pts',(-1.78949886305682,34.9504118454753,0.901757944562123));
#9665=CARTESIAN_POINT('Ctrl Pts',(-1.81425661023148,34.9729434627324,0.850871989782791));
#9666=CARTESIAN_POINT('Ctrl Pts',(-1.83685166290977,34.9956101450087,0.79892230744325));
#9667=CARTESIAN_POINT('Ctrl Pts',(-1.85972419431345,35.0185551856582,0.746334656613635));
#9668=CARTESIAN_POINT('Ctrl Pts',(-1.88038006398612,35.0416383428795,0.692657569316508));
#9669=CARTESIAN_POINT('Ctrl Pts',(-1.89869012259731,35.0647322103537,0.63818234323446));
#9670=CARTESIAN_POINT('Ctrl Pts',(-1.91677450018293,35.0875414338621,0.584378552736114));
#9671=CARTESIAN_POINT('Ctrl Pts',(-1.93257038953459,35.1103608021511,0.529796922546848));
#9672=CARTESIAN_POINT('Ctrl Pts',(-1.94600287773923,35.1330671741603,0.474735383867086));
#9673=CARTESIAN_POINT('Ctrl Pts',(-1.95968680874581,35.1561985868406,0.418643148018389));
#9674=CARTESIAN_POINT('Ctrl Pts',(-1.97091779663295,35.1792124134477,0.362053629991456));
#9675=CARTESIAN_POINT('Ctrl Pts',(-1.97967164017628,35.2019827968593,0.305288522461236));
#9676=CARTESIAN_POINT('Ctrl Pts',(-1.9884254837196,35.2247531802708,0.248523414931019));
#9677=CARTESIAN_POINT('Ctrl Pts',(-1.99470232098214,35.2472798392506,0.191583499818388));
#9678=CARTESIAN_POINT('Ctrl Pts',(-1.99853290967534,35.2694457553837,0.134785361999652));
#9679=CARTESIAN_POINT('Ctrl Pts',(-1.99906986517665,35.2725528784821,0.126823642533447));
#9680=CARTESIAN_POINT('Ctrl Pts',(-1.99955883944008,35.2756529313069,0.118864689739538));
#9681=CARTESIAN_POINT('Ctrl Pts',(-2.,35.2787456100736,0.110909354270899));
#9682=CARTESIAN_POINT('Ctrl Pts',(-2.00309415362537,35.3004366316368,0.0551132738463816));
#9683=CARTESIAN_POINT('Ctrl Pts',(-2.00386648849116,35.3224912941222,-0.00112119337437951));
#9684=CARTESIAN_POINT('Ctrl Pts',(-2.00224737448763,35.3447999714326,-0.057500749753497));
#9685=CARTESIAN_POINT('Ctrl Pts',(-2.00063044773093,35.3670785121475,-0.113804143486897));
#9686=CARTESIAN_POINT('Ctrl Pts',(-1.99662830833435,35.3896101294058,-0.170251546611904));
#9687=CARTESIAN_POINT('Ctrl Pts',(-1.99022135678294,35.4122768116832,-0.22653881757851));
#9688=CARTESIAN_POINT('Ctrl Pts',(-1.98373572461215,35.4352218523323,-0.283517324822981));
#9689=CARTESIAN_POINT('Ctrl Pts',(-1.97478568883704,35.4583050095531,-0.340330980858573));
#9690=CARTESIAN_POINT('Ctrl Pts',(-1.96340505169788,35.4813988770269,-0.396662939826877));
#9691=CARTESIAN_POINT('Ctrl Pts',(-1.95216468684771,35.504208100538,-0.452300578017591));
#9692=CARTESIAN_POINT('Ctrl Pts',(-1.93855351320464,35.5270274688296,-0.507467601023617));
#9693=CARTESIAN_POINT('Ctrl Pts',(-1.92265561988317,35.5497338408415,-0.561868536400175));
#9694=CARTESIAN_POINT('Ctrl Pts',(-1.90646013383459,35.5728652535196,-0.617287803098313));
#9695=CARTESIAN_POINT('Ctrl Pts',(-1.88789169564186,35.5958790801247,-0.671911257236012));
#9696=CARTESIAN_POINT('Ctrl Pts',(-1.8670901927673,35.6186494635342,-0.725448204172447));
#9697=CARTESIAN_POINT('Ctrl Pts',(-1.84628868989274,35.6414198469437,-0.778985151108882));
#9698=CARTESIAN_POINT('Ctrl Pts',(-1.82325463286292,35.6639465059214,-0.831434982712158));
#9699=CARTESIAN_POINT('Ctrl Pts',(-1.7981729510754,35.6861124220525,-0.882538907292838));
#9700=CARTESIAN_POINT('Ctrl Pts',(-1.79465710844794,35.6892195451502,-0.889702436357317));
#9701=CARTESIAN_POINT('Ctrl Pts',(-1.79110109618577,35.6923195979742,-0.896839578794341));
#9702=CARTESIAN_POINT('Ctrl Pts',(-1.78750548470434,35.6954122767402,-0.903949681684091));
#9703=CARTESIAN_POINT('Ctrl Pts',(-1.7622870601352,35.7171032983032,-0.953817581575309));
#9704=CARTESIAN_POINT('Ctrl Pts',(-1.73483868813926,35.7391579607882,-1.00290422618897));
#9705=CARTESIAN_POINT('Ctrl Pts',(-1.7052467160915,35.7614666380983,-1.05092079726496));
#9706=CARTESIAN_POINT('Ctrl Pts',(-1.67569471957129,35.7837451788179,-1.09887250318912));
#9707=CARTESIAN_POINT('Ctrl Pts',(-1.64400506361483,35.8062767960809,-1.14575631858438));
#9708=CARTESIAN_POINT('Ctrl Pts',(-1.61031284531932,35.8289434783632,-1.19129904938451));
#9709=CARTESIAN_POINT('Ctrl Pts',(-1.57620686947829,35.8518885190113,-1.23740106803997));
#9710=CARTESIAN_POINT('Ctrl Pts',(-1.54004908311541,35.8749716762312,-1.28212811955859));
#9711=CARTESIAN_POINT('Ctrl Pts',(-1.50202718275863,35.8980655437039,-1.3252227084981));
#9712=CARTESIAN_POINT('Ctrl Pts',(-1.46447392215545,35.9208747672145,-1.36778613415137));
#9713=CARTESIAN_POINT('Ctrl Pts',(-1.42510278850262,35.9436941355056,-1.40875659070282));
#9714=CARTESIAN_POINT('Ctrl Pts',(-1.38413434133177,35.966400507517,-1.44792023606651));
#9715=CARTESIAN_POINT('Ctrl Pts',(-1.34239900563994,35.9895319201938,-1.48781698585917));
#9716=CARTESIAN_POINT('Ctrl Pts',(-1.29900653938969,36.0125457467975,-1.525838065686));
#9717=CARTESIAN_POINT('Ctrl Pts',(-1.25422343599754,36.0353161302057,-1.56180167033442));
#9718=CARTESIAN_POINT('Ctrl Pts',(-1.20944033260538,36.0580865136139,-1.59776527498283));
#9719=CARTESIAN_POINT('Ctrl Pts',(-1.16326733826615,36.0806131725903,-1.63167113305853));
#9720=CARTESIAN_POINT('Ctrl Pts',(-1.11599400238079,36.1027790887202,-1.66338758908287));
#9721=CARTESIAN_POINT('Ctrl Pts',(-1.10936742881818,36.1058862118175,-1.66783346591924));
#9722=CARTESIAN_POINT('Ctrl Pts',(-1.10271926064514,36.1089862646413,-1.67223640644858));
#9723=CARTESIAN_POINT('Ctrl Pts',(-1.09605031831594,36.1120789434069,-1.67659613043343));
#9724=CARTESIAN_POINT('Ctrl Pts',(-1.04927657205386,36.1337699649681,-1.70717378628555));
#9725=CARTESIAN_POINT('Ctrl Pts',(-1.00096226231002,36.1558246274514,-1.73595988150737));
#9726=CARTESIAN_POINT('Ctrl Pts',(-0.951326577234831,36.1781333047596,-1.76274746583607));
#9727=CARTESIAN_POINT('Ctrl Pts',(-0.90175794458037,36.2004118454672,-1.78949886304713));
#9728=CARTESIAN_POINT('Ctrl Pts',(-0.850871989815301,36.2229434627181,-1.81425661021575));
#9729=CARTESIAN_POINT('Ctrl Pts',(-0.798922307490469,36.2456101449881,-1.83685166288923));
#9730=CARTESIAN_POINT('Ctrl Pts',(-0.746334656657006,36.2685551856395,-1.8597241942962));
#9731=CARTESIAN_POINT('Ctrl Pts',(-0.692657569355879,36.2916383428626,-1.88038006397175));
#9732=CARTESIAN_POINT('Ctrl Pts',(-0.638182343269583,36.3147322103388,-1.8986901225855));
#9733=CARTESIAN_POINT('Ctrl Pts',(-0.584378552779296,36.337541433844,-1.91677450016952));
#9734=CARTESIAN_POINT('Ctrl Pts',(-0.529796922598241,36.3603608021297,-1.93257038952026));
#9735=CARTESIAN_POINT('Ctrl Pts',(-0.474735383926685,36.3830671741357,-1.9460028777247));
#9736=CARTESIAN_POINT('Ctrl Pts',(-0.418643148067304,36.4061985868206,-1.95968680873571));
#9737=CARTESIAN_POINT('Ctrl Pts',(-0.362053630029398,36.4292124134324,-1.97091779662633));
#9738=CARTESIAN_POINT('Ctrl Pts',(-0.305288522488081,36.4519827968485,-1.97967164017215));
#9739=CARTESIAN_POINT('Ctrl Pts',(-0.248523414946763,36.4747531802646,-1.98842548371797));
#9740=CARTESIAN_POINT('Ctrl Pts',(-0.191583499822922,36.4972798392487,-1.99470232098204));
#9741=CARTESIAN_POINT('Ctrl Pts',(-0.134785361993063,36.5194457553861,-1.99853290967581));
#9742=CARTESIAN_POINT('Ctrl Pts',(-0.126823642529047,36.5225528784837,-1.99906986517694));
#9743=CARTESIAN_POINT('Ctrl Pts',(-0.118864689737348,36.5256529313077,-1.99955883944022));
#9744=CARTESIAN_POINT('Ctrl Pts',(-0.110909354270885,36.5287456100735,-2.00000000000002));
#9745=CARTESIAN_POINT('Ctrl Pts',(-0.0551132738534362,36.550436631634,-2.00309415362498));
#9746=CARTESIAN_POINT('Ctrl Pts',(0.00112119336012617,36.5724912941166,
-2.00386648849097));
#9747=CARTESIAN_POINT('Ctrl Pts',(0.0575007497320264,36.5947999714241,-2.00224737448824));
#9748=CARTESIAN_POINT('Ctrl Pts',(0.113804143472436,36.6170785121417,-2.00063044773194));
#9749=CARTESIAN_POINT('Ctrl Pts',(0.170251546604555,36.6396101294028,-1.99662830833518));
#9750=CARTESIAN_POINT('Ctrl Pts',(0.226538817578213,36.6622768116831,-1.99022135678297));
#9751=CARTESIAN_POINT('Ctrl Pts',(0.283517324822228,36.685221852332,-1.98373572461224));
#9752=CARTESIAN_POINT('Ctrl Pts',(0.340330980857321,36.7083050095526,-1.97478568883723));
#9753=CARTESIAN_POINT('Ctrl Pts',(0.396662939825195,36.7313988770262,-1.96340505169821));
#9754=CARTESIAN_POINT('Ctrl Pts',(0.452300578007919,36.754208100534,-1.95216468684971));
#9755=CARTESIAN_POINT('Ctrl Pts',(0.507467601006086,36.7770274688224,-1.93855351320899));
#9756=CARTESIAN_POINT('Ctrl Pts',(0.561868536375043,36.799733840831,-1.92265561989052));
#9757=CARTESIAN_POINT('Ctrl Pts',(0.617287803076668,36.8228652535105,-1.9064601338417));
#9758=CARTESIAN_POINT('Ctrl Pts',(0.671911257217822,36.845879080117,-1.88789169564844));
#9759=CARTESIAN_POINT('Ctrl Pts',(0.725448204157609,36.8686494635279,-1.86709019277307));
#9760=CARTESIAN_POINT('Ctrl Pts',(0.7789851510974,36.8914198469388,-1.84628868989769));
#9761=CARTESIAN_POINT('Ctrl Pts',(0.831434982703969,36.9139465059178,-1.82325463286677));
#9762=CARTESIAN_POINT('Ctrl Pts',(0.882538907287744,36.9361124220503,-1.79817295107791));
#9763=CARTESIAN_POINT('Ctrl Pts',(0.889702436353935,36.9392195451487,-1.79465710844964));
#9764=CARTESIAN_POINT('Ctrl Pts',(0.896839578792637,36.9423195979735,-1.79110109618665));
#9765=CARTESIAN_POINT('Ctrl Pts',(0.903949681684071,36.9454122767402,-1.78750548470436));
#9766=CARTESIAN_POINT('Ctrl Pts',(0.953817581548078,36.9671032982913,-1.76228706014896));
#9767=CARTESIAN_POINT('Ctrl Pts',(1.0029042261354,36.9891579607642,-1.73483868816921));
#9768=CARTESIAN_POINT('Ctrl Pts',(1.05092079718636,37.0114666380618,-1.70524671613992));
#9769=CARTESIAN_POINT('Ctrl Pts',(1.09887250313603,37.0337451787924,-1.67569471960703));
#9770=CARTESIAN_POINT('Ctrl Pts',(1.14575631855595,37.0562767960668,-1.64400506363559));
#9771=CARTESIAN_POINT('Ctrl Pts',(1.19129904937932,37.0789434783606,-1.61031284532312));
#9772=CARTESIAN_POINT('Ctrl Pts',(1.23740106803564,37.1018885190091,-1.57620686948168));
#9773=CARTESIAN_POINT('Ctrl Pts',(1.2821281195551,37.1249716762293,-1.54004908311832));
#9774=CARTESIAN_POINT('Ctrl Pts',(1.32522270849541,37.1480655437024,-1.50202718276097));
#9775=CARTESIAN_POINT('Ctrl Pts',(1.36778613415348,37.1708747672156,-1.46447392215369));
#9776=CARTESIAN_POINT('Ctrl Pts',(1.40875659070937,37.1936941355092,-1.42510278849638));
#9777=CARTESIAN_POINT('Ctrl Pts',(1.44792023607709,37.2164005075231,-1.38413434132068));
#9778=CARTESIAN_POINT('Ctrl Pts',(1.48781698586827,37.2395319201992,-1.34239900562977));
#9779=CARTESIAN_POINT('Ctrl Pts',(1.52583806569367,37.2625457468023,-1.2990065393806));
#9780=CARTESIAN_POINT('Ctrl Pts',(1.56180167034078,37.2853161302098,-1.25422343598961));
#9781=CARTESIAN_POINT('Ctrl Pts',(1.59776527498789,37.3080865136173,-1.20944033259862));
#9782=CARTESIAN_POINT('Ctrl Pts',(1.6316711330624,37.330613172593,-1.16326733826065));
#9783=CARTESIAN_POINT('Ctrl Pts',(1.66338758908568,37.3527790887222,-1.11599400237662));
#9784=CARTESIAN_POINT('Ctrl Pts',(1.66783346592109,37.3558862118188,-1.10936742881541));
#9785=CARTESIAN_POINT('Ctrl Pts',(1.67223640644948,37.3589862646419,-1.10271926064377));
#9786=CARTESIAN_POINT('Ctrl Pts',(1.67659613043341,37.3620789434069,-1.09605031831598));
#9787=CARTESIAN_POINT('Ctrl Pts',(1.70717378627815,37.3837699649629,-1.04927657206516));
#9788=CARTESIAN_POINT('Ctrl Pts',(1.73595988149344,37.4058246274407,-1.0009622623334));
#9789=CARTESIAN_POINT('Ctrl Pts',(1.76274746581662,37.4281333047434,-0.951326577270847));
#9790=CARTESIAN_POINT('Ctrl Pts',(1.78949886303967,37.4504118454601,-0.901757944596598));
#9791=CARTESIAN_POINT('Ctrl Pts',(1.81425661021869,37.4729434627202,-0.850871989810561));
#9792=CARTESIAN_POINT('Ctrl Pts',(1.83685166290074,37.4956101449996,-0.798922307463975));
#9793=CARTESIAN_POINT('Ctrl Pts',(1.85972419430607,37.5185551856502,-0.746334656632202));
#9794=CARTESIAN_POINT('Ctrl Pts',(1.88038006398015,37.5416383428725,-0.692657569332864));
#9795=CARTESIAN_POINT('Ctrl Pts',(1.89869012259259,37.5647322103477,-0.63818234324847));
#9796=CARTESIAN_POINT('Ctrl Pts',(1.91677450017505,37.5875414338517,-0.584378552760858));
#9797=CARTESIAN_POINT('Ctrl Pts',(1.93257038952445,37.6103608021361,-0.529796922582627));
#9798=CARTESIAN_POINT('Ctrl Pts',(1.9460028777278,37.6330671741409,-0.474735383913968));
#9799=CARTESIAN_POINT('Ctrl Pts',(1.95968680873801,37.6561985868251,-0.418643148056295));
#9800=CARTESIAN_POINT('Ctrl Pts',(1.97091779662797,37.6792124134361,-0.362053630020127));
#9801=CARTESIAN_POINT('Ctrl Pts',(1.9796716401733,37.7019827968515,-0.305288522480569));
#9802=CARTESIAN_POINT('Ctrl Pts',(1.98842548371863,37.7247531802668,-0.248523414941015));
#9803=CARTESIAN_POINT('Ctrl Pts',(1.99470232098237,37.7472798392503,-0.191583499818941));
#9804=CARTESIAN_POINT('Ctrl Pts',(1.99853290967595,37.769445755387,-0.134785361990866));
#9805=CARTESIAN_POINT('Ctrl Pts',(1.99906986517703,37.7725528784843,-0.12682364252758));
#9806=CARTESIAN_POINT('Ctrl Pts',(1.99955883944025,37.7756529313079,-0.118864689736665));
#9807=CARTESIAN_POINT('Ctrl Pts',(2.00000000000001,37.7787456100735,-0.110909354270941));
#9808=CARTESIAN_POINT('Ctrl Pts',(2.00309415362695,37.8004366316478,-0.0551132738181009));
#9809=CARTESIAN_POINT('Ctrl Pts',(2.00386648849195,37.8224912941446,0.00112119343143236));
#9810=CARTESIAN_POINT('Ctrl Pts',(2.00224737448518,37.8447999714666,0.0575007498392763));
#9811=CARTESIAN_POINT('Ctrl Pts',(2.00063044772644,37.8670785121765,0.113804143559674));
#9812=CARTESIAN_POINT('Ctrl Pts',(1.99662830832893,37.8896101294297,0.170251546671467));
#9813=CARTESIAN_POINT('Ctrl Pts',(1.9902213567777,37.9122768117019,0.226538817624831));
#9814=CARTESIAN_POINT('Ctrl Pts',(1.98373572460605,37.9352218523494,0.283517324865039));
#9815=CARTESIAN_POINT('Ctrl Pts',(1.97478568883041,37.9583050095686,0.340330980896365));
#9816=CARTESIAN_POINT('Ctrl Pts',(1.96340505169111,37.9813988770406,0.396662939860387));
#9817=CARTESIAN_POINT('Ctrl Pts',(1.95216468684383,38.004208100544,0.452300578031931));
#9818=CARTESIAN_POINT('Ctrl Pts',(1.93855351320529,38.0270274688278,0.507467601019013));
#9819=CARTESIAN_POINT('Ctrl Pts',(1.9226556198899,38.0497338408319,0.561868536377183));
#9820=CARTESIAN_POINT('Ctrl Pts',(1.90646013384102,38.0728652535115,0.617287803078779));
#9821=CARTESIAN_POINT('Ctrl Pts',(1.8878916956477,38.0958790801179,0.671911257219888));
#9822=CARTESIAN_POINT('Ctrl Pts',(1.86709019277227,38.1186494635288,0.725448204159634));
#9823=CARTESIAN_POINT('Ctrl Pts',(1.84628868989685,38.1414198469397,0.778985151099376));
#9824=CARTESIAN_POINT('Ctrl Pts',(1.82325463286587,38.1639465059187,0.831434982705915));
#9825=CARTESIAN_POINT('Ctrl Pts',(1.79817295107695,38.1861124220511,0.882538907289653));
#9826=CARTESIAN_POINT('Ctrl Pts',(1.79465710844899,38.1892195451493,0.889702436355193));
#9827=CARTESIAN_POINT('Ctrl Pts',(1.7911010961863,38.1923195979738,0.896839578793259));
#9828=CARTESIAN_POINT('Ctrl Pts',(1.78750548470435,38.1954122767402,0.903949681684035));
#9829=CARTESIAN_POINT('Ctrl Pts',(1.76228706013013,38.2171032983075,0.953817581585345));
#9830=CARTESIAN_POINT('Ctrl Pts',(1.7348386881282,38.2391579607971,1.00290422620872));
#9831=CARTESIAN_POINT('Ctrl Pts',(1.70524671607363,38.2614666381118,1.05092079729395));
#9832=CARTESIAN_POINT('Ctrl Pts',(1.67569471955799,38.2837451788273,1.09887250320886));
#9833=CARTESIAN_POINT('Ctrl Pts',(1.64400506360691,38.3062767960863,1.14575631859525));
#9834=CARTESIAN_POINT('Ctrl Pts',(1.61031284531752,38.3289434783644,1.19129904938695));
#9835=CARTESIAN_POINT('Ctrl Pts',(1.57620686947642,38.3518885190125,1.23740106804235));
#9836=CARTESIAN_POINT('Ctrl Pts',(1.54004908311345,38.3749716762323,1.28212811956094));
#9837=CARTESIAN_POINT('Ctrl Pts',(1.50202718275659,38.3980655437051,1.3252227085004));
#9838=CARTESIAN_POINT('Ctrl Pts',(1.46447392215405,38.4208747672153,1.36778613415282));
#9839=CARTESIAN_POINT('Ctrl Pts',(1.42510278850193,38.443694135506,1.40875659070347));
#9840=CARTESIAN_POINT('Ctrl Pts',(1.38413434133184,38.4664005075169,1.44792023606643));
#9841=CARTESIAN_POINT('Ctrl Pts',(1.3423990056396,38.4895319201939,1.48781698585948));
#9842=CARTESIAN_POINT('Ctrl Pts',(1.29900653938895,38.5125457467979,1.52583806568664));
#9843=CARTESIAN_POINT('Ctrl Pts',(1.25422343599634,38.5353161302063,1.56180167033536));
#9844=CARTESIAN_POINT('Ctrl Pts',(1.20944033260373,38.5580865136147,1.59776527498408));
#9845=CARTESIAN_POINT('Ctrl Pts',(1.16326733826403,38.5806131725914,1.63167113306004));
#9846=CARTESIAN_POINT('Ctrl Pts',(1.11599400237818,38.6027790887214,1.6633875890846));
#9847=CARTESIAN_POINT('Ctrl Pts',(1.10936742881645,38.6058862118183,1.66783346592037));
#9848=CARTESIAN_POINT('Ctrl Pts',(1.10271926064427,38.6089862646417,1.67223640644913));
#9849=CARTESIAN_POINT('Ctrl Pts',(1.09605031831595,38.6120789434069,1.6765961304334));
#9850=CARTESIAN_POINT('Ctrl Pts',(1.0492765720158,38.6337699649858,1.70717378631043));
#9851=CARTESIAN_POINT('Ctrl Pts',(1.00096226223136,38.6558246274873,1.73595988155423));
#9852=CARTESIAN_POINT('Ctrl Pts',(0.951326577113638,38.6781333048141,1.76274746590148));
#9853=CARTESIAN_POINT('Ctrl Pts',(0.901757944475194,38.700411845514,1.7894988630995));
#9854=CARTESIAN_POINT('Ctrl Pts',(0.850871989727273,38.7229434627568,1.8142566102564));
#9855=CARTESIAN_POINT('Ctrl Pts',(0.798922307420521,38.7456101450186,1.83685166291966));
#9856=CARTESIAN_POINT('Ctrl Pts',(0.746334656591805,38.7685551856676,1.85972419432218));
#9857=CARTESIAN_POINT('Ctrl Pts',(0.692657569295748,38.7916383428884,1.88038006399372));
#9858=CARTESIAN_POINT('Ctrl Pts',(0.638182343214835,38.814732210362,1.89869012260392));
#9859=CARTESIAN_POINT('Ctrl Pts',(0.584378552717411,38.83754143387,1.9167745001886));
#9860=CARTESIAN_POINT('Ctrl Pts',(0.529796922529156,38.8603608021585,1.93257038953941));
#9861=CARTESIAN_POINT('Ctrl Pts',(0.474735383850398,38.8830671741672,1.94600287774331));
#9862=CARTESIAN_POINT('Ctrl Pts',(0.41864314800303,38.9061985868468,1.95968680874905));
#9863=CARTESIAN_POINT('Ctrl Pts',(0.362053629977474,38.9292124134533,1.97091779663548));
#9864=CARTESIAN_POINT('Ctrl Pts',(0.305288522448675,38.9519827968643,1.97967164017821));
#9865=CARTESIAN_POINT('Ctrl Pts',(0.248523414919876,38.9747531802752,1.98842548372094));
#9866=CARTESIAN_POINT('Ctrl Pts',(0.191583499808698,38.9972798392543,1.99470232098303));
#9867=CARTESIAN_POINT('Ctrl Pts',(0.1347853619914,39.0194457553868,1.9985329096759));
#9868=CARTESIAN_POINT('Ctrl Pts',(0.126823642527947,39.0225528784841,1.99906986517699));
#9869=CARTESIAN_POINT('Ctrl Pts',(0.118864689736811,39.0256529313079,1.99955883944023));
#9870=CARTESIAN_POINT('Ctrl Pts',(0.110909354270921,39.0287456100735,2.));
#9871=CARTESIAN_POINT('Ctrl Pts',(0.0551132738216044,39.0504366316464,2.00309415362675));
#9872=CARTESIAN_POINT('Ctrl Pts',(-0.00112119342432845,39.0724912941418,
2.00386648849185));
#9873=CARTESIAN_POINT('Ctrl Pts',(-0.0575007498285725,39.0947999714623,
2.00224737448548));
#9874=CARTESIAN_POINT('Ctrl Pts',(-0.113804143544574,39.1170785121705,2.00063044772717));
#9875=CARTESIAN_POINT('Ctrl Pts',(-0.170251546651944,39.1396101294219,1.99662830833046));
#9876=CARTESIAN_POINT('Ctrl Pts',(-0.226538817601016,39.1622768116923,1.9902213567804));
#9877=CARTESIAN_POINT('Ctrl Pts',(-0.283517324843828,39.1852218523408,1.98373572460914));
#9878=CARTESIAN_POINT('Ctrl Pts',(-0.340330980877668,39.2083050095609,1.97478568883371));
#9879=CARTESIAN_POINT('Ctrl Pts',(-0.396662939844236,39.231398877034,1.96340505169437));
#9880=CARTESIAN_POINT('Ctrl Pts',(-0.452300578025572,39.2542081005414,1.95216468684558));
#9881=CARTESIAN_POINT('Ctrl Pts',(-0.507467601022369,39.2770274688292,1.93855351320469));
#9882=CARTESIAN_POINT('Ctrl Pts',(-0.561868536389967,39.2997338408373,1.92265561988615));
#9883=CARTESIAN_POINT('Ctrl Pts',(-0.617287803090361,39.3228652535163,1.90646013383722));
#9884=CARTESIAN_POINT('Ctrl Pts',(-0.671911257230311,39.3458790801223,1.88789169564393));
#9885=CARTESIAN_POINT('Ctrl Pts',(-0.725448204168872,39.3686494635327,1.86709019276865));
#9886=CARTESIAN_POINT('Ctrl Pts',(-0.778985151107431,39.3914198469431,1.84628868989338));
#9887=CARTESIAN_POINT('Ctrl Pts',(-0.831434982712827,39.4139465059217,1.82325463286265));
#9888=CARTESIAN_POINT('Ctrl Pts',(-0.882538907295425,39.4361124220536,1.79817295107409));
#9889=CARTESIAN_POINT('Ctrl Pts',(-0.889702436359024,39.4392195451509,1.79465710844706));
#9890=CARTESIAN_POINT('Ctrl Pts',(-0.896839578795191,39.4423195979746,1.7911010961853));
#9891=CARTESIAN_POINT('Ctrl Pts',(-0.903949681684063,39.4454122767402,1.78750548470431));
#9892=CARTESIAN_POINT('Ctrl Pts',(-0.953817581594742,39.4671032983116,1.76228706012535));
#9893=CARTESIAN_POINT('Ctrl Pts',(-1.00290422622729,39.4891579608055,1.73483868811778));
#9894=CARTESIAN_POINT('Ctrl Pts',(-1.0509207973212,39.5114666381245,1.7052467160568));
#9895=CARTESIAN_POINT('Ctrl Pts',(-1.09887250321436,39.5337451788302,1.67569471955352));
#9896=CARTESIAN_POINT('Ctrl Pts',(-1.14575631857987,39.5562767960791,1.64400506361672));
#9897=CARTESIAN_POINT('Ctrl Pts',(-1.191299049352,39.578943478347,1.61031284534333));
#9898=CARTESIAN_POINT('Ctrl Pts',(-1.23740106801089,39.6018885189965,1.5762068695012));
#9899=CARTESIAN_POINT('Ctrl Pts',(-1.28212811953282,39.6249716762176,1.54004908313695));
#9900=CARTESIAN_POINT('Ctrl Pts',(-1.32522270847548,39.6480655436917,1.50202718277854));
#9901=CARTESIAN_POINT('Ctrl Pts',(-1.36778613413884,39.6708747672075,1.4644739221676));
#9902=CARTESIAN_POINT('Ctrl Pts',(-1.40875659069979,39.6936941355038,1.42510278850608));
#9903=CARTESIAN_POINT('Ctrl Pts',(-1.44792023607208,39.7164005075202,1.38413434132589));
#9904=CARTESIAN_POINT('Ctrl Pts',(-1.48781698586376,39.7395319201965,1.34239900563475));
#9905=CARTESIAN_POINT('Ctrl Pts',(-1.52583806568971,39.7625457467998,1.29900653938524));
#9906=CARTESIAN_POINT('Ctrl Pts',(-1.56180167033728,39.7853161302076,1.25422343599392));
#9907=CARTESIAN_POINT('Ctrl Pts',(-1.59776527498484,39.8080865136153,1.2094403326026));
#9908=CARTESIAN_POINT('Ctrl Pts',(-1.63167113305979,39.8306131725912,1.16326733826427));
#9909=CARTESIAN_POINT('Ctrl Pts',(-1.66338758908347,39.8527790887206,1.11599400237985));
#9910=CARTESIAN_POINT('Ctrl Pts',(-1.66783346591964,39.8558862118178,1.10936742881753));
#9911=CARTESIAN_POINT('Ctrl Pts',(-1.67223640644877,39.8589862646414,1.10271926064481));
#9912=CARTESIAN_POINT('Ctrl Pts',(-1.67659613043342,39.8620789434069,1.09605031831591));
#9913=CARTESIAN_POINT('Ctrl Pts',(-1.70717378631508,39.883769964989,1.04927657200867));
#9914=CARTESIAN_POINT('Ctrl Pts',(-1.73595988156297,39.905824627494,1.00096226221665));
#9915=CARTESIAN_POINT('Ctrl Pts',(-1.76274746591369,39.9281333048242,0.951326577090993));
#9916=CARTESIAN_POINT('Ctrl Pts',(-1.78949886311837,39.9504118455302,0.901757944438676));
#9917=CARTESIAN_POINT('Ctrl Pts',(-1.81425661028082,39.9729434627793,0.850871989676198));
#9918=CARTESIAN_POINT('Ctrl Pts',(-1.8368516629484,39.9956101450475,0.798922307354412));
#9919=CARTESIAN_POINT('Ctrl Pts',(-1.85972419434675,40.0185551856943,0.746334656530118));
#9920=CARTESIAN_POINT('Ctrl Pts',(-1.88038006401451,40.0416383429127,0.69265756923881));
#9921=CARTESIAN_POINT('Ctrl Pts',(-1.89869012262136,40.064732210384,0.638182343162886));
#9922=CARTESIAN_POINT('Ctrl Pts',(-1.91677450020403,40.0875414338913,0.58437855266658));
#9923=CARTESIAN_POINT('Ctrl Pts',(-1.93257038955292,40.1103608021791,0.529796922479594));
#9924=CARTESIAN_POINT('Ctrl Pts',(-1.94600287775504,40.133067174187,0.474735383802248));
#9925=CARTESIAN_POINT('Ctrl Pts',(-1.95968680875752,40.1561985868634,0.418643147962249));
#9926=CARTESIAN_POINT('Ctrl Pts',(-1.97091779664134,40.1792124134667,0.362053629944233));
#9927=CARTESIAN_POINT('Ctrl Pts',(-1.97967164018214,40.2019827968745,0.305288522423077));
#9928=CARTESIAN_POINT('Ctrl Pts',(-1.98842548372294,40.2247531802823,0.248523414901921));
#9929=CARTESIAN_POINT('Ctrl Pts',(-1.99470232098377,40.2472798392583,0.191583499798515));
#9930=CARTESIAN_POINT('Ctrl Pts',(-1.99853290967604,40.2694457553877,0.134785361988986));
#9931=CARTESIAN_POINT('Ctrl Pts',(-1.99906986517707,40.2725528784847,0.126823642526306));
#9932=CARTESIAN_POINT('Ctrl Pts',(-1.99955883944026,40.2756529313082,0.118864689735964));
#9933=CARTESIAN_POINT('Ctrl Pts',(-1.99999999999998,40.2787456100735,0.110909354270834));
#9934=CARTESIAN_POINT('Origin',(-2.00026128978551,0.00614793747541198,0.00052367985300868));
#9935=CARTESIAN_POINT('Origin',(-2.,39.7212543899267,-0.110909354270917));
#9936=CARTESIAN_POINT('Origin',(-1.99999999999999,40.0000000000001,-7.63278329429795E-14));
#9937=CARTESIAN_POINT('',(-1.74999999999999,39.9999999999897,-4.17027523624824E-12));
#9938=CARTESIAN_POINT('',(-1.99999999998663,40.0000000000001,-7.63278329429795E-14));
#9939=CARTESIAN_POINT('Origin',(-2.00046279962269,40.0004045588857,0.000160968866383087));
#9940=CARTESIAN_POINT('Origin',(-2.,-0.27874561007344,-0.110909354270924));
#9941=CARTESIAN_POINT('',(-2.28755052096797,0.0795884994942361,0.0313009478093308));
#9942=CARTESIAN_POINT('',(-1.91825489052517,-0.0225146681393854,-0.00895830181614488));
#9943=CARTESIAN_POINT('Origin',(-2.,-2.08166817117217E-14,-3.46944695195361E-14));
#9944=CARTESIAN_POINT('Ctrl Pts',(-2.,0.278745610073468,0.110909354270813));
#9945=CARTESIAN_POINT('Ctrl Pts',(-2.02971807190995,0.487078943406699,-0.424989030591362));
#9946=CARTESIAN_POINT('Ctrl Pts',(-1.78750548470433,0.695412276740089,-0.90394968168412));
#9947=CARTESIAN_POINT('Ctrl Pts',(-1.54529289749872,0.903745610073333,-1.3829103327768));
#9948=CARTESIAN_POINT('Ctrl Pts',(-1.09605031831593,1.11207894340676,-1.67659613043348));
#9949=CARTESIAN_POINT('Ctrl Pts',(-0.646807739133152,1.32041227674011,-1.97028192809006));
#9950=CARTESIAN_POINT('Ctrl Pts',(-0.110909354270893,1.52874561007344,-2.00000000000001));
#9951=CARTESIAN_POINT('Ctrl Pts',(0.42498903059134,1.7370789434067,-2.02971807190998));
#9952=CARTESIAN_POINT('Ctrl Pts',(0.903949681684066,1.94541227674011,-1.78750548470433));
#9953=CARTESIAN_POINT('Ctrl Pts',(1.38291033277679,2.15374561007344,-1.54529289749872));
#9954=CARTESIAN_POINT('Ctrl Pts',(1.67659613043343,2.36207894340677,-1.09605031831594));
#9955=CARTESIAN_POINT('Ctrl Pts',(1.97028192809005,2.57041227674009,-0.646807739133166));
#9956=CARTESIAN_POINT('Ctrl Pts',(2.00000000000003,2.77874561007344,-0.110909354270911));
#9957=CARTESIAN_POINT('Ctrl Pts',(2.02971807190995,2.98707894340676,0.424989030591319));
#9958=CARTESIAN_POINT('Ctrl Pts',(1.78750548470433,3.1954122767401,0.903949681684016));
#9959=CARTESIAN_POINT('Ctrl Pts',(1.54529289749872,3.40374561007338,1.38291033277678));
#9960=CARTESIAN_POINT('Ctrl Pts',(1.09605031831593,3.61207894340677,1.67659613043342));
#9961=CARTESIAN_POINT('Ctrl Pts',(0.646807739133154,3.82041227674006,1.97028192809004));
#9962=CARTESIAN_POINT('Ctrl Pts',(0.110909354270907,4.02874561007344,1.99999999999995));
#9963=CARTESIAN_POINT('Ctrl Pts',(-0.424989030591324,4.23707894340672,2.02971807190993));
#9964=CARTESIAN_POINT('Ctrl Pts',(-0.903949681684066,4.44541227674011,1.78750548470433));
#9965=CARTESIAN_POINT('Ctrl Pts',(-1.38291033277679,4.65374561007344,1.54529289749866));
#9966=CARTESIAN_POINT('Ctrl Pts',(-1.67659613043344,4.8620789434068,1.09605031831587));
#9967=CARTESIAN_POINT('Ctrl Pts',(-1.97028192809005,5.07041227674005,0.646807739133138));
#9968=CARTESIAN_POINT('Ctrl Pts',(-2.,5.27874561007342,0.110909354270813));
#9969=CARTESIAN_POINT('Ctrl Pts',(-2.02971807190995,5.48707894340671,-0.424989030591405));
#9970=CARTESIAN_POINT('Ctrl Pts',(-1.78750548470433,5.6954122767401,-0.90394968168412));
#9971=CARTESIAN_POINT('Ctrl Pts',(-1.54529289749872,5.90374561007338,-1.38291033277678));
#9972=CARTESIAN_POINT('Ctrl Pts',(-1.09605031831592,6.11207894340678,-1.67659613043342));
#9973=CARTESIAN_POINT('Ctrl Pts',(-0.646807739133139,6.3204122767401,-1.97028192809006));
#9974=CARTESIAN_POINT('Ctrl Pts',(-0.110909354270905,6.52874561007347,-2.00000000000006));
#9975=CARTESIAN_POINT('Ctrl Pts',(0.424989030591338,6.73707894340672,-2.02971807190996));
#9976=CARTESIAN_POINT('Ctrl Pts',(0.903949681684068,6.94541227674014,-1.78750548470433));
#9977=CARTESIAN_POINT('Ctrl Pts',(1.38291033277681,7.15374561007342,-1.54529289749877));
#9978=CARTESIAN_POINT('Ctrl Pts',(1.6765961304334,7.36207894340677,-1.09605031831599));
#9979=CARTESIAN_POINT('Ctrl Pts',(1.97028192809006,7.57041227674011,-0.646807739133152));
#9980=CARTESIAN_POINT('Ctrl Pts',(2.,7.77874561007349,-0.110909354270917));
#9981=CARTESIAN_POINT('Ctrl Pts',(2.02971807190995,7.98707894340672,0.424989030591319));
#9982=CARTESIAN_POINT('Ctrl Pts',(1.78750548470433,8.19541227674012,0.903949681684058));
#9983=CARTESIAN_POINT('Ctrl Pts',(1.54529289749873,8.40374561007341,1.3829103327768));
#9984=CARTESIAN_POINT('Ctrl Pts',(1.09605031831593,8.6120789434068,1.67659613043337));
#9985=CARTESIAN_POINT('Ctrl Pts',(0.646807739133154,8.82041227674011,1.97028192809005));
#9986=CARTESIAN_POINT('Ctrl Pts',(0.110909354270904,9.02874561007346,1.99999999999994));
#9987=CARTESIAN_POINT('Ctrl Pts',(-0.424989030591337,9.23707894340678,2.02971807190995));
#9988=CARTESIAN_POINT('Ctrl Pts',(-0.903949681684064,9.44541227674011,1.78750548470427));
#9989=CARTESIAN_POINT('Ctrl Pts',(-1.38291033277679,9.65374561007344,1.54529289749871));
#9990=CARTESIAN_POINT('Ctrl Pts',(-1.67659613043342,9.86207894340678,1.09605031831593));
#9991=CARTESIAN_POINT('Ctrl Pts',(-1.97028192809005,10.0704122767401,0.646807739133152));
#9992=CARTESIAN_POINT('Ctrl Pts',(-1.99999999999999,10.2787456100735,0.110909354270841));
#9993=CARTESIAN_POINT('Ctrl Pts',(-2.02971807190994,10.4870789434068,-0.42498903059134));
#9994=CARTESIAN_POINT('Ctrl Pts',(-1.78750548470433,10.6954122767401,-0.903949681684169));
#9995=CARTESIAN_POINT('Ctrl Pts',(-1.54529289749871,10.9037456100734,-1.38291033277681));
#9996=CARTESIAN_POINT('Ctrl Pts',(-1.09605031831593,11.1120789434068,-1.67659613043348));
#9997=CARTESIAN_POINT('Ctrl Pts',(-0.646807739133152,11.3204122767401,-1.97028192809006));
#9998=CARTESIAN_POINT('Ctrl Pts',(-0.110909354270907,11.5287456100735,-2.00000000000002));
#9999=CARTESIAN_POINT('Ctrl Pts',(0.424989030591338,11.7370789434068,-2.02971807190997));
#10000=CARTESIAN_POINT('Ctrl Pts',(0.903949681684066,11.9454122767401,-1.78750548470433));
#10001=CARTESIAN_POINT('Ctrl Pts',(1.3829103327768,12.1537456100734,-1.54529289749877));
#10002=CARTESIAN_POINT('Ctrl Pts',(1.67659613043342,12.3620789434068,-1.09605031831594));
#10003=CARTESIAN_POINT('Ctrl Pts',(1.97028192809008,12.5704122767401,-0.646807739133166));
#10004=CARTESIAN_POINT('Ctrl Pts',(2.,12.7787456100735,-0.110909354270959));
#10005=CARTESIAN_POINT('Ctrl Pts',(2.02971807190995,12.9870789434068,0.42498903059134));
#10006=CARTESIAN_POINT('Ctrl Pts',(1.78750548470433,13.1954122767401,0.903949681684009));
#10007=CARTESIAN_POINT('Ctrl Pts',(1.54529289749872,13.4037456100734,1.38291033277679));
#10008=CARTESIAN_POINT('Ctrl Pts',(1.09605031831593,13.6120789434068,1.67659613043342));
#10009=CARTESIAN_POINT('Ctrl Pts',(0.646807739133154,13.8204122767401,1.97028192809006));
#10010=CARTESIAN_POINT('Ctrl Pts',(0.110909354270907,14.0287456100735,1.99999999999997));
#10011=CARTESIAN_POINT('Ctrl Pts',(-0.424989030591338,14.2370789434068,
2.02971807190995));
#10012=CARTESIAN_POINT('Ctrl Pts',(-0.903949681684066,14.4454122767402,
1.78750548470424));
#10013=CARTESIAN_POINT('Ctrl Pts',(-1.38291033277679,14.6537456100734,1.54529289749866));
#10014=CARTESIAN_POINT('Ctrl Pts',(-1.67659613043342,14.8620789434068,1.09605031831587));
#10015=CARTESIAN_POINT('Ctrl Pts',(-1.97028192809004,15.0704122767401,0.646807739133166));
#10016=CARTESIAN_POINT('Ctrl Pts',(-2.,15.2787456100735,0.110909354270848));
#10017=CARTESIAN_POINT('Ctrl Pts',(-2.02971807190995,15.4870789434068,-0.424989030591448));
#10018=CARTESIAN_POINT('Ctrl Pts',(-1.78750548470433,15.6954122767401,-0.903949681684079));
#10019=CARTESIAN_POINT('Ctrl Pts',(-1.54529289749872,15.9037456100734,-1.3829103327768));
#10020=CARTESIAN_POINT('Ctrl Pts',(-1.09605031831592,16.1120789434068,-1.67659613043346));
#10021=CARTESIAN_POINT('Ctrl Pts',(-0.646807739133152,16.3204122767401,
-1.97028192809011));
#10022=CARTESIAN_POINT('Ctrl Pts',(-0.110909354270907,16.5287456100735,
-2.00000000000005));
#10023=CARTESIAN_POINT('Ctrl Pts',(0.42498903059134,16.7370789434068,-2.02971807190995));
#10024=CARTESIAN_POINT('Ctrl Pts',(0.90394968168408,16.9454122767401,-1.78750548470433));
#10025=CARTESIAN_POINT('Ctrl Pts',(1.38291033277679,17.1537456100734,-1.54529289749872));
#10026=CARTESIAN_POINT('Ctrl Pts',(1.67659613043342,17.3620789434068,-1.09605031831599));
#10027=CARTESIAN_POINT('Ctrl Pts',(1.97028192809005,17.5704122767401,-0.646807739133152));
#10028=CARTESIAN_POINT('Ctrl Pts',(2.,17.7787456100735,-0.110909354270917));
#10029=CARTESIAN_POINT('Ctrl Pts',(2.02971807190995,17.9870789434068,0.424989030591283));
#10030=CARTESIAN_POINT('Ctrl Pts',(1.78750548470433,18.1954122767401,0.903949681684051));
#10031=CARTESIAN_POINT('Ctrl Pts',(1.54529289749873,18.4037456100734,1.3829103327768));
#10032=CARTESIAN_POINT('Ctrl Pts',(1.09605031831593,18.6120789434068,1.67659613043337));
#10033=CARTESIAN_POINT('Ctrl Pts',(0.646807739133154,18.8204122767401,1.97028192809005));
#10034=CARTESIAN_POINT('Ctrl Pts',(0.110909354270905,19.0287456100735,1.99999999999995));
#10035=CARTESIAN_POINT('Ctrl Pts',(-0.424989030591338,19.2370789434068,
2.02971807190995));
#10036=CARTESIAN_POINT('Ctrl Pts',(-0.903949681684064,19.4454122767402,
1.78750548470426));
#10037=CARTESIAN_POINT('Ctrl Pts',(-1.38291033277679,19.6537456100734,1.54529289749871));
#10038=CARTESIAN_POINT('Ctrl Pts',(-1.67659613043342,19.8620789434068,1.0960503183159));
#10039=CARTESIAN_POINT('Ctrl Pts',(-1.97028192809006,20.0704122767401,0.646807739133152));
#10040=CARTESIAN_POINT('Ctrl Pts',(-1.99999999999999,20.2787456100735,0.11090935427082));
#10041=CARTESIAN_POINT('Ctrl Pts',(-2.02971807190993,20.4870789434068,-0.424989030591398));
#10042=CARTESIAN_POINT('Ctrl Pts',(-1.78750548470433,20.6954122767402,-0.903949681684127));
#10043=CARTESIAN_POINT('Ctrl Pts',(-1.5452928974987,20.9037456100735,-1.38291033277683));
#10044=CARTESIAN_POINT('Ctrl Pts',(-1.09605031831595,21.1120789434068,-1.67659613043348));
#10045=CARTESIAN_POINT('Ctrl Pts',(-0.646807739133154,21.3204122767401,
-1.97028192809006));
#10046=CARTESIAN_POINT('Ctrl Pts',(-0.110909354270907,21.5287456100735,
-2.));
#10047=CARTESIAN_POINT('Ctrl Pts',(0.424989030591338,21.7370789434068,-2.02971807190994));
#10048=CARTESIAN_POINT('Ctrl Pts',(0.903949681684066,21.9454122767402,-1.78750548470436));
#10049=CARTESIAN_POINT('Ctrl Pts',(1.38291033277679,22.1537456100734,-1.54529289749877));
#10050=CARTESIAN_POINT('Ctrl Pts',(1.67659613043343,22.3620789434069,-1.09605031831595));
#10051=CARTESIAN_POINT('Ctrl Pts',(1.97028192809003,22.5704122767401,-0.646807739133152));
#10052=CARTESIAN_POINT('Ctrl Pts',(2.,22.7787456100735,-0.110909354270945));
#10053=CARTESIAN_POINT('Ctrl Pts',(2.02971807190997,22.9870789434068,0.42498903059134));
#10054=CARTESIAN_POINT('Ctrl Pts',(1.78750548470433,23.1954122767402,0.903949681684009));
#10055=CARTESIAN_POINT('Ctrl Pts',(1.54529289749872,23.4037456100734,1.38291033277679));
#10056=CARTESIAN_POINT('Ctrl Pts',(1.09605031831593,23.6120789434068,1.6765961304334));
#10057=CARTESIAN_POINT('Ctrl Pts',(0.646807739133168,23.8204122767401,1.97028192809006));
#10058=CARTESIAN_POINT('Ctrl Pts',(0.110909354270907,24.0287456100735,1.99999999999992));
#10059=CARTESIAN_POINT('Ctrl Pts',(-0.424989030591338,24.2370789434068,
2.02971807190996));
#10060=CARTESIAN_POINT('Ctrl Pts',(-0.903949681684066,24.4454122767402,
1.78750548470424));
#10061=CARTESIAN_POINT('Ctrl Pts',(-1.38291033277678,24.6537456100735,1.54529289749864));
#10062=CARTESIAN_POINT('Ctrl Pts',(-1.67659613043341,24.8620789434068,1.09605031831588));
#10063=CARTESIAN_POINT('Ctrl Pts',(-1.97028192809005,25.0704122767401,0.646807739133166));
#10064=CARTESIAN_POINT('Ctrl Pts',(-2.,25.2787456100735,0.110909354270855));
#10065=CARTESIAN_POINT('Ctrl Pts',(-2.02971807190995,25.4870789434068,-0.424989030591369));
#10066=CARTESIAN_POINT('Ctrl Pts',(-1.78750548470433,25.6954122767401,-0.903949681684079));
#10067=CARTESIAN_POINT('Ctrl Pts',(-1.54529289749871,25.9037456100735,-1.3829103327768));
#10068=CARTESIAN_POINT('Ctrl Pts',(-1.09605031831593,26.1120789434068,-1.67659613043345));
#10069=CARTESIAN_POINT('Ctrl Pts',(-0.646807739133152,26.3204122767401,
-1.97028192809011));
#10070=CARTESIAN_POINT('Ctrl Pts',(-0.110909354270907,26.5287456100735,
-2.00000000000004));
#10071=CARTESIAN_POINT('Ctrl Pts',(0.424989030591353,26.7370789434068,-2.02971807190995));
#10072=CARTESIAN_POINT('Ctrl Pts',(0.90394968168408,26.9454122767402,-1.78750548470438));
#10073=CARTESIAN_POINT('Ctrl Pts',(1.38291033277679,27.1537456100734,-1.54529289749872));
#10074=CARTESIAN_POINT('Ctrl Pts',(1.6765961304334,27.3620789434068,-1.09605031831597));
#10075=CARTESIAN_POINT('Ctrl Pts',(1.97028192809005,27.5704122767401,-0.64680773913318));
#10076=CARTESIAN_POINT('Ctrl Pts',(1.99999999999997,27.7787456100735,-0.110909354270911));
#10077=CARTESIAN_POINT('Ctrl Pts',(2.02971807190995,27.9870789434068,0.424989030591333));
#10078=CARTESIAN_POINT('Ctrl Pts',(1.78750548470433,28.1954122767402,0.903949681684037));
#10079=CARTESIAN_POINT('Ctrl Pts',(1.5452928974987,28.4037456100735,1.38291033277679));
#10080=CARTESIAN_POINT('Ctrl Pts',(1.09605031831593,28.6120789434068,1.67659613043337));
#10081=CARTESIAN_POINT('Ctrl Pts',(0.646807739133154,28.8204122767401,1.97028192809002));
#10082=CARTESIAN_POINT('Ctrl Pts',(0.110909354270921,29.0287456100735,1.99999999999997));
#10083=CARTESIAN_POINT('Ctrl Pts',(-0.424989030591338,29.2370789434068,
2.02971807190995));
#10084=CARTESIAN_POINT('Ctrl Pts',(-0.903949681684064,29.4454122767402,
1.78750548470427));
#10085=CARTESIAN_POINT('Ctrl Pts',(-1.38291033277679,29.6537456100735,1.54529289749868));
#10086=CARTESIAN_POINT('Ctrl Pts',(-1.67659613043342,29.8620789434068,1.09605031831586));
#10087=CARTESIAN_POINT('Ctrl Pts',(-1.97028192809005,30.0704122767401,0.646807739133123));
#10088=CARTESIAN_POINT('Ctrl Pts',(-2.,30.2787456100735,0.110909354270834));
#10089=CARTESIAN_POINT('Ctrl Pts',(-2.02971807190995,30.4870789434068,-0.424989030591398));
#10090=CARTESIAN_POINT('Ctrl Pts',(-1.78750548470432,30.6954122767402,-0.903949681684113));
#10091=CARTESIAN_POINT('Ctrl Pts',(-1.54529289749872,30.9037456100735,-1.38291033277676));
#10092=CARTESIAN_POINT('Ctrl Pts',(-1.09605031831593,31.1120789434068,-1.67659613043348));
#10093=CARTESIAN_POINT('Ctrl Pts',(-0.646807739133152,31.3204122767401,
-1.97028192809006));
#10094=CARTESIAN_POINT('Ctrl Pts',(-0.110909354270905,31.5287456100735,
-2.));
#10095=CARTESIAN_POINT('Ctrl Pts',(0.42498903059134,31.7370789434068,-2.02971807190996));
#10096=CARTESIAN_POINT('Ctrl Pts',(0.903949681684054,31.9454122767402,-1.78750548470435));
#10097=CARTESIAN_POINT('Ctrl Pts',(1.38291033277679,32.1537456100735,-1.54529289749877));
#10098=CARTESIAN_POINT('Ctrl Pts',(1.67659613043342,32.3620789434069,-1.09605031831598));
#10099=CARTESIAN_POINT('Ctrl Pts',(1.97028192809005,32.5704122767401,-0.646807739133152));
#10100=CARTESIAN_POINT('Ctrl Pts',(2.,32.7787456100735,-0.110909354270917));
#10101=CARTESIAN_POINT('Ctrl Pts',(2.02971807190995,32.9870789434069,0.424989030591311));
#10102=CARTESIAN_POINT('Ctrl Pts',(1.78750548470433,33.1954122767402,0.903949681684009));
#10103=CARTESIAN_POINT('Ctrl Pts',(1.54529289749872,33.4037456100734,1.38291033277681));
#10104=CARTESIAN_POINT('Ctrl Pts',(1.09605031831593,33.6120789434068,1.67659613043341));
#10105=CARTESIAN_POINT('Ctrl Pts',(0.646807739133154,33.8204122767401,1.97028192809006));
#10106=CARTESIAN_POINT('Ctrl Pts',(0.110909354270907,34.0287456100735,1.99999999999993));
#10107=CARTESIAN_POINT('Ctrl Pts',(-0.424989030591338,34.2370789434068,
2.02971807190994));
#10108=CARTESIAN_POINT('Ctrl Pts',(-0.903949681684066,34.4454122767402,
1.78750548470426));
#10109=CARTESIAN_POINT('Ctrl Pts',(-1.38291033277681,34.6537456100735,1.54529289749869));
#10110=CARTESIAN_POINT('Ctrl Pts',(-1.67659613043341,34.8620789434068,1.0960503183159));
#10111=CARTESIAN_POINT('Ctrl Pts',(-1.97028192809005,35.0704122767402,0.646807739133166));
#10112=CARTESIAN_POINT('Ctrl Pts',(-2.,35.2787456100736,0.110909354270855));
#10113=CARTESIAN_POINT('Ctrl Pts',(-2.02971807190995,35.4870789434068,-0.424989030591383));
#10114=CARTESIAN_POINT('Ctrl Pts',(-1.78750548470433,35.6954122767402,-0.903949681684099));
#10115=CARTESIAN_POINT('Ctrl Pts',(-1.54529289749872,35.9037456100735,-1.38291033277681));
#10116=CARTESIAN_POINT('Ctrl Pts',(-1.09605031831593,36.1120789434069,-1.67659613043344));
#10117=CARTESIAN_POINT('Ctrl Pts',(-0.646807739133139,36.3204122767402,
-1.97028192809006));
#10118=CARTESIAN_POINT('Ctrl Pts',(-0.110909354270907,36.5287456100735,
-2.00000000000004));
#10119=CARTESIAN_POINT('Ctrl Pts',(0.424989030591338,36.7370789434068,-2.02971807190996));
#10120=CARTESIAN_POINT('Ctrl Pts',(0.903949681684066,36.9454122767402,-1.78750548470439));
#10121=CARTESIAN_POINT('Ctrl Pts',(1.38291033277679,37.1537456100734,-1.54529289749872));
#10122=CARTESIAN_POINT('Ctrl Pts',(1.67659613043343,37.3620789434069,-1.09605031831598));
#10123=CARTESIAN_POINT('Ctrl Pts',(1.97028192809006,37.5704122767401,-0.646807739133152));
#10124=CARTESIAN_POINT('Ctrl Pts',(2.,37.7787456100735,-0.110909354270952));
#10125=CARTESIAN_POINT('Ctrl Pts',(2.02971807190997,37.9870789434069,0.424989030591333));
#10126=CARTESIAN_POINT('Ctrl Pts',(1.78750548470433,38.1954122767402,0.903949681684023));
#10127=CARTESIAN_POINT('Ctrl Pts',(1.54529289749872,38.4037456100734,1.3829103327768));
#10128=CARTESIAN_POINT('Ctrl Pts',(1.09605031831595,38.6120789434069,1.67659613043338));
#10129=CARTESIAN_POINT('Ctrl Pts',(0.646807739133154,38.8204122767402,1.97028192809006));
#10130=CARTESIAN_POINT('Ctrl Pts',(0.110909354270921,39.0287456100735,1.99999999999997));
#10131=CARTESIAN_POINT('Ctrl Pts',(-0.424989030591324,39.2370789434069,
2.02971807190996));
#10132=CARTESIAN_POINT('Ctrl Pts',(-0.903949681684052,39.4454122767402,
1.78750548470429));
#10133=CARTESIAN_POINT('Ctrl Pts',(-1.38291033277679,39.6537456100735,1.54529289749867));
#10134=CARTESIAN_POINT('Ctrl Pts',(-1.67659613043342,39.8620789434069,1.09605031831587));
#10135=CARTESIAN_POINT('Ctrl Pts',(-1.97028192809005,40.0704122767402,0.646807739133166));
#10136=CARTESIAN_POINT('Ctrl Pts',(-2.,40.2787456100735,0.110909354270834));
#10137=CARTESIAN_POINT('Ctrl Pts',(-1.40000000000002,0.278745610073447,
0.110909354270819));
#10138=CARTESIAN_POINT('Ctrl Pts',(-1.42971807190993,0.487078943406762,
-0.264219515132761));
#10139=CARTESIAN_POINT('Ctrl Pts',(-1.26789024243367,0.695412276740075,
-0.603949681684109));
#10140=CARTESIAN_POINT('Ctrl Pts',(-1.10606241295736,0.903745610073446,
-0.943679848235563));
#10141=CARTESIAN_POINT('Ctrl Pts',(-0.796050318315929,1.11207894340677,
-1.1569808881628));
#10142=CARTESIAN_POINT('Ctrl Pts',(-0.486038223674453,1.3204122767401,-1.37028192809014));
#10143=CARTESIAN_POINT('Ctrl Pts',(-0.110909354270902,1.52874561007343,
-1.40000000000009));
#10144=CARTESIAN_POINT('Ctrl Pts',(0.26421951513267,1.73707894340676,-1.42971807191003));
#10145=CARTESIAN_POINT('Ctrl Pts',(0.60394968168407,1.9454122767401,-1.26789024243367));
#10146=CARTESIAN_POINT('Ctrl Pts',(0.943679848235471,2.15374561007345,-1.10606241295738));
#10147=CARTESIAN_POINT('Ctrl Pts',(1.15698088816274,2.36207894340676,-0.796050318316012));
#10148=CARTESIAN_POINT('Ctrl Pts',(1.37028192809006,2.5704122767401,-0.486038223674555));
#10149=CARTESIAN_POINT('Ctrl Pts',(1.39999999999998,2.77874561007344,-0.110909354270902));
#10150=CARTESIAN_POINT('Ctrl Pts',(1.42971807190994,2.98707894340678,0.264219515132648));
#10151=CARTESIAN_POINT('Ctrl Pts',(1.26789024243366,3.19541227674007,0.60394968168399));
#10152=CARTESIAN_POINT('Ctrl Pts',(1.10606241295741,3.40374561007344,0.943679848235385));
#10153=CARTESIAN_POINT('Ctrl Pts',(0.796050318315931,3.61207894340678,1.15698088816276));
#10154=CARTESIAN_POINT('Ctrl Pts',(0.486038223674496,3.82041227674011,1.37028192808997));
#10155=CARTESIAN_POINT('Ctrl Pts',(0.110909354270899,4.02874561007344,1.4));
#10156=CARTESIAN_POINT('Ctrl Pts',(-0.264219515132648,4.23707894340677,
1.42971807190986));
#10157=CARTESIAN_POINT('Ctrl Pts',(-0.603949681684091,4.44541227674011,
1.2678902424336));
#10158=CARTESIAN_POINT('Ctrl Pts',(-0.943679848235468,4.65374561007345,
1.1060624129573));
#10159=CARTESIAN_POINT('Ctrl Pts',(-1.15698088816278,4.86207894340679,0.796050318315845));
#10160=CARTESIAN_POINT('Ctrl Pts',(-1.37028192809003,5.07041227674011,0.486038223674474));
#10161=CARTESIAN_POINT('Ctrl Pts',(-1.40000000000002,5.27874561007345,0.110909354270819));
#10162=CARTESIAN_POINT('Ctrl Pts',(-1.42971807190992,5.4870789434068,-0.264219515132837));
#10163=CARTESIAN_POINT('Ctrl Pts',(-1.26789024243366,5.69541227674011,-0.603949681684078));
#10164=CARTESIAN_POINT('Ctrl Pts',(-1.10606241295738,5.90374561007345,-0.943679848235563));
#10165=CARTESIAN_POINT('Ctrl Pts',(-0.79605031831595,6.11207894340678,-1.15698088816284));
#10166=CARTESIAN_POINT('Ctrl Pts',(-0.486038223674474,6.32041227674012,
-1.37028192809014));
#10167=CARTESIAN_POINT('Ctrl Pts',(-0.110909354270923,6.52874561007347,
-1.40000000000009));
#10168=CARTESIAN_POINT('Ctrl Pts',(0.264219515132672,6.7370789434068,-1.42971807191003));
#10169=CARTESIAN_POINT('Ctrl Pts',(0.60394968168407,6.94541227674011,-1.26789024243367));
#10170=CARTESIAN_POINT('Ctrl Pts',(0.943679848235474,7.15374561007344,-1.10606241295738));
#10171=CARTESIAN_POINT('Ctrl Pts',(1.15698088816276,7.36207894340676,-0.796050318316012));
#10172=CARTESIAN_POINT('Ctrl Pts',(1.37028192809008,7.57041227674013,-0.486038223674566));
#10173=CARTESIAN_POINT('Ctrl Pts',(1.4,7.77874561007344,-0.110909354270902));
#10174=CARTESIAN_POINT('Ctrl Pts',(1.42971807190995,7.98707894340678,0.264219515132605));
#10175=CARTESIAN_POINT('Ctrl Pts',(1.26789024243366,8.19541227674011,0.603949681683985));
#10176=CARTESIAN_POINT('Ctrl Pts',(1.10606241295739,8.40374561007346,0.943679848235385));
#10177=CARTESIAN_POINT('Ctrl Pts',(0.796050318315911,8.6120789434068,1.15698088816276));
#10178=CARTESIAN_POINT('Ctrl Pts',(0.486038223674474,8.82041227674011,1.37028192809001));
#10179=CARTESIAN_POINT('Ctrl Pts',(0.110909354270881,9.02874561007344,1.4));
#10180=CARTESIAN_POINT('Ctrl Pts',(-0.264219515132648,9.23707894340678,
1.42971807190988));
#10181=CARTESIAN_POINT('Ctrl Pts',(-0.603949681684091,9.44541227674012,
1.26789024243366));
#10182=CARTESIAN_POINT('Ctrl Pts',(-0.943679848235471,9.65374561007344,
1.1060624129573));
#10183=CARTESIAN_POINT('Ctrl Pts',(-1.15698088816276,9.86207894340679,0.796050318315845));
#10184=CARTESIAN_POINT('Ctrl Pts',(-1.37028192809006,10.0704122767401,0.486038223674393));
#10185=CARTESIAN_POINT('Ctrl Pts',(-1.40000000000002,10.2787456100734,0.110909354270819));
#10186=CARTESIAN_POINT('Ctrl Pts',(-1.42971807190993,10.4870789434068,-0.264219515132756));
#10187=CARTESIAN_POINT('Ctrl Pts',(-1.26789024243369,10.6954122767401,-0.60394968168412));
#10188=CARTESIAN_POINT('Ctrl Pts',(-1.10606241295736,10.9037456100735,-0.94367984823553));
#10189=CARTESIAN_POINT('Ctrl Pts',(-0.79605031831595,11.1120789434068,-1.15698088816285));
#10190=CARTESIAN_POINT('Ctrl Pts',(-0.486038223674453,11.3204122767401,
-1.37028192809014));
#10191=CARTESIAN_POINT('Ctrl Pts',(-0.110909354270923,11.5287456100735,
-1.40000000000009));
#10192=CARTESIAN_POINT('Ctrl Pts',(0.264219515132691,11.7370789434068,-1.42971807191005));
#10193=CARTESIAN_POINT('Ctrl Pts',(0.60394968168405,11.9454122767401,-1.26789024243367));
#10194=CARTESIAN_POINT('Ctrl Pts',(0.943679848235492,12.1537456100735,-1.10606241295747));
#10195=CARTESIAN_POINT('Ctrl Pts',(1.15698088816276,12.3620789434068,-0.796050318316012));
#10196=CARTESIAN_POINT('Ctrl Pts',(1.37028192809006,12.5704122767401,-0.48603822367456));
#10197=CARTESIAN_POINT('Ctrl Pts',(1.4,12.7787456100735,-0.110909354270902));
#10198=CARTESIAN_POINT('Ctrl Pts',(1.42971807190997,12.9870789434068,0.264219515132578));
#10199=CARTESIAN_POINT('Ctrl Pts',(1.26789024243366,13.1954122767402,0.603949681683979));
#10200=CARTESIAN_POINT('Ctrl Pts',(1.10606241295738,13.4037456100734,0.943679848235428));
#10201=CARTESIAN_POINT('Ctrl Pts',(0.796050318315911,13.6120789434068,1.15698088816276));
#10202=CARTESIAN_POINT('Ctrl Pts',(0.486038223674477,13.8204122767401,1.37028192809001));
#10203=CARTESIAN_POINT('Ctrl Pts',(0.110909354270902,14.0287456100735,1.4));
#10204=CARTESIAN_POINT('Ctrl Pts',(-0.264219515132648,14.2370789434068,
1.42971807190986));
#10205=CARTESIAN_POINT('Ctrl Pts',(-0.603949681684091,14.4454122767401,
1.26789024243366));
#10206=CARTESIAN_POINT('Ctrl Pts',(-0.943679848235471,14.6537456100735,
1.10606241295732));
#10207=CARTESIAN_POINT('Ctrl Pts',(-1.15698088816278,14.8620789434068,0.796050318315845));
#10208=CARTESIAN_POINT('Ctrl Pts',(-1.37028192809005,15.0704122767401,0.48603822367442));
#10209=CARTESIAN_POINT('Ctrl Pts',(-1.4,15.2787456100735,0.110909354270819));
#10210=CARTESIAN_POINT('Ctrl Pts',(-1.42971807190992,15.4870789434068,-0.264219515132718));
#10211=CARTESIAN_POINT('Ctrl Pts',(-1.26789024243366,15.6954122767401,-0.603949681684167));
#10212=CARTESIAN_POINT('Ctrl Pts',(-1.10606241295736,15.9037456100735,-0.943679848235573));
#10213=CARTESIAN_POINT('Ctrl Pts',(-0.796050318315929,16.1120789434068,
-1.15698088816286));
#10214=CARTESIAN_POINT('Ctrl Pts',(-0.486038223674453,16.3204122767402,
-1.37028192809016));
#10215=CARTESIAN_POINT('Ctrl Pts',(-0.110909354270902,16.5287456100735,
-1.40000000000009));
#10216=CARTESIAN_POINT('Ctrl Pts',(0.264219515132672,16.7370789434068,-1.42971807191007));
#10217=CARTESIAN_POINT('Ctrl Pts',(0.60394968168407,16.9454122767402,-1.26789024243367));
#10218=CARTESIAN_POINT('Ctrl Pts',(0.943679848235471,17.1537456100735,-1.10606241295741));
#10219=CARTESIAN_POINT('Ctrl Pts',(1.15698088816274,17.3620789434068,-0.796050318316007));
#10220=CARTESIAN_POINT('Ctrl Pts',(1.37028192809005,17.5704122767402,-0.486038223674528));
#10221=CARTESIAN_POINT('Ctrl Pts',(1.39999999999998,17.7787456100735,-0.110909354270907));
#10222=CARTESIAN_POINT('Ctrl Pts',(1.42971807190994,17.9870789434068,0.2642195151326));
#10223=CARTESIAN_POINT('Ctrl Pts',(1.26789024243364,18.1954122767402,0.603949681683979));
#10224=CARTESIAN_POINT('Ctrl Pts',(1.10606241295739,18.4037456100735,0.943679848235406));
#10225=CARTESIAN_POINT('Ctrl Pts',(0.796050318315929,18.6120789434068,1.15698088816276));
#10226=CARTESIAN_POINT('Ctrl Pts',(0.486038223674496,18.8204122767402,1.37028192808999));
#10227=CARTESIAN_POINT('Ctrl Pts',(0.110909354270902,19.0287456100735,1.39999999999996));
#10228=CARTESIAN_POINT('Ctrl Pts',(-0.26421951513267,19.2370789434068,1.42971807190988));
#10229=CARTESIAN_POINT('Ctrl Pts',(-0.60394968168407,19.4454122767402,1.26789024243363));
#10230=CARTESIAN_POINT('Ctrl Pts',(-0.943679848235452,19.6537456100735,
1.1060624129573));
#10231=CARTESIAN_POINT('Ctrl Pts',(-1.15698088816278,19.8620789434068,0.796050318315845));
#10232=CARTESIAN_POINT('Ctrl Pts',(-1.37028192809005,20.0704122767402,0.486038223674393));
#10233=CARTESIAN_POINT('Ctrl Pts',(-1.4,20.2787456100735,0.110909354270813));
#10234=CARTESIAN_POINT('Ctrl Pts',(-1.42971807190994,20.4870789434068,-0.26421951513274));
#10235=CARTESIAN_POINT('Ctrl Pts',(-1.26789024243366,20.6954122767402,-0.603949681684167));
#10236=CARTESIAN_POINT('Ctrl Pts',(-1.10606241295736,20.9037456100735,-0.943679848235573));
#10237=CARTESIAN_POINT('Ctrl Pts',(-0.79605031831595,21.1120789434068,-1.15698088816285));
#10238=CARTESIAN_POINT('Ctrl Pts',(-0.486038223674453,21.3204122767402,
-1.37028192809015));
#10239=CARTESIAN_POINT('Ctrl Pts',(-0.110909354270923,21.5287456100735,
-1.4000000000001));
#10240=CARTESIAN_POINT('Ctrl Pts',(0.264219515132691,21.7370789434068,-1.42971807191004));
#10241=CARTESIAN_POINT('Ctrl Pts',(0.60394968168407,21.9454122767402,-1.26789024243367));
#10242=CARTESIAN_POINT('Ctrl Pts',(0.943679848235474,22.1537456100735,-1.10606241295747));
#10243=CARTESIAN_POINT('Ctrl Pts',(1.15698088816276,22.3620789434068,-0.796050318316001));
#10244=CARTESIAN_POINT('Ctrl Pts',(1.37028192809006,22.5704122767402,-0.486038223674555));
#10245=CARTESIAN_POINT('Ctrl Pts',(1.4,22.7787456100735,-0.110909354270928));
#10246=CARTESIAN_POINT('Ctrl Pts',(1.42971807190997,22.9870789434068,0.264219515132573));
#10247=CARTESIAN_POINT('Ctrl Pts',(1.26789024243366,23.1954122767402,0.603949681684057));
#10248=CARTESIAN_POINT('Ctrl Pts',(1.10606241295738,23.4037456100735,0.943679848235433));
#10249=CARTESIAN_POINT('Ctrl Pts',(0.796050318315926,23.6120789434068,1.15698088816273));
#10250=CARTESIAN_POINT('Ctrl Pts',(0.486038223674474,23.8204122767402,1.37028192809002));
#10251=CARTESIAN_POINT('Ctrl Pts',(0.110909354270881,24.0287456100735,1.39999999999998));
#10252=CARTESIAN_POINT('Ctrl Pts',(-0.264219515132651,24.2370789434069,
1.42971807190985));
#10253=CARTESIAN_POINT('Ctrl Pts',(-0.603949681684091,24.4454122767401,
1.2678902424336));
#10254=CARTESIAN_POINT('Ctrl Pts',(-0.943679848235471,24.6537456100735,
1.10606241295733));
#10255=CARTESIAN_POINT('Ctrl Pts',(-1.15698088816276,24.8620789434068,0.796050318315887));
#10256=CARTESIAN_POINT('Ctrl Pts',(-1.37028192809005,25.0704122767401,0.486038223674404));
#10257=CARTESIAN_POINT('Ctrl Pts',(-1.4,25.2787456100735,0.110909354270813));
#10258=CARTESIAN_POINT('Ctrl Pts',(-1.42971807190994,25.4870789434068,-0.264219515132734));
#10259=CARTESIAN_POINT('Ctrl Pts',(-1.26789024243369,25.6954122767402,-0.603949681684162));
#10260=CARTESIAN_POINT('Ctrl Pts',(-1.10606241295738,25.9037456100735,-0.943679848235541));
#10261=CARTESIAN_POINT('Ctrl Pts',(-0.79605031831595,26.1120789434068,-1.15698088816286));
#10262=CARTESIAN_POINT('Ctrl Pts',(-0.486038223674453,26.3204122767402,
-1.37028192809015));
#10263=CARTESIAN_POINT('Ctrl Pts',(-0.110909354270923,26.5287456100735,
-1.4000000000001));
#10264=CARTESIAN_POINT('Ctrl Pts',(0.264219515132694,26.7370789434069,-1.42971807191004));
#10265=CARTESIAN_POINT('Ctrl Pts',(0.60394968168405,26.9454122767402,-1.26789024243367));
#10266=CARTESIAN_POINT('Ctrl Pts',(0.943679848235492,27.1537456100735,-1.10606241295747));
#10267=CARTESIAN_POINT('Ctrl Pts',(1.15698088816274,27.3620789434069,-0.796050318316001));
#10268=CARTESIAN_POINT('Ctrl Pts',(1.37028192809008,27.5704122767402,-0.486038223674528));
#10269=CARTESIAN_POINT('Ctrl Pts',(1.39999999999998,27.7787456100735,-0.110909354270917));
#10270=CARTESIAN_POINT('Ctrl Pts',(1.42971807190997,27.9870789434068,0.264219515132594));
#10271=CARTESIAN_POINT('Ctrl Pts',(1.26789024243366,28.1954122767402,0.603949681684047));
#10272=CARTESIAN_POINT('Ctrl Pts',(1.10606241295738,28.4037456100735,0.943679848235406));
#10273=CARTESIAN_POINT('Ctrl Pts',(0.796050318315908,28.6120789434068,1.15698088816274));
#10274=CARTESIAN_POINT('Ctrl Pts',(0.486038223674496,28.8204122767402,1.37028192809));
#10275=CARTESIAN_POINT('Ctrl Pts',(0.110909354270902,29.0287456100735,1.39999999999997));
#10276=CARTESIAN_POINT('Ctrl Pts',(-0.26421951513267,29.2370789434068,1.42971807190989));
#10277=CARTESIAN_POINT('Ctrl Pts',(-0.603949681684091,29.4454122767402,
1.26789024243359));
#10278=CARTESIAN_POINT('Ctrl Pts',(-0.943679848235452,29.6537456100735,
1.10606241295731));
#10279=CARTESIAN_POINT('Ctrl Pts',(-1.15698088816278,29.8620789434069,0.796050318315892));
#10280=CARTESIAN_POINT('Ctrl Pts',(-1.37028192809005,30.0704122767402,0.486038223674393));
#10281=CARTESIAN_POINT('Ctrl Pts',(-1.4,30.2787456100735,0.11090935427086));
#10282=CARTESIAN_POINT('Ctrl Pts',(-1.42971807190994,30.4870789434069,-0.26421951513274));
#10283=CARTESIAN_POINT('Ctrl Pts',(-1.26789024243366,30.6954122767402,-0.603949681684162));
#10284=CARTESIAN_POINT('Ctrl Pts',(-1.10606241295736,30.9037456100735,-0.943679848235563));
#10285=CARTESIAN_POINT('Ctrl Pts',(-0.79605031831595,31.1120789434068,-1.15698088816285));
#10286=CARTESIAN_POINT('Ctrl Pts',(-0.486038223674471,31.3204122767402,
-1.37028192809016));
#10287=CARTESIAN_POINT('Ctrl Pts',(-0.110909354270923,31.5287456100735,
-1.4000000000001));
#10288=CARTESIAN_POINT('Ctrl Pts',(0.264219515132691,31.7370789434069,-1.42971807191));
#10289=CARTESIAN_POINT('Ctrl Pts',(0.60394968168407,31.9454122767402,-1.26789024243368));
#10290=CARTESIAN_POINT('Ctrl Pts',(0.943679848235474,32.1537456100735,-1.10606241295744));
#10291=CARTESIAN_POINT('Ctrl Pts',(1.15698088816274,32.3620789434069,-0.796050318315981));
#10292=CARTESIAN_POINT('Ctrl Pts',(1.37028192809005,32.5704122767402,-0.48603822367455));
#10293=CARTESIAN_POINT('Ctrl Pts',(1.4,32.7787456100735,-0.110909354270917));
#10294=CARTESIAN_POINT('Ctrl Pts',(1.42971807190994,32.9870789434069,0.264219515132578));
#10295=CARTESIAN_POINT('Ctrl Pts',(1.26789024243364,33.1954122767402,0.603949681684047));
#10296=CARTESIAN_POINT('Ctrl Pts',(1.10606241295741,33.4037456100735,0.943679848235428));
#10297=CARTESIAN_POINT('Ctrl Pts',(0.796050318315929,33.6120789434069,1.15698088816274));
#10298=CARTESIAN_POINT('Ctrl Pts',(0.486038223674496,33.8204122767402,1.37028192809002));
#10299=CARTESIAN_POINT('Ctrl Pts',(0.110909354270881,34.0287456100735,1.39999999999998));
#10300=CARTESIAN_POINT('Ctrl Pts',(-0.26421951513267,34.2370789434069,1.42971807190985));
#10301=CARTESIAN_POINT('Ctrl Pts',(-0.603949681684091,34.4454122767402,
1.26789024243359));
#10302=CARTESIAN_POINT('Ctrl Pts',(-0.943679848235449,34.6537456100735,
1.10606241295733));
#10303=CARTESIAN_POINT('Ctrl Pts',(-1.15698088816278,34.8620789434069,0.796050318315903));
#10304=CARTESIAN_POINT('Ctrl Pts',(-1.37028192809003,35.0704122767402,0.486038223674404));
#10305=CARTESIAN_POINT('Ctrl Pts',(-1.4,35.2787456100735,0.11090935427086));
#10306=CARTESIAN_POINT('Ctrl Pts',(-1.42971807190994,35.4870789434069,-0.264219515132756));
#10307=CARTESIAN_POINT('Ctrl Pts',(-1.26789024243369,35.6954122767402,-0.603949681684089));
#10308=CARTESIAN_POINT('Ctrl Pts',(-1.10606241295738,35.9037456100736,-0.943679848235563));
#10309=CARTESIAN_POINT('Ctrl Pts',(-0.79605031831595,36.1120789434069,-1.15698088816278));
#10310=CARTESIAN_POINT('Ctrl Pts',(-0.486038223674474,36.3204122767402,
-1.37028192809014));
#10311=CARTESIAN_POINT('Ctrl Pts',(-0.11090935427092,36.5287456100735,-1.40000000000009));
#10312=CARTESIAN_POINT('Ctrl Pts',(0.264219515132672,36.7370789434069,-1.42971807191003));
#10313=CARTESIAN_POINT('Ctrl Pts',(0.60394968168405,36.9454122767402,-1.2678902424337));
#10314=CARTESIAN_POINT('Ctrl Pts',(0.943679848235492,37.1537456100735,-1.10606241295747));
#10315=CARTESIAN_POINT('Ctrl Pts',(1.15698088816274,37.3620789434068,-0.796050318315981));
#10316=CARTESIAN_POINT('Ctrl Pts',(1.37028192809008,37.5704122767402,-0.486038223674555));
#10317=CARTESIAN_POINT('Ctrl Pts',(1.4,37.7787456100735,-0.110909354270923));
#10318=CARTESIAN_POINT('Ctrl Pts',(1.42971807190994,37.9870789434069,0.264219515132605));
#10319=CARTESIAN_POINT('Ctrl Pts',(1.26789024243366,38.1954122767402,0.603949681684011));
#10320=CARTESIAN_POINT('Ctrl Pts',(1.10606241295738,38.4037456100735,0.943679848235417));
#10321=CARTESIAN_POINT('Ctrl Pts',(0.796050318315929,38.6120789434069,1.15698088816273));
#10322=CARTESIAN_POINT('Ctrl Pts',(0.486038223674474,38.8204122767402,1.37028192808999));
#10323=CARTESIAN_POINT('Ctrl Pts',(0.110909354270881,39.0287456100735,1.39999999999998));
#10324=CARTESIAN_POINT('Ctrl Pts',(-0.264219515132648,39.2370789434069,
1.42971807190988));
#10325=CARTESIAN_POINT('Ctrl Pts',(-0.603949681684073,39.4454122767402,
1.26789024243359));
#10326=CARTESIAN_POINT('Ctrl Pts',(-0.943679848235474,39.6537456100736,
1.10606241295731));
#10327=CARTESIAN_POINT('Ctrl Pts',(-1.15698088816278,39.8620789434069,0.796050318315897));
#10328=CARTESIAN_POINT('Ctrl Pts',(-1.37028192809005,40.0704122767402,0.486038223674399));
#10329=CARTESIAN_POINT('Ctrl Pts',(-1.4,40.2787456100735,0.11090935427086));
#10330=CARTESIAN_POINT('Ctrl Pts',(-1.4,-0.278745610073483,-0.110909354270949));
#10331=CARTESIAN_POINT('Ctrl Pts',(-1.37028192809006,-0.0704122767401418,
-0.486038223674447));
#10332=CARTESIAN_POINT('Ctrl Pts',(-1.1569808881628,0.137921056593191,-0.796050318316017));
#10333=CARTESIAN_POINT('Ctrl Pts',(-0.943679848235495,0.346254389926559,
-1.10606241295736));
#10334=CARTESIAN_POINT('Ctrl Pts',(-0.60394968168412,0.554587723259871,
-1.26789024243366));
#10335=CARTESIAN_POINT('Ctrl Pts',(-0.264219515132702,0.762921056593206,
-1.42971807191002));
#10336=CARTESIAN_POINT('Ctrl Pts',(0.11090935427085,0.971254389926519,-1.39999999999999));
#10337=CARTESIAN_POINT('Ctrl Pts',(0.486038223674463,1.17958772325989,-1.37028192809015));
#10338=CARTESIAN_POINT('Ctrl Pts',(0.7960503183159,1.3879210565932,-1.15698088816281));
#10339=CARTESIAN_POINT('Ctrl Pts',(1.10606241295738,1.59625438992658,-0.943679848235584));
#10340=CARTESIAN_POINT('Ctrl Pts',(1.26789024243364,1.80458772325987,-0.603949681684177));
#10341=CARTESIAN_POINT('Ctrl Pts',(1.42971807190996,2.01292105659321,-0.264219515132788));
#10342=CARTESIAN_POINT('Ctrl Pts',(1.39999999999998,2.22125438992654,0.110909354270787));
#10343=CARTESIAN_POINT('Ctrl Pts',(1.37028192809009,2.42958772325987,0.486038223674361));
#10344=CARTESIAN_POINT('Ctrl Pts',(1.15698088816276,2.63792105659322,0.796050318315897));
#10345=CARTESIAN_POINT('Ctrl Pts',(0.943679848235517,2.84625438992656,1.10606241295735));
#10346=CARTESIAN_POINT('Ctrl Pts',(0.603949681684099,3.05458772325989,1.26789024243365));
#10347=CARTESIAN_POINT('Ctrl Pts',(0.264219515132705,3.26292105659324,1.42971807190985));
#10348=CARTESIAN_POINT('Ctrl Pts',(-0.110909354270889,3.47125438992654,
1.39999999999992));
#10349=CARTESIAN_POINT('Ctrl Pts',(-0.48603822367442,3.67958772325988,1.37028192808998));
#10350=CARTESIAN_POINT('Ctrl Pts',(-0.796050318315921,3.8879210565932,1.15698088816272));
#10351=CARTESIAN_POINT('Ctrl Pts',(-1.10606241295734,4.09625438992655,0.943679848235406));
#10352=CARTESIAN_POINT('Ctrl Pts',(-1.26789024243365,4.30458772325989,0.603949681684094));
#10353=CARTESIAN_POINT('Ctrl Pts',(-1.42971807190994,4.51292105659323,0.2642195151326));
#10354=CARTESIAN_POINT('Ctrl Pts',(-1.4,4.72125438992655,-0.110909354270949));
#10355=CARTESIAN_POINT('Ctrl Pts',(-1.37028192809004,4.9295877232599,-0.486038223674442));
#10356=CARTESIAN_POINT('Ctrl Pts',(-1.15698088816278,5.13792105659321,-0.796050318315991));
#10357=CARTESIAN_POINT('Ctrl Pts',(-0.943679848235495,5.34625438992658,
-1.10606241295745));
#10358=CARTESIAN_POINT('Ctrl Pts',(-0.603949681684099,5.55458772325993,
-1.26789024243366));
#10359=CARTESIAN_POINT('Ctrl Pts',(-0.264219515132702,5.76292105659326,
-1.42971807190998));
#10360=CARTESIAN_POINT('Ctrl Pts',(0.110909354270868,5.97125438992656,-1.40000000000003));
#10361=CARTESIAN_POINT('Ctrl Pts',(0.486038223674442,6.17958772325989,-1.37028192809015));
#10362=CARTESIAN_POINT('Ctrl Pts',(0.796050318315879,6.38792105659323,-1.15698088816278));
#10363=CARTESIAN_POINT('Ctrl Pts',(1.10606241295736,6.59625438992658,-0.943679848235606));
#10364=CARTESIAN_POINT('Ctrl Pts',(1.26789024243365,6.80458772325986,-0.603949681684177));
#10365=CARTESIAN_POINT('Ctrl Pts',(1.42971807190994,7.01292105659325,-0.264219515132794));
#10366=CARTESIAN_POINT('Ctrl Pts',(1.4,7.22125438992654,0.110909354270824));
#10367=CARTESIAN_POINT('Ctrl Pts',(1.37028192809007,7.42958772325991,0.486038223674361));
#10368=CARTESIAN_POINT('Ctrl Pts',(1.15698088816276,7.63792105659323,0.796050318315897));
#10369=CARTESIAN_POINT('Ctrl Pts',(0.943679848235498,7.84625438992655,1.10606241295728));
#10370=CARTESIAN_POINT('Ctrl Pts',(0.603949681684078,8.05458772325989,1.26789024243365));
#10371=CARTESIAN_POINT('Ctrl Pts',(0.264219515132724,8.26292105659323,1.42971807190989));
#10372=CARTESIAN_POINT('Ctrl Pts',(-0.110909354270889,8.47125438992655,
1.39999999999992));
#10373=CARTESIAN_POINT('Ctrl Pts',(-0.486038223674439,8.67958772325992,
1.37028192808998));
#10374=CARTESIAN_POINT('Ctrl Pts',(-0.796050318315921,8.88792105659323,
1.15698088816273));
#10375=CARTESIAN_POINT('Ctrl Pts',(-1.10606241295736,9.09625438992657,0.94367984823539));
#10376=CARTESIAN_POINT('Ctrl Pts',(-1.26789024243365,9.3045877232599,0.603949681684094));
#10377=CARTESIAN_POINT('Ctrl Pts',(-1.42971807190994,9.51292105659322,0.264219515132616));
#10378=CARTESIAN_POINT('Ctrl Pts',(-1.4,9.72125438992658,-0.110909354270954));
#10379=CARTESIAN_POINT('Ctrl Pts',(-1.37028192809006,9.92958772325988,-0.486038223674523));
#10380=CARTESIAN_POINT('Ctrl Pts',(-1.1569808881628,10.1379210565933,-0.796050318315991));
#10381=CARTESIAN_POINT('Ctrl Pts',(-0.943679848235474,10.3462543899266,
-1.10606241295745));
#10382=CARTESIAN_POINT('Ctrl Pts',(-0.60394968168412,10.5545877232599,-1.26789024243366));
#10383=CARTESIAN_POINT('Ctrl Pts',(-0.264219515132683,10.7629210565932,
-1.42971807191006));
#10384=CARTESIAN_POINT('Ctrl Pts',(0.110909354270847,10.9712543899266,-1.40000000000007));
#10385=CARTESIAN_POINT('Ctrl Pts',(0.486038223674463,11.1795877232599,-1.37028192809018));
#10386=CARTESIAN_POINT('Ctrl Pts',(0.7960503183159,11.3879210565933,-1.15698088816279));
#10387=CARTESIAN_POINT('Ctrl Pts',(1.10606241295736,11.5962543899266,-0.943679848235595));
#10388=CARTESIAN_POINT('Ctrl Pts',(1.26789024243365,11.8045877232599,-0.603949681684188));
#10389=CARTESIAN_POINT('Ctrl Pts',(1.42971807190994,12.0129210565932,-0.264219515132707));
#10390=CARTESIAN_POINT('Ctrl Pts',(1.4,12.2212543899266,0.110909354270855));
#10391=CARTESIAN_POINT('Ctrl Pts',(1.37028192809006,12.4295877232599,0.486038223674382));
#10392=CARTESIAN_POINT('Ctrl Pts',(1.15698088816276,12.6379210565932,0.796050318315897));
#10393=CARTESIAN_POINT('Ctrl Pts',(0.943679848235517,12.8462543899266,1.10606241295731));
#10394=CARTESIAN_POINT('Ctrl Pts',(0.603949681684099,13.0545877232599,1.26789024243365));
#10395=CARTESIAN_POINT('Ctrl Pts',(0.264219515132705,13.2629210565933,1.42971807190989));
#10396=CARTESIAN_POINT('Ctrl Pts',(-0.110909354270889,13.4712543899266,
1.39999999999992));
#10397=CARTESIAN_POINT('Ctrl Pts',(-0.48603822367442,13.6795877232599,1.37028192808998));
#10398=CARTESIAN_POINT('Ctrl Pts',(-0.7960503183159,13.8879210565933,1.15698088816275));
#10399=CARTESIAN_POINT('Ctrl Pts',(-1.10606241295736,14.0962543899266,0.943679848235428));
#10400=CARTESIAN_POINT('Ctrl Pts',(-1.26789024243365,14.3045877232599,0.603949681684078));
#10401=CARTESIAN_POINT('Ctrl Pts',(-1.42971807190992,14.5129210565933,0.264219515132632));
#10402=CARTESIAN_POINT('Ctrl Pts',(-1.40000000000002,14.7212543899266,-0.110909354270954));
#10403=CARTESIAN_POINT('Ctrl Pts',(-1.37028192809007,14.9295877232599,-0.486038223674463));
#10404=CARTESIAN_POINT('Ctrl Pts',(-1.15698088816278,15.1379210565933,-0.796050318315991));
#10405=CARTESIAN_POINT('Ctrl Pts',(-0.943679848235495,15.3462543899266,
-1.10606241295744));
#10406=CARTESIAN_POINT('Ctrl Pts',(-0.60394968168412,15.55458772326,-1.26789024243366));
#10407=CARTESIAN_POINT('Ctrl Pts',(-0.264219515132702,15.7629210565933,
-1.42971807191003));
#10408=CARTESIAN_POINT('Ctrl Pts',(0.110909354270868,15.9712543899266,-1.40000000000008));
#10409=CARTESIAN_POINT('Ctrl Pts',(0.486038223674463,16.1795877232599,-1.37028192809016));
#10410=CARTESIAN_POINT('Ctrl Pts',(0.796050318315879,16.3879210565933,-1.15698088816279));
#10411=CARTESIAN_POINT('Ctrl Pts',(1.10606241295736,16.5962543899266,-0.94367984823559));
#10412=CARTESIAN_POINT('Ctrl Pts',(1.26789024243365,16.8045877232599,-0.603949681684188));
#10413=CARTESIAN_POINT('Ctrl Pts',(1.42971807190996,17.0129210565933,-0.264219515132783));
#10414=CARTESIAN_POINT('Ctrl Pts',(1.39999999999998,17.2212543899266,0.11090935427085));
#10415=CARTESIAN_POINT('Ctrl Pts',(1.37028192809007,17.4295877232599,0.486038223674382));
#10416=CARTESIAN_POINT('Ctrl Pts',(1.15698088816276,17.6379210565933,0.796050318315892));
#10417=CARTESIAN_POINT('Ctrl Pts',(0.943679848235517,17.8462543899266,1.10606241295728));
#10418=CARTESIAN_POINT('Ctrl Pts',(0.603949681684099,18.0545877232599,1.26789024243363));
#10419=CARTESIAN_POINT('Ctrl Pts',(0.264219515132724,18.2629210565933,1.42971807190987));
#10420=CARTESIAN_POINT('Ctrl Pts',(-0.110909354270889,18.4712543899266,
1.39999999999997));
#10421=CARTESIAN_POINT('Ctrl Pts',(-0.48603822367442,18.6795877232599,1.37028192808996));
#10422=CARTESIAN_POINT('Ctrl Pts',(-0.796050318315921,18.8879210565933,
1.15698088816276));
#10423=CARTESIAN_POINT('Ctrl Pts',(-1.10606241295736,19.0962543899266,0.943679848235417));
#10424=CARTESIAN_POINT('Ctrl Pts',(-1.26789024243365,19.3045877232599,0.603949681684037));
#10425=CARTESIAN_POINT('Ctrl Pts',(-1.42971807190994,19.5129210565933,0.264219515132616));
#10426=CARTESIAN_POINT('Ctrl Pts',(-1.4,19.7212543899266,-0.110909354270954));
#10427=CARTESIAN_POINT('Ctrl Pts',(-1.37028192809006,19.9295877232599,-0.486038223674496));
#10428=CARTESIAN_POINT('Ctrl Pts',(-1.1569808881628,20.1379210565933,-0.796050318315996));
#10429=CARTESIAN_POINT('Ctrl Pts',(-0.943679848235474,20.3462543899266,
-1.10606241295739));
#10430=CARTESIAN_POINT('Ctrl Pts',(-0.603949681684099,20.5545877232599,
-1.26789024243366));
#10431=CARTESIAN_POINT('Ctrl Pts',(-0.264219515132683,20.7629210565933,
-1.42971807191002));
#10432=CARTESIAN_POINT('Ctrl Pts',(0.110909354270868,20.9712543899266,-1.40000000000009));
#10433=CARTESIAN_POINT('Ctrl Pts',(0.486038223674463,21.1795877232599,-1.37028192809016));
#10434=CARTESIAN_POINT('Ctrl Pts',(0.796050318315879,21.3879210565933,-1.15698088816278));
#10435=CARTESIAN_POINT('Ctrl Pts',(1.10606241295736,21.5962543899266,-0.943679848235579));
#10436=CARTESIAN_POINT('Ctrl Pts',(1.26789024243365,21.8045877232599,-0.603949681684177));
#10437=CARTESIAN_POINT('Ctrl Pts',(1.42971807190994,22.0129210565933,-0.264219515132783));
#10438=CARTESIAN_POINT('Ctrl Pts',(1.4,22.2212543899266,0.110909354270855));
#10439=CARTESIAN_POINT('Ctrl Pts',(1.37028192809006,22.42958772326,0.486038223674372));
#10440=CARTESIAN_POINT('Ctrl Pts',(1.15698088816276,22.6379210565933,0.796050318315892));
#10441=CARTESIAN_POINT('Ctrl Pts',(0.943679848235495,22.8462543899266,1.10606241295731));
#10442=CARTESIAN_POINT('Ctrl Pts',(0.603949681684078,23.0545877232599,1.26789024243363));
#10443=CARTESIAN_POINT('Ctrl Pts',(0.264219515132726,23.2629210565933,1.42971807190989));
#10444=CARTESIAN_POINT('Ctrl Pts',(-0.110909354270889,23.4712543899266,
1.39999999999997));
#10445=CARTESIAN_POINT('Ctrl Pts',(-0.48603822367442,23.6795877232599,1.37028192808997));
#10446=CARTESIAN_POINT('Ctrl Pts',(-0.796050318315921,23.8879210565932,
1.15698088816274));
#10447=CARTESIAN_POINT('Ctrl Pts',(-1.10606241295736,24.0962543899266,0.943679848235433));
#10448=CARTESIAN_POINT('Ctrl Pts',(-1.26789024243367,24.3045877232599,0.603949681684089));
#10449=CARTESIAN_POINT('Ctrl Pts',(-1.42971807190992,24.5129210565933,0.264219515132643));
#10450=CARTESIAN_POINT('Ctrl Pts',(-1.40000000000002,24.7212543899266,-0.110909354270923));
#10451=CARTESIAN_POINT('Ctrl Pts',(-1.37028192809004,24.9295877232599,-0.486038223674528));
#10452=CARTESIAN_POINT('Ctrl Pts',(-1.1569808881628,25.1379210565933,-0.796050318315996));
#10453=CARTESIAN_POINT('Ctrl Pts',(-0.943679848235474,25.3462543899266,
-1.10606241295742));
#10454=CARTESIAN_POINT('Ctrl Pts',(-0.60394968168412,25.5545877232599,-1.26789024243365));
#10455=CARTESIAN_POINT('Ctrl Pts',(-0.264219515132702,25.7629210565933,
-1.42971807191003));
#10456=CARTESIAN_POINT('Ctrl Pts',(0.110909354270847,25.9712543899266,-1.40000000000008));
#10457=CARTESIAN_POINT('Ctrl Pts',(0.486038223674463,26.17958772326,-1.37028192809014));
#10458=CARTESIAN_POINT('Ctrl Pts',(0.7960503183159,26.3879210565933,-1.15698088816279));
#10459=CARTESIAN_POINT('Ctrl Pts',(1.10606241295738,26.5962543899266,-0.943679848235541));
#10460=CARTESIAN_POINT('Ctrl Pts',(1.26789024243363,26.80458772326,-0.603949681684177));
#10461=CARTESIAN_POINT('Ctrl Pts',(1.42971807190996,27.0129210565933,-0.264219515132761));
#10462=CARTESIAN_POINT('Ctrl Pts',(1.4,27.2212543899266,0.110909354270855));
#10463=CARTESIAN_POINT('Ctrl Pts',(1.37028192809007,27.42958772326,0.486038223674393));
#10464=CARTESIAN_POINT('Ctrl Pts',(1.15698088816278,27.6379210565933,0.796050318315892));
#10465=CARTESIAN_POINT('Ctrl Pts',(0.943679848235495,27.8462543899266,1.10606241295729));
#10466=CARTESIAN_POINT('Ctrl Pts',(0.603949681684099,28.0545877232599,1.26789024243361));
#10467=CARTESIAN_POINT('Ctrl Pts',(0.264219515132724,28.2629210565933,1.42971807190986));
#10468=CARTESIAN_POINT('Ctrl Pts',(-0.110909354270889,28.4712543899266,
1.39999999999997));
#10469=CARTESIAN_POINT('Ctrl Pts',(-0.48603822367442,28.67958772326,1.37028192808997));
#10470=CARTESIAN_POINT('Ctrl Pts',(-0.796050318315921,28.8879210565933,
1.15698088816275));
#10471=CARTESIAN_POINT('Ctrl Pts',(-1.10606241295734,29.0962543899266,0.943679848235406));
#10472=CARTESIAN_POINT('Ctrl Pts',(-1.26789024243365,29.30458772326,0.603949681684083));
#10473=CARTESIAN_POINT('Ctrl Pts',(-1.42971807190992,29.5129210565933,0.264219515132621));
#10474=CARTESIAN_POINT('Ctrl Pts',(-1.40000000000002,29.7212543899266,-0.110909354270923));
#10475=CARTESIAN_POINT('Ctrl Pts',(-1.37028192809006,29.92958772326,-0.486038223674506));
#10476=CARTESIAN_POINT('Ctrl Pts',(-1.1569808881628,30.1379210565933,-0.796050318315996));
#10477=CARTESIAN_POINT('Ctrl Pts',(-0.943679848235495,30.3462543899266,
-1.10606241295744));
#10478=CARTESIAN_POINT('Ctrl Pts',(-0.60394968168412,30.5545877232599,-1.26789024243366));
#10479=CARTESIAN_POINT('Ctrl Pts',(-0.264219515132702,30.7629210565933,
-1.42971807191004));
#10480=CARTESIAN_POINT('Ctrl Pts',(0.110909354270868,30.9712543899266,-1.40000000000007));
#10481=CARTESIAN_POINT('Ctrl Pts',(0.486038223674439,31.17958772326,-1.37028192809015));
#10482=CARTESIAN_POINT('Ctrl Pts',(0.796050318315879,31.3879210565933,-1.15698088816279));
#10483=CARTESIAN_POINT('Ctrl Pts',(1.10606241295736,31.5962543899266,-0.943679848235557));
#10484=CARTESIAN_POINT('Ctrl Pts',(1.26789024243365,31.80458772326,-0.603949681684177));
#10485=CARTESIAN_POINT('Ctrl Pts',(1.42971807190996,32.0129210565933,-0.264219515132783));
#10486=CARTESIAN_POINT('Ctrl Pts',(1.39999999999998,32.2212543899266,0.11090935427085));
#10487=CARTESIAN_POINT('Ctrl Pts',(1.37028192809008,32.42958772326,0.486038223674377));
#10488=CARTESIAN_POINT('Ctrl Pts',(1.15698088816278,32.6379210565933,0.796050318315892));
#10489=CARTESIAN_POINT('Ctrl Pts',(0.943679848235498,32.8462543899267,1.1060624129573));
#10490=CARTESIAN_POINT('Ctrl Pts',(0.603949681684078,33.05458772326,1.26789024243359));
#10491=CARTESIAN_POINT('Ctrl Pts',(0.264219515132705,33.2629210565933,1.4297180719099));
#10492=CARTESIAN_POINT('Ctrl Pts',(-0.110909354270871,33.4712543899267,
1.39999999999998));
#10493=CARTESIAN_POINT('Ctrl Pts',(-0.486038223674439,33.67958772326,1.37028192808999));
#10494=CARTESIAN_POINT('Ctrl Pts',(-0.796050318315921,33.8879210565933,
1.15698088816275));
#10495=CARTESIAN_POINT('Ctrl Pts',(-1.10606241295736,34.0962543899266,0.943679848235417));
#10496=CARTESIAN_POINT('Ctrl Pts',(-1.26789024243367,34.30458772326,0.603949681684083));
#10497=CARTESIAN_POINT('Ctrl Pts',(-1.42971807190994,34.5129210565933,0.264219515132643));
#10498=CARTESIAN_POINT('Ctrl Pts',(-1.4,34.7212543899266,-0.110909354270923));
#10499=CARTESIAN_POINT('Ctrl Pts',(-1.37028192809004,34.92958772326,-0.486038223674517));
#10500=CARTESIAN_POINT('Ctrl Pts',(-1.1569808881628,35.1379210565933,-0.796050318315944));
#10501=CARTESIAN_POINT('Ctrl Pts',(-0.943679848235495,35.3462543899267,
-1.10606241295742));
#10502=CARTESIAN_POINT('Ctrl Pts',(-0.60394968168412,35.55458772326,-1.26789024243366));
#10503=CARTESIAN_POINT('Ctrl Pts',(-0.26421951513268,35.7629210565933,-1.42971807191003));
#10504=CARTESIAN_POINT('Ctrl Pts',(0.110909354270847,35.9712543899266,-1.40000000000004));
#10505=CARTESIAN_POINT('Ctrl Pts',(0.486038223674442,36.17958772326,-1.37028192809012));
#10506=CARTESIAN_POINT('Ctrl Pts',(0.796050318315903,36.3879210565933,-1.15698088816279));
#10507=CARTESIAN_POINT('Ctrl Pts',(1.10606241295738,36.5962543899266,-0.943679848235568));
#10508=CARTESIAN_POINT('Ctrl Pts',(1.26789024243365,36.80458772326,-0.603949681684162));
#10509=CARTESIAN_POINT('Ctrl Pts',(1.42971807190994,37.0129210565933,-0.264219515132788));
#10510=CARTESIAN_POINT('Ctrl Pts',(1.4,37.2212543899267,0.110909354270845));
#10511=CARTESIAN_POINT('Ctrl Pts',(1.37028192809007,37.42958772326,0.486038223674372));
#10512=CARTESIAN_POINT('Ctrl Pts',(1.15698088816278,37.6379210565933,0.796050318315845));
#10513=CARTESIAN_POINT('Ctrl Pts',(0.943679848235495,37.8462543899266,1.1060624129573));
#10514=CARTESIAN_POINT('Ctrl Pts',(0.603949681684099,38.05458772326,1.26789024243359));
#10515=CARTESIAN_POINT('Ctrl Pts',(0.264219515132702,38.2629210565934,1.42971807190987));
#10516=CARTESIAN_POINT('Ctrl Pts',(-0.110909354270891,38.4712543899267,
1.39999999999999));
#10517=CARTESIAN_POINT('Ctrl Pts',(-0.486038223674442,38.67958772326,1.37028192808997));
#10518=CARTESIAN_POINT('Ctrl Pts',(-0.796050318315942,38.8879210565933,
1.15698088816275));
#10519=CARTESIAN_POINT('Ctrl Pts',(-1.10606241295734,39.0962543899267,0.943679848235401));
#10520=CARTESIAN_POINT('Ctrl Pts',(-1.26789024243367,39.30458772326,0.603949681684089));
#10521=CARTESIAN_POINT('Ctrl Pts',(-1.42971807190992,39.5129210565933,0.264219515132632));
#10522=CARTESIAN_POINT('Ctrl Pts',(-1.40000000000002,39.7212543899266,-0.110909354270923));
#10523=CARTESIAN_POINT('Ctrl Pts',(-2.,-0.27874561007344,-0.110909354270924));
#10524=CARTESIAN_POINT('Ctrl Pts',(-1.97028192809006,-0.0704122767402082,
-0.646807739133109));
#10525=CARTESIAN_POINT('Ctrl Pts',(-1.67659613043344,0.137921056593222,
-1.0960503183159));
#10526=CARTESIAN_POINT('Ctrl Pts',(-1.38291033277682,0.346254389926512,
-1.54529289749873));
#10527=CARTESIAN_POINT('Ctrl Pts',(-0.903949681684104,0.554587723259871,
-1.78750548470438));
#10528=CARTESIAN_POINT('Ctrl Pts',(-0.424989030591367,0.762921056593226,
-2.02971807190993));
#10529=CARTESIAN_POINT('Ctrl Pts',(0.110909354270878,0.971254389926561,
-2.00000000000006));
#10530=CARTESIAN_POINT('Ctrl Pts',(0.646807739133123,1.17958772325984,-1.97028192809007));
#10531=CARTESIAN_POINT('Ctrl Pts',(1.09605031831591,1.38792105659322,-1.67659613043344));
#10532=CARTESIAN_POINT('Ctrl Pts',(1.54529289749868,1.59625438992652,-1.38291033277687));
#10533=CARTESIAN_POINT('Ctrl Pts',(1.78750548470428,1.80458772325989,-0.903949681684113));
#10534=CARTESIAN_POINT('Ctrl Pts',(2.02971807190996,2.01292105659317,-0.42498903059139));
#10535=CARTESIAN_POINT('Ctrl Pts',(2.,2.22125438992656,0.110909354270855));
#10536=CARTESIAN_POINT('Ctrl Pts',(1.97028192809007,2.42958772325984,0.646807739133102));
#10537=CARTESIAN_POINT('Ctrl Pts',(1.67659613043345,2.63792105659317,1.09605031831587));
#10538=CARTESIAN_POINT('Ctrl Pts',(1.38291033277682,2.8462543899265,1.54529289749866));
#10539=CARTESIAN_POINT('Ctrl Pts',(0.903949681684104,3.0545877232599,1.78750548470426));
#10540=CARTESIAN_POINT('Ctrl Pts',(0.424989030591383,3.26292105659317,2.02971807190993));
#10541=CARTESIAN_POINT('Ctrl Pts',(-0.11090935427085,3.47125438992654,1.99999999999995));
#10542=CARTESIAN_POINT('Ctrl Pts',(-0.646807739133109,3.67958772325983,
1.97028192809007));
#10543=CARTESIAN_POINT('Ctrl Pts',(-1.0960503183159,3.88792105659323,1.67659613043343));
#10544=CARTESIAN_POINT('Ctrl Pts',(-1.54529289749868,4.09625438992648,1.38291033277681));
#10545=CARTESIAN_POINT('Ctrl Pts',(-1.78750548470431,4.30458772325989,0.903949681684051));
#10546=CARTESIAN_POINT('Ctrl Pts',(-2.02971807190994,4.51292105659318,0.424989030591333));
#10547=CARTESIAN_POINT('Ctrl Pts',(-2.,4.72125438992654,-0.110909354270966));
#10548=CARTESIAN_POINT('Ctrl Pts',(-1.97028192809006,4.92958772325984,-0.646807739133087));
#10549=CARTESIAN_POINT('Ctrl Pts',(-1.67659613043343,5.13792105659321,-1.09605031831595));
#10550=CARTESIAN_POINT('Ctrl Pts',(-1.38291033277682,5.34625438992653,-1.54529289749872));
#10551=CARTESIAN_POINT('Ctrl Pts',(-0.903949681684091,5.5545877232599,-1.78750548470436));
#10552=CARTESIAN_POINT('Ctrl Pts',(-0.424989030591382,5.76292105659322,
-2.02971807190993));
#10553=CARTESIAN_POINT('Ctrl Pts',(0.110909354270865,5.97125438992659,-2.00000000000009));
#10554=CARTESIAN_POINT('Ctrl Pts',(0.64680773913311,6.17958772325983,-1.97028192809005));
#10555=CARTESIAN_POINT('Ctrl Pts',(1.0960503183159,6.38792105659326,-1.67659613043349));
#10556=CARTESIAN_POINT('Ctrl Pts',(1.54529289749868,6.5962543899265,-1.38291033277683));
#10557=CARTESIAN_POINT('Ctrl Pts',(1.7875054847043,6.80458772325989,-0.903949681684162));
#10558=CARTESIAN_POINT('Ctrl Pts',(2.02971807190991,7.01292105659322,-0.424989030591398));
#10559=CARTESIAN_POINT('Ctrl Pts',(2.,7.22125438992656,0.110909354270862));
#10560=CARTESIAN_POINT('Ctrl Pts',(1.97028192809006,7.42958772325989,0.646807739133109));
#10561=CARTESIAN_POINT('Ctrl Pts',(1.67659613043344,7.63792105659322,1.09605031831585));
#10562=CARTESIAN_POINT('Ctrl Pts',(1.38291033277683,7.84625438992656,1.54529289749869));
#10563=CARTESIAN_POINT('Ctrl Pts',(0.903949681684104,8.05458772325989,1.78750548470431));
#10564=CARTESIAN_POINT('Ctrl Pts',(0.424989030591398,8.26292105659318,2.02971807190991));
#10565=CARTESIAN_POINT('Ctrl Pts',(-0.110909354270878,8.47125438992655,
1.99999999999995));
#10566=CARTESIAN_POINT('Ctrl Pts',(-0.646807739133123,8.67958772325983,
1.97028192809004));
#10567=CARTESIAN_POINT('Ctrl Pts',(-1.0960503183159,8.88792105659324,1.67659613043339));
#10568=CARTESIAN_POINT('Ctrl Pts',(-1.54529289749868,9.0962543899265,1.38291033277682));
#10569=CARTESIAN_POINT('Ctrl Pts',(-1.78750548470431,9.3045877232599,0.903949681684085));
#10570=CARTESIAN_POINT('Ctrl Pts',(-2.02971807190993,9.51292105659317,0.424989030591355));
#10571=CARTESIAN_POINT('Ctrl Pts',(-2.,9.72125438992657,-0.110909354270924));
#10572=CARTESIAN_POINT('Ctrl Pts',(-1.97028192809007,9.92958772325983,-0.646807739133123));
#10573=CARTESIAN_POINT('Ctrl Pts',(-1.67659613043344,10.1379210565932,-1.09605031831599));
#10574=CARTESIAN_POINT('Ctrl Pts',(-1.38291033277681,10.3462543899265,-1.54529289749875));
#10575=CARTESIAN_POINT('Ctrl Pts',(-0.903949681684116,10.5545877232599,
-1.78750548470438));
#10576=CARTESIAN_POINT('Ctrl Pts',(-0.424989030591382,10.7629210565932,
-2.02971807190998));
#10577=CARTESIAN_POINT('Ctrl Pts',(0.110909354270878,10.9712543899266,-2.00000000000009));
#10578=CARTESIAN_POINT('Ctrl Pts',(0.646807739133123,11.1795877232599,-1.97028192809007));
#10579=CARTESIAN_POINT('Ctrl Pts',(1.09605031831591,11.3879210565932,-1.67659613043351));
#10580=CARTESIAN_POINT('Ctrl Pts',(1.54529289749868,11.5962543899265,-1.38291033277682));
#10581=CARTESIAN_POINT('Ctrl Pts',(1.78750548470431,11.8045877232599,-0.903949681684182));
#10582=CARTESIAN_POINT('Ctrl Pts',(2.02971807190993,12.0129210565932,-0.424989030591383));
#10583=CARTESIAN_POINT('Ctrl Pts',(2.,12.2212543899266,0.110909354270862));
#10584=CARTESIAN_POINT('Ctrl Pts',(1.97028192809007,12.4295877232599,0.646807739133051));
#10585=CARTESIAN_POINT('Ctrl Pts',(1.67659613043345,12.6379210565932,1.09605031831589));
#10586=CARTESIAN_POINT('Ctrl Pts',(1.38291033277683,12.8462543899266,1.54529289749867));
#10587=CARTESIAN_POINT('Ctrl Pts',(0.903949681684118,13.0545877232599,1.78750548470425));
#10588=CARTESIAN_POINT('Ctrl Pts',(0.424989030591382,13.2629210565932,2.02971807190993));
#10589=CARTESIAN_POINT('Ctrl Pts',(-0.110909354270864,13.4712543899266,
1.99999999999997));
#10590=CARTESIAN_POINT('Ctrl Pts',(-0.646807739133109,13.6795877232599,
1.97028192809006));
#10591=CARTESIAN_POINT('Ctrl Pts',(-1.0960503183159,13.8879210565932,1.67659613043339));
#10592=CARTESIAN_POINT('Ctrl Pts',(-1.54529289749868,14.0962543899266,1.38291033277682));
#10593=CARTESIAN_POINT('Ctrl Pts',(-1.7875054847043,14.3045877232599,0.903949681684092));
#10594=CARTESIAN_POINT('Ctrl Pts',(-2.02971807190993,14.5129210565932,0.424989030591326));
#10595=CARTESIAN_POINT('Ctrl Pts',(-2.,14.7212543899266,-0.110909354270938));
#10596=CARTESIAN_POINT('Ctrl Pts',(-1.97028192809006,14.9295877232599,-0.646807739133109));
#10597=CARTESIAN_POINT('Ctrl Pts',(-1.67659613043344,15.1379210565933,-1.09605031831595));
#10598=CARTESIAN_POINT('Ctrl Pts',(-1.38291033277683,15.3462543899265,-1.54529289749874));
#10599=CARTESIAN_POINT('Ctrl Pts',(-0.903949681684104,15.5545877232599,
-1.78750548470439));
#10600=CARTESIAN_POINT('Ctrl Pts',(-0.424989030591382,15.7629210565932,
-2.02971807190993));
#10601=CARTESIAN_POINT('Ctrl Pts',(0.110909354270852,15.9712543899266,-2.00000000000006));
#10602=CARTESIAN_POINT('Ctrl Pts',(0.646807739133109,16.1795877232599,-1.97028192809006));
#10603=CARTESIAN_POINT('Ctrl Pts',(1.0960503183159,16.3879210565933,-1.67659613043349));
#10604=CARTESIAN_POINT('Ctrl Pts',(1.5452928974987,16.5962543899265,-1.38291033277688));
#10605=CARTESIAN_POINT('Ctrl Pts',(1.78750548470431,16.8045877232599,-0.903949681684148));
#10606=CARTESIAN_POINT('Ctrl Pts',(2.02971807190993,17.0129210565932,-0.424989030591383));
#10607=CARTESIAN_POINT('Ctrl Pts',(2.,17.2212543899266,0.110909354270813));
#10608=CARTESIAN_POINT('Ctrl Pts',(1.97028192809007,17.4295877232599,0.646807739133109));
#10609=CARTESIAN_POINT('Ctrl Pts',(1.67659613043345,17.6379210565933,1.09605031831585));
#10610=CARTESIAN_POINT('Ctrl Pts',(1.38291033277684,17.8462543899265,1.54529289749865));
#10611=CARTESIAN_POINT('Ctrl Pts',(0.903949681684104,18.0545877232599,1.78750548470431));
#10612=CARTESIAN_POINT('Ctrl Pts',(0.424989030591369,18.2629210565932,2.02971807190994));
#10613=CARTESIAN_POINT('Ctrl Pts',(-0.110909354270865,18.4712543899266,
2.));
#10614=CARTESIAN_POINT('Ctrl Pts',(-0.646807739133109,18.6795877232599,
1.97028192809006));
#10615=CARTESIAN_POINT('Ctrl Pts',(-1.0960503183159,18.8879210565933,1.6765961304334));
#10616=CARTESIAN_POINT('Ctrl Pts',(-1.54529289749867,19.0962543899266,1.38291033277682));
#10617=CARTESIAN_POINT('Ctrl Pts',(-1.78750548470431,19.3045877232599,0.903949681684071));
#10618=CARTESIAN_POINT('Ctrl Pts',(-2.02971807190993,19.5129210565932,0.42498903059134));
#10619=CARTESIAN_POINT('Ctrl Pts',(-2.,19.7212543899266,-0.110909354270924));
#10620=CARTESIAN_POINT('Ctrl Pts',(-1.97028192809006,19.9295877232599,-0.646807739133152));
#10621=CARTESIAN_POINT('Ctrl Pts',(-1.67659613043345,20.1379210565933,-1.09605031831597));
#10622=CARTESIAN_POINT('Ctrl Pts',(-1.38291033277682,20.3462543899266,-1.54529289749875));
#10623=CARTESIAN_POINT('Ctrl Pts',(-0.903949681684103,20.5545877232599,
-1.78750548470438));
#10624=CARTESIAN_POINT('Ctrl Pts',(-0.424989030591367,20.7629210565932,
-2.02971807190997));
#10625=CARTESIAN_POINT('Ctrl Pts',(0.110909354270864,20.9712543899266,-2.0000000000001));
#10626=CARTESIAN_POINT('Ctrl Pts',(0.64680773913311,21.1795877232599,-1.97028192809011));
#10627=CARTESIAN_POINT('Ctrl Pts',(1.0960503183159,21.3879210565933,-1.67659613043352));
#10628=CARTESIAN_POINT('Ctrl Pts',(1.54529289749868,21.5962543899266,-1.38291033277682));
#10629=CARTESIAN_POINT('Ctrl Pts',(1.78750548470431,21.8045877232599,-0.90394968168419));
#10630=CARTESIAN_POINT('Ctrl Pts',(2.02971807190991,22.0129210565932,-0.42498903059139));
#10631=CARTESIAN_POINT('Ctrl Pts',(2.,22.2212543899266,0.110909354270855));
#10632=CARTESIAN_POINT('Ctrl Pts',(1.9702819280901,22.4295877232599,0.646807739133087));
#10633=CARTESIAN_POINT('Ctrl Pts',(1.67659613043345,22.6379210565933,1.09605031831588));
#10634=CARTESIAN_POINT('Ctrl Pts',(1.38291033277683,22.8462543899266,1.54529289749862));
#10635=CARTESIAN_POINT('Ctrl Pts',(0.903949681684118,23.0545877232599,1.78750548470426));
#10636=CARTESIAN_POINT('Ctrl Pts',(0.424989030591383,23.2629210565932,2.02971807190993));
#10637=CARTESIAN_POINT('Ctrl Pts',(-0.110909354270864,23.4712543899266,
1.99999999999997));
#10638=CARTESIAN_POINT('Ctrl Pts',(-0.646807739133109,23.6795877232599,
1.97028192809003));
#10639=CARTESIAN_POINT('Ctrl Pts',(-1.09605031831588,23.8879210565933,1.67659613043339));
#10640=CARTESIAN_POINT('Ctrl Pts',(-1.54529289749869,24.0962543899266,1.38291033277682));
#10641=CARTESIAN_POINT('Ctrl Pts',(-1.78750548470431,24.3045877232599,0.903949681684092));
#10642=CARTESIAN_POINT('Ctrl Pts',(-2.02971807190995,24.5129210565932,0.424989030591319));
#10643=CARTESIAN_POINT('Ctrl Pts',(-2.,24.7212543899266,-0.110909354270938));
#10644=CARTESIAN_POINT('Ctrl Pts',(-1.97028192809005,24.9295877232599,-0.646807739133109));
#10645=CARTESIAN_POINT('Ctrl Pts',(-1.67659613043344,25.1379210565933,-1.09605031831594));
#10646=CARTESIAN_POINT('Ctrl Pts',(-1.38291033277682,25.3462543899266,-1.54529289749872));
#10647=CARTESIAN_POINT('Ctrl Pts',(-0.903949681684104,25.55458772326,-1.7875054847044));
#10648=CARTESIAN_POINT('Ctrl Pts',(-0.424989030591382,25.7629210565933,
-2.02971807190993));
#10649=CARTESIAN_POINT('Ctrl Pts',(0.110909354270864,25.9712543899266,-2.00000000000006));
#10650=CARTESIAN_POINT('Ctrl Pts',(0.646807739133109,26.1795877232599,-1.97028192809006));
#10651=CARTESIAN_POINT('Ctrl Pts',(1.0960503183159,26.3879210565933,-1.67659613043348));
#10652=CARTESIAN_POINT('Ctrl Pts',(1.5452928974987,26.5962543899266,-1.38291033277687));
#10653=CARTESIAN_POINT('Ctrl Pts',(1.78750548470431,26.80458772326,-0.903949681684155));
#10654=CARTESIAN_POINT('Ctrl Pts',(2.02971807190993,27.0129210565933,-0.424989030591383));
#10655=CARTESIAN_POINT('Ctrl Pts',(2.00000000000003,27.2212543899266,0.11090935427082));
#10656=CARTESIAN_POINT('Ctrl Pts',(1.97028192809007,27.4295877232599,0.646807739133109));
#10657=CARTESIAN_POINT('Ctrl Pts',(1.67659613043345,27.6379210565933,1.09605031831587));
#10658=CARTESIAN_POINT('Ctrl Pts',(1.38291033277684,27.8462543899266,1.54529289749868));
#10659=CARTESIAN_POINT('Ctrl Pts',(0.903949681684103,28.0545877232599,1.78750548470431));
#10660=CARTESIAN_POINT('Ctrl Pts',(0.424989030591382,28.2629210565932,2.02971807190993));
#10661=CARTESIAN_POINT('Ctrl Pts',(-0.110909354270852,28.4712543899266,
1.99999999999998));
#10662=CARTESIAN_POINT('Ctrl Pts',(-0.646807739133109,28.6795877232599,
1.97028192809006));
#10663=CARTESIAN_POINT('Ctrl Pts',(-1.0960503183159,28.8879210565933,1.67659613043341));
#10664=CARTESIAN_POINT('Ctrl Pts',(-1.54529289749868,29.0962543899266,1.38291033277682));
#10665=CARTESIAN_POINT('Ctrl Pts',(-1.78750548470432,29.30458772326,0.903949681684071));
#10666=CARTESIAN_POINT('Ctrl Pts',(-2.02971807190993,29.5129210565933,0.42498903059134));
#10667=CARTESIAN_POINT('Ctrl Pts',(-2.,29.7212543899266,-0.110909354270917));
#10668=CARTESIAN_POINT('Ctrl Pts',(-1.97028192809006,29.9295877232599,-0.646807739133087));
#10669=CARTESIAN_POINT('Ctrl Pts',(-1.67659613043345,30.1379210565933,-1.09605031831597));
#10670=CARTESIAN_POINT('Ctrl Pts',(-1.38291033277683,30.3462543899266,-1.54529289749872));
#10671=CARTESIAN_POINT('Ctrl Pts',(-0.903949681684103,30.55458772326,-1.78750548470437));
#10672=CARTESIAN_POINT('Ctrl Pts',(-0.424989030591367,30.7629210565933,
-2.02971807190996));
#10673=CARTESIAN_POINT('Ctrl Pts',(0.110909354270865,30.9712543899266,-2.00000000000009));
#10674=CARTESIAN_POINT('Ctrl Pts',(0.646807739133123,31.1795877232599,-1.97028192809004));
#10675=CARTESIAN_POINT('Ctrl Pts',(1.0960503183159,31.3879210565933,-1.67659613043352));
#10676=CARTESIAN_POINT('Ctrl Pts',(1.54529289749868,31.5962543899266,-1.38291033277685));
#10677=CARTESIAN_POINT('Ctrl Pts',(1.78750548470431,31.80458772326,-0.903949681684169));
#10678=CARTESIAN_POINT('Ctrl Pts',(2.02971807190993,32.0129210565933,-0.424989030591419));
#10679=CARTESIAN_POINT('Ctrl Pts',(2.,32.2212543899266,0.110909354270869));
#10680=CARTESIAN_POINT('Ctrl Pts',(1.97028192809004,32.4295877232599,0.646807739133087));
#10681=CARTESIAN_POINT('Ctrl Pts',(1.67659613043345,32.6379210565933,1.09605031831587));
#10682=CARTESIAN_POINT('Ctrl Pts',(1.38291033277682,32.8462543899266,1.54529289749868));
#10683=CARTESIAN_POINT('Ctrl Pts',(0.903949681684104,33.0545877232599,1.78750548470431));
#10684=CARTESIAN_POINT('Ctrl Pts',(0.424989030591383,33.2629210565932,2.02971807190993));
#10685=CARTESIAN_POINT('Ctrl Pts',(-0.110909354270864,33.4712543899267,
1.99999999999997));
#10686=CARTESIAN_POINT('Ctrl Pts',(-0.646807739133109,33.6795877232599,
1.97028192809004));
#10687=CARTESIAN_POINT('Ctrl Pts',(-1.09605031831588,33.8879210565934,1.6765961304334));
#10688=CARTESIAN_POINT('Ctrl Pts',(-1.54529289749868,34.0962543899266,1.38291033277683));
#10689=CARTESIAN_POINT('Ctrl Pts',(-1.78750548470431,34.30458772326,0.903949681684037));
#10690=CARTESIAN_POINT('Ctrl Pts',(-2.02971807190994,34.5129210565932,0.424989030591383));
#10691=CARTESIAN_POINT('Ctrl Pts',(-2.,34.7212543899267,-0.110909354270938));
#10692=CARTESIAN_POINT('Ctrl Pts',(-1.97028192809006,34.9295877232599,-0.646807739133123));
#10693=CARTESIAN_POINT('Ctrl Pts',(-1.67659613043344,35.1379210565933,-1.09605031831594));
#10694=CARTESIAN_POINT('Ctrl Pts',(-1.38291033277682,35.3462543899267,-1.54529289749875));
#10695=CARTESIAN_POINT('Ctrl Pts',(-0.903949681684103,35.55458772326,-1.78750548470439));
#10696=CARTESIAN_POINT('Ctrl Pts',(-0.424989030591382,35.7629210565932,
-2.02971807190993));
#10697=CARTESIAN_POINT('Ctrl Pts',(0.110909354270864,35.9712543899267,-2.00000000000003));
#10698=CARTESIAN_POINT('Ctrl Pts',(0.64680773913311,36.1795877232599,-1.97028192809006));
#10699=CARTESIAN_POINT('Ctrl Pts',(1.0960503183159,36.3879210565933,-1.67659613043348));
#10700=CARTESIAN_POINT('Ctrl Pts',(1.54529289749869,36.5962543899266,-1.38291033277682));
#10701=CARTESIAN_POINT('Ctrl Pts',(1.78750548470431,36.80458772326,-0.903949681684127));
#10702=CARTESIAN_POINT('Ctrl Pts',(2.02971807190993,37.0129210565932,-0.424989030591383));
#10703=CARTESIAN_POINT('Ctrl Pts',(2.,37.2212543899267,0.110909354270834));
#10704=CARTESIAN_POINT('Ctrl Pts',(1.97028192809006,37.4295877232599,0.646807739133109));
#10705=CARTESIAN_POINT('Ctrl Pts',(1.67659613043345,37.6379210565933,1.09605031831588));
#10706=CARTESIAN_POINT('Ctrl Pts',(1.38291033277681,37.8462543899266,1.54529289749865));
#10707=CARTESIAN_POINT('Ctrl Pts',(0.903949681684104,38.0545877232599,1.78750548470431));
#10708=CARTESIAN_POINT('Ctrl Pts',(0.424989030591383,38.2629210565933,2.02971807190991));
#10709=CARTESIAN_POINT('Ctrl Pts',(-0.11090935427085,38.4712543899266,1.99999999999995));
#10710=CARTESIAN_POINT('Ctrl Pts',(-0.64680773913311,38.67958772326,1.97028192809006));
#10711=CARTESIAN_POINT('Ctrl Pts',(-1.0960503183159,38.8879210565933,1.67659613043344));
#10712=CARTESIAN_POINT('Ctrl Pts',(-1.54529289749868,39.0962543899266,1.38291033277682));
#10713=CARTESIAN_POINT('Ctrl Pts',(-1.78750548470431,39.30458772326,0.903949681684064));
#10714=CARTESIAN_POINT('Ctrl Pts',(-2.02971807190993,39.5129210565932,0.424989030591369));
#10715=CARTESIAN_POINT('Ctrl Pts',(-2.,39.7212543899267,-0.110909354270917));
#10716=CARTESIAN_POINT('Ctrl Pts',(-2.6,-0.278745610073447,-0.11090935427086));
#10717=CARTESIAN_POINT('Ctrl Pts',(-2.57028192809005,-0.0704122767401095,
-0.807577254591869));
#10718=CARTESIAN_POINT('Ctrl Pts',(-2.19621137270411,0.137921056593207,
-1.39605031831597));
#10719=CARTESIAN_POINT('Ctrl Pts',(-1.82214081731814,0.346254389926554,
-1.98452338204009));
#10720=CARTESIAN_POINT('Ctrl Pts',(-1.20394968168411,0.554587723259855,
-2.30712072697501));
#10721=CARTESIAN_POINT('Ctrl Pts',(-0.585758546050059,0.762921056593228,
-2.62971807191003));
#10722=CARTESIAN_POINT('Ctrl Pts',(0.11090935427086,0.971254389926535,-2.60000000000008));
#10723=CARTESIAN_POINT('Ctrl Pts',(0.807577254591799,1.17958772325987,-2.57028192809015));
#10724=CARTESIAN_POINT('Ctrl Pts',(1.39605031831589,1.38792105659322,-2.19621137270419));
#10725=CARTESIAN_POINT('Ctrl Pts',(1.98452338204001,1.59625438992655,-1.82214081731816));
#10726=CARTESIAN_POINT('Ctrl Pts',(2.30712072697495,1.80458772325989,-1.20394968168416));
#10727=CARTESIAN_POINT('Ctrl Pts',(2.62971807190993,2.01292105659322,-0.585758546050151));
#10728=CARTESIAN_POINT('Ctrl Pts',(2.59999999999998,2.22125438992652,0.110909354270808));
#10729=CARTESIAN_POINT('Ctrl Pts',(2.57028192809007,2.42958772325989,0.807577254591686));
#10730=CARTESIAN_POINT('Ctrl Pts',(2.19621137270409,2.63792105659321,1.39605031831586));
#10731=CARTESIAN_POINT('Ctrl Pts',(1.82214081731816,2.84625438992655,1.98452338203998));
#10732=CARTESIAN_POINT('Ctrl Pts',(1.20394968168409,3.05458772325989,2.30712072697489));
#10733=CARTESIAN_POINT('Ctrl Pts',(0.585758546050062,3.26292105659321,2.62971807190987));
#10734=CARTESIAN_POINT('Ctrl Pts',(-0.11090935427086,3.47125438992654,2.59999999999991));
#10735=CARTESIAN_POINT('Ctrl Pts',(-0.807577254591778,3.67958772325991,
2.57028192809));
#10736=CARTESIAN_POINT('Ctrl Pts',(-1.39605031831589,3.8879210565932,2.19621137270409));
#10737=CARTESIAN_POINT('Ctrl Pts',(-1.98452338203998,4.09625438992658,1.82214081731811));
#10738=CARTESIAN_POINT('Ctrl Pts',(-2.30712072697499,4.30458772325988,1.20394968168402));
#10739=CARTESIAN_POINT('Ctrl Pts',(-2.62971807190992,4.51292105659321,0.585758546049978));
#10740=CARTESIAN_POINT('Ctrl Pts',(-2.6,4.72125438992652,-0.110909354270855));
#10741=CARTESIAN_POINT('Ctrl Pts',(-2.57028192809005,4.92958772325988,-0.807577254591864));
#10742=CARTESIAN_POINT('Ctrl Pts',(-2.19621137270413,5.13792105659322,-1.39605031831589));
#10743=CARTESIAN_POINT('Ctrl Pts',(-1.82214081731815,5.34625438992655,-1.98452338204009));
#10744=CARTESIAN_POINT('Ctrl Pts',(-1.20394968168413,5.55458772325989,-2.30712072697498));
#10745=CARTESIAN_POINT('Ctrl Pts',(-0.585758546050059,5.76292105659322,
-2.62971807191006));
#10746=CARTESIAN_POINT('Ctrl Pts',(0.110909354270839,5.97125438992656,-2.6));
#10747=CARTESIAN_POINT('Ctrl Pts',(0.807577254591799,6.1795877232599,-2.57028192809015));
#10748=CARTESIAN_POINT('Ctrl Pts',(1.39605031831589,6.38792105659324,-2.19621137270419));
#10749=CARTESIAN_POINT('Ctrl Pts',(1.98452338204003,6.59625438992657,-1.82214081731824));
#10750=CARTESIAN_POINT('Ctrl Pts',(2.30712072697497,6.80458772325989,-1.20394968168419));
#10751=CARTESIAN_POINT('Ctrl Pts',(2.62971807190993,7.01292105659322,-0.58575854605014));
#10752=CARTESIAN_POINT('Ctrl Pts',(2.6,7.22125438992658,0.110909354270855));
#10753=CARTESIAN_POINT('Ctrl Pts',(2.57028192809009,7.42958772325989,0.807577254591767));
#10754=CARTESIAN_POINT('Ctrl Pts',(2.19621137270411,7.63792105659324,1.39605031831581));
#10755=CARTESIAN_POINT('Ctrl Pts',(1.82214081731816,7.84625438992655,1.98452338203995));
#10756=CARTESIAN_POINT('Ctrl Pts',(1.20394968168409,8.05458772325989,2.30712072697495));
#10757=CARTESIAN_POINT('Ctrl Pts',(0.585758546050062,8.26292105659324,2.62971807190983));
#10758=CARTESIAN_POINT('Ctrl Pts',(-0.11090935427086,8.47125438992656,2.59999999999999));
#10759=CARTESIAN_POINT('Ctrl Pts',(-0.807577254591772,8.67958772325989,
2.57028192809002));
#10760=CARTESIAN_POINT('Ctrl Pts',(-1.39605031831589,8.88792105659322,2.1962113727041));
#10761=CARTESIAN_POINT('Ctrl Pts',(-1.98452338203998,9.09625438992657,1.82214081731807));
#10762=CARTESIAN_POINT('Ctrl Pts',(-2.30712072697499,9.30458772325988,1.20394968168402));
#10763=CARTESIAN_POINT('Ctrl Pts',(-2.62971807190992,9.51292105659323,0.585758546050059));
#10764=CARTESIAN_POINT('Ctrl Pts',(-2.6,9.72125438992655,-0.11090935427086));
#10765=CARTESIAN_POINT('Ctrl Pts',(-2.57028192809007,9.92958772325989,-0.80757725459195));
#10766=CARTESIAN_POINT('Ctrl Pts',(-2.19621137270412,10.1379210565932,-1.39605031831597));
#10767=CARTESIAN_POINT('Ctrl Pts',(-1.82214081731816,10.3462543899266,-1.98452338204001));
#10768=CARTESIAN_POINT('Ctrl Pts',(-1.20394968168413,10.5545877232599,-2.30712072697498));
#10769=CARTESIAN_POINT('Ctrl Pts',(-0.585758546050059,10.7629210565933,
-2.62971807191005));
#10770=CARTESIAN_POINT('Ctrl Pts',(0.11090935427086,10.9712543899266,-2.6));
#10771=CARTESIAN_POINT('Ctrl Pts',(0.80757725459178,11.1795877232599,-2.57028192809015));
#10772=CARTESIAN_POINT('Ctrl Pts',(1.39605031831587,11.3879210565932,-2.19621137270419));
#10773=CARTESIAN_POINT('Ctrl Pts',(1.98452338204001,11.5962543899266,-1.82214081731816));
#10774=CARTESIAN_POINT('Ctrl Pts',(2.30712072697495,11.8045877232599,-1.20394968168419));
#10775=CARTESIAN_POINT('Ctrl Pts',(2.62971807190993,12.0129210565933,-0.585758546050162));
#10776=CARTESIAN_POINT('Ctrl Pts',(2.6,12.2212543899266,0.11090935427085));
#10777=CARTESIAN_POINT('Ctrl Pts',(2.57028192809007,12.4295877232599,0.807577254591702));
#10778=CARTESIAN_POINT('Ctrl Pts',(2.19621137270409,12.6379210565932,1.39605031831582));
#10779=CARTESIAN_POINT('Ctrl Pts',(1.82214081731816,12.8462543899266,1.98452338203998));
#10780=CARTESIAN_POINT('Ctrl Pts',(1.20394968168411,13.0545877232599,2.30712072697493));
#10781=CARTESIAN_POINT('Ctrl Pts',(0.585758546050084,13.2629210565932,2.62971807190985));
#10782=CARTESIAN_POINT('Ctrl Pts',(-0.11090935427086,13.4712543899266,2.59999999999995));
#10783=CARTESIAN_POINT('Ctrl Pts',(-0.807577254591778,13.6795877232599,
2.57028192809));
#10784=CARTESIAN_POINT('Ctrl Pts',(-1.39605031831591,13.8879210565933,2.19621137270409));
#10785=CARTESIAN_POINT('Ctrl Pts',(-1.98452338204001,14.0962543899266,1.82214081731811));
#10786=CARTESIAN_POINT('Ctrl Pts',(-2.30712072697499,14.3045877232599,1.20394968168402));
#10787=CARTESIAN_POINT('Ctrl Pts',(-2.62971807190992,14.5129210565932,0.585758546049984));
#10788=CARTESIAN_POINT('Ctrl Pts',(-2.60000000000002,14.7212543899266,-0.110909354270865));
#10789=CARTESIAN_POINT('Ctrl Pts',(-2.57028192809007,14.9295877232599,-0.807577254591869));
#10790=CARTESIAN_POINT('Ctrl Pts',(-2.19621137270411,15.1379210565932,-1.39605031831597));
#10791=CARTESIAN_POINT('Ctrl Pts',(-1.82214081731815,15.3462543899266,-1.98452338204009));
#10792=CARTESIAN_POINT('Ctrl Pts',(-1.20394968168413,15.5545877232599,-2.30712072697498));
#10793=CARTESIAN_POINT('Ctrl Pts',(-0.58575854605004,15.7629210565933,-2.62971807191003));
#10794=CARTESIAN_POINT('Ctrl Pts',(0.110909354270839,15.9712543899266,-2.6));
#10795=CARTESIAN_POINT('Ctrl Pts',(0.807577254591799,16.1795877232599,-2.57028192809018));
#10796=CARTESIAN_POINT('Ctrl Pts',(1.39605031831589,16.3879210565933,-2.19621137270417));
#10797=CARTESIAN_POINT('Ctrl Pts',(1.98452338204002,16.5962543899266,-1.82214081731817));
#10798=CARTESIAN_POINT('Ctrl Pts',(2.30712072697497,16.8045877232599,-1.20394968168419));
#10799=CARTESIAN_POINT('Ctrl Pts',(2.62971807190995,17.0129210565933,-0.585758546050151));
#10800=CARTESIAN_POINT('Ctrl Pts',(2.59999999999998,17.2212543899266,0.110909354270855));
#10801=CARTESIAN_POINT('Ctrl Pts',(2.57028192809007,17.42958772326,0.807577254591713));
#10802=CARTESIAN_POINT('Ctrl Pts',(2.19621137270409,17.6379210565933,1.39605031831588));
#10803=CARTESIAN_POINT('Ctrl Pts',(1.82214081731816,17.8462543899266,1.98452338203995));
#10804=CARTESIAN_POINT('Ctrl Pts',(1.20394968168411,18.0545877232599,2.30712072697492));
#10805=CARTESIAN_POINT('Ctrl Pts',(0.585758546050062,18.2629210565933,2.62971807190985));
#10806=CARTESIAN_POINT('Ctrl Pts',(-0.11090935427086,18.4712543899266,2.59999999999995));
#10807=CARTESIAN_POINT('Ctrl Pts',(-0.807577254591775,18.6795877232599,
2.57028192809003));
#10808=CARTESIAN_POINT('Ctrl Pts',(-1.39605031831589,18.8879210565933,2.19621137270408));
#10809=CARTESIAN_POINT('Ctrl Pts',(-1.98452338204001,19.0962543899266,1.82214081731808));
#10810=CARTESIAN_POINT('Ctrl Pts',(-2.30712072697499,19.3045877232599,1.2039496816841));
#10811=CARTESIAN_POINT('Ctrl Pts',(-2.62971807190991,19.5129210565933,0.585758546050022));
#10812=CARTESIAN_POINT('Ctrl Pts',(-2.6,19.7212543899266,-0.110909354270865));
#10813=CARTESIAN_POINT('Ctrl Pts',(-2.57028192809005,19.9295877232599,-0.807577254591831));
#10814=CARTESIAN_POINT('Ctrl Pts',(-2.19621137270411,20.1379210565933,-1.39605031831597));
#10815=CARTESIAN_POINT('Ctrl Pts',(-1.82214081731814,20.3462543899266,-1.98452338204008));
#10816=CARTESIAN_POINT('Ctrl Pts',(-1.20394968168413,20.5545877232599,-2.30712072697501));
#10817=CARTESIAN_POINT('Ctrl Pts',(-0.585758546050059,20.7629210565933,
-2.62971807191003));
#10818=CARTESIAN_POINT('Ctrl Pts',(0.110909354270839,20.9712543899266,-2.6));
#10819=CARTESIAN_POINT('Ctrl Pts',(0.80757725459178,21.1795877232599,-2.57028192809016));
#10820=CARTESIAN_POINT('Ctrl Pts',(1.39605031831587,21.3879210565933,-2.19621137270417));
#10821=CARTESIAN_POINT('Ctrl Pts',(1.98452338204003,21.5962543899266,-1.82214081731822));
#10822=CARTESIAN_POINT('Ctrl Pts',(2.30712072697495,21.8045877232599,-1.20394968168419));
#10823=CARTESIAN_POINT('Ctrl Pts',(2.62971807190993,22.0129210565933,-0.585758546050135));
#10824=CARTESIAN_POINT('Ctrl Pts',(2.6,22.2212543899266,0.11090935427085));
#10825=CARTESIAN_POINT('Ctrl Pts',(2.57028192809009,22.42958772326,0.807577254591702));
#10826=CARTESIAN_POINT('Ctrl Pts',(2.19621137270411,22.6379210565933,1.39605031831588));
#10827=CARTESIAN_POINT('Ctrl Pts',(1.82214081731818,22.8462543899266,1.98452338203997));
#10828=CARTESIAN_POINT('Ctrl Pts',(1.20394968168411,23.0545877232599,2.30712072697493));
#10829=CARTESIAN_POINT('Ctrl Pts',(0.585758546050081,23.2629210565933,2.62971807190987));
#10830=CARTESIAN_POINT('Ctrl Pts',(-0.110909354270881,23.4712543899266,
2.59999999999995));
#10831=CARTESIAN_POINT('Ctrl Pts',(-0.807577254591756,23.6795877232599,
2.57028192809001));
#10832=CARTESIAN_POINT('Ctrl Pts',(-1.39605031831591,23.8879210565933,2.19621137270406));
#10833=CARTESIAN_POINT('Ctrl Pts',(-1.98452338204,24.0962543899266,1.82214081731812));
#10834=CARTESIAN_POINT('Ctrl Pts',(-2.30712072697499,24.3045877232599,1.2039496816841));
#10835=CARTESIAN_POINT('Ctrl Pts',(-2.62971807190993,24.5129210565933,0.585758546050016));
#10836=CARTESIAN_POINT('Ctrl Pts',(-2.60000000000002,24.7212543899266,-0.110909354270829));
#10837=CARTESIAN_POINT('Ctrl Pts',(-2.57028192809006,24.92958772326,-0.807577254591853));
#10838=CARTESIAN_POINT('Ctrl Pts',(-2.19621137270413,25.1379210565933,-1.39605031831596));
#10839=CARTESIAN_POINT('Ctrl Pts',(-1.82214081731816,25.3462543899266,-1.98452338204004));
#10840=CARTESIAN_POINT('Ctrl Pts',(-1.20394968168413,25.5545877232599,-2.30712072697501));
#10841=CARTESIAN_POINT('Ctrl Pts',(-0.58575854605004,25.7629210565933,-2.6297180719101));
#10842=CARTESIAN_POINT('Ctrl Pts',(0.110909354270839,25.9712543899266,-2.6));
#10843=CARTESIAN_POINT('Ctrl Pts',(0.807577254591778,26.17958772326,-2.57028192809015));
#10844=CARTESIAN_POINT('Ctrl Pts',(1.39605031831587,26.3879210565933,-2.19621137270417));
#10845=CARTESIAN_POINT('Ctrl Pts',(1.98452338204001,26.5962543899266,-1.82214081731824));
#10846=CARTESIAN_POINT('Ctrl Pts',(2.30712072697495,26.80458772326,-1.2039496816842));
#10847=CARTESIAN_POINT('Ctrl Pts',(2.62971807190995,27.0129210565933,-0.585758546050172));
#10848=CARTESIAN_POINT('Ctrl Pts',(2.6,27.2212543899266,0.110909354270782));
#10849=CARTESIAN_POINT('Ctrl Pts',(2.57028192809007,27.42958772326,0.807577254591718));
#10850=CARTESIAN_POINT('Ctrl Pts',(2.19621137270409,27.6379210565932,1.39605031831588));
#10851=CARTESIAN_POINT('Ctrl Pts',(1.82214081731816,27.8462543899266,1.98452338203995));
#10852=CARTESIAN_POINT('Ctrl Pts',(1.20394968168409,28.05458772326,2.30712072697492));
#10853=CARTESIAN_POINT('Ctrl Pts',(0.585758546050084,28.2629210565933,2.62971807190984));
#10854=CARTESIAN_POINT('Ctrl Pts',(-0.11090935427086,28.4712543899266,2.59999999999994));
#10855=CARTESIAN_POINT('Ctrl Pts',(-0.807577254591778,28.67958772326,2.57028192809003));
#10856=CARTESIAN_POINT('Ctrl Pts',(-1.39605031831591,28.8879210565933,2.19621137270406));
#10857=CARTESIAN_POINT('Ctrl Pts',(-1.98452338204001,29.0962543899266,1.82214081731809));
#10858=CARTESIAN_POINT('Ctrl Pts',(-2.30712072697499,29.3045877232599,1.20394968168406));
#10859=CARTESIAN_POINT('Ctrl Pts',(-2.62971807190993,29.5129210565933,0.58575854605));
#10860=CARTESIAN_POINT('Ctrl Pts',(-2.60000000000002,29.7212543899266,-0.110909354270912));
#10861=CARTESIAN_POINT('Ctrl Pts',(-2.57028192809006,29.92958772326,-0.807577254591837));
#10862=CARTESIAN_POINT('Ctrl Pts',(-2.19621137270411,30.1379210565933,-1.39605031831594));
#10863=CARTESIAN_POINT('Ctrl Pts',(-1.82214081731815,30.3462543899266,-1.9845233820401));
#10864=CARTESIAN_POINT('Ctrl Pts',(-1.20394968168413,30.5545877232599,-2.307120726975));
#10865=CARTESIAN_POINT('Ctrl Pts',(-0.585758546050038,30.7629210565933,
-2.62971807191006));
#10866=CARTESIAN_POINT('Ctrl Pts',(0.110909354270839,30.9712543899266,-2.60000000000004));
#10867=CARTESIAN_POINT('Ctrl Pts',(0.807577254591778,31.17958772326,-2.57028192809014));
#10868=CARTESIAN_POINT('Ctrl Pts',(1.39605031831589,31.3879210565933,-2.19621137270416));
#10869=CARTESIAN_POINT('Ctrl Pts',(1.98452338204003,31.5962543899266,-1.82214081731823));
#10870=CARTESIAN_POINT('Ctrl Pts',(2.30712072697497,31.80458772326,-1.2039496816842));
#10871=CARTESIAN_POINT('Ctrl Pts',(2.62971807190996,32.0129210565933,-0.585758546050146));
#10872=CARTESIAN_POINT('Ctrl Pts',(2.59999999999998,32.2212543899266,0.110909354270782));
#10873=CARTESIAN_POINT('Ctrl Pts',(2.57028192809009,32.4295877232599,0.807577254591702));
#10874=CARTESIAN_POINT('Ctrl Pts',(2.19621137270409,32.6379210565933,1.39605031831587));
#10875=CARTESIAN_POINT('Ctrl Pts',(1.82214081731818,32.8462543899266,1.98452338203996));
#10876=CARTESIAN_POINT('Ctrl Pts',(1.20394968168411,33.05458772326,2.30712072697492));
#10877=CARTESIAN_POINT('Ctrl Pts',(0.585758546050062,33.2629210565933,2.62971807190987));
#10878=CARTESIAN_POINT('Ctrl Pts',(-0.11090935427086,33.4712543899266,2.59999999999995));
#10879=CARTESIAN_POINT('Ctrl Pts',(-0.807577254591756,33.67958772326,2.57028192809));
#10880=CARTESIAN_POINT('Ctrl Pts',(-1.39605031831591,33.8879210565933,2.19621137270406));
#10881=CARTESIAN_POINT('Ctrl Pts',(-1.98452338204,34.0962543899266,1.82214081731811));
#10882=CARTESIAN_POINT('Ctrl Pts',(-2.30712072697497,34.3045877232599,1.20394968168407));
#10883=CARTESIAN_POINT('Ctrl Pts',(-2.62971807190993,34.5129210565933,0.585758546050016));
#10884=CARTESIAN_POINT('Ctrl Pts',(-2.6,34.7212543899266,-0.110909354270923));
#10885=CARTESIAN_POINT('Ctrl Pts',(-2.57028192809006,34.92958772326,-0.807577254591853));
#10886=CARTESIAN_POINT('Ctrl Pts',(-2.19621137270411,35.1379210565933,-1.39605031831593));
#10887=CARTESIAN_POINT('Ctrl Pts',(-1.82214081731814,35.3462543899266,-1.98452338204009));
#10888=CARTESIAN_POINT('Ctrl Pts',(-1.20394968168411,35.55458772326,-2.30712072697501));
#10889=CARTESIAN_POINT('Ctrl Pts',(-0.58575854605004,35.7629210565933,-2.62971807190999));
#10890=CARTESIAN_POINT('Ctrl Pts',(0.110909354270858,35.9712543899266,-2.60000000000004));
#10891=CARTESIAN_POINT('Ctrl Pts',(0.807577254591799,36.17958772326,-2.57028192809016));
#10892=CARTESIAN_POINT('Ctrl Pts',(1.39605031831587,36.3879210565933,-2.19621137270416));
#10893=CARTESIAN_POINT('Ctrl Pts',(1.98452338204001,36.5962543899266,-1.82214081731826));
#10894=CARTESIAN_POINT('Ctrl Pts',(2.30712072697495,36.80458772326,-1.20394968168412));
#10895=CARTESIAN_POINT('Ctrl Pts',(2.62971807190995,37.0129210565933,-0.585758546050162));
#10896=CARTESIAN_POINT('Ctrl Pts',(2.6,37.2212543899266,0.110909354270793));
#10897=CARTESIAN_POINT('Ctrl Pts',(2.57028192809009,37.42958772326,0.807577254591713));
#10898=CARTESIAN_POINT('Ctrl Pts',(2.19621137270409,37.6379210565933,1.39605031831585));
#10899=CARTESIAN_POINT('Ctrl Pts',(1.82214081731818,37.8462543899266,1.98452338203995));
#10900=CARTESIAN_POINT('Ctrl Pts',(1.20394968168411,38.05458772326,2.30712072697493));
#10901=CARTESIAN_POINT('Ctrl Pts',(0.585758546050084,38.2629210565933,2.62971807190984));
#10902=CARTESIAN_POINT('Ctrl Pts',(-0.110909354270881,38.4712543899266,
2.59999999999996));
#10903=CARTESIAN_POINT('Ctrl Pts',(-0.807577254591756,38.67958772326,2.57028192809004));
#10904=CARTESIAN_POINT('Ctrl Pts',(-1.39605031831591,38.8879210565933,2.19621137270406));
#10905=CARTESIAN_POINT('Ctrl Pts',(-1.98452338204001,39.0962543899267,1.82214081731809));
#10906=CARTESIAN_POINT('Ctrl Pts',(-2.30712072697501,39.30458772326,1.20394968168406));
#10907=CARTESIAN_POINT('Ctrl Pts',(-2.62971807190992,39.5129210565933,0.585758546049984));
#10908=CARTESIAN_POINT('Ctrl Pts',(-2.60000000000002,39.7212543899267,-0.110909354270912));
#10909=CARTESIAN_POINT('Ctrl Pts',(-2.60000000000002,0.278745610073436,
0.110909354270912));
#10910=CARTESIAN_POINT('Ctrl Pts',(-2.62971807190994,0.487078943406783,
-0.585758546050092));
#10911=CARTESIAN_POINT('Ctrl Pts',(-2.307120726975,0.695412276740106,-1.20394968168414));
#10912=CARTESIAN_POINT('Ctrl Pts',(-1.98452338204005,0.903745610073436,
-1.82214081731813));
#10913=CARTESIAN_POINT('Ctrl Pts',(-1.39605031831596,1.11207894340677,-2.19621137270408));
#10914=CARTESIAN_POINT('Ctrl Pts',(-0.807577254591829,1.32041227674011,
-2.57028192809019));
#10915=CARTESIAN_POINT('Ctrl Pts',(-0.110909354270912,1.52874561007344,
-2.60000000000008));
#10916=CARTESIAN_POINT('Ctrl Pts',(0.585758546050027,1.73707894340677,-2.62971807191004));
#10917=CARTESIAN_POINT('Ctrl Pts',(1.20394968168406,1.9454122767401,-2.30712072697508));
#10918=CARTESIAN_POINT('Ctrl Pts',(1.82214081731812,2.15374561007341,-1.98452338204012));
#10919=CARTESIAN_POINT('Ctrl Pts',(2.19621137270406,2.36207894340677,-1.39605031831594));
#10920=CARTESIAN_POINT('Ctrl Pts',(2.57028192809005,2.5704122767401,-0.807577254591869));
#10921=CARTESIAN_POINT('Ctrl Pts',(2.59999999999998,2.77874561007344,-0.110909354270907));
#10922=CARTESIAN_POINT('Ctrl Pts',(2.62971807190997,2.98707894340676,0.585758546049919));
#10923=CARTESIAN_POINT('Ctrl Pts',(2.30712072697498,3.19541227674011,1.20394968168406));
#10924=CARTESIAN_POINT('Ctrl Pts',(1.98452338204005,3.40374561007341,1.82214081731804));
#10925=CARTESIAN_POINT('Ctrl Pts',(1.39605031831592,3.61207894340678,2.19621137270405));
#10926=CARTESIAN_POINT('Ctrl Pts',(0.807577254591831,3.82041227674012,2.57028192808996));
#10927=CARTESIAN_POINT('Ctrl Pts',(0.110909354270912,4.02874561007344,2.6));
#10928=CARTESIAN_POINT('Ctrl Pts',(-0.585758546050005,4.23707894340677,
2.62971807190995));
#10929=CARTESIAN_POINT('Ctrl Pts',(-1.20394968168408,4.4454122767401,2.30712072697499));
#10930=CARTESIAN_POINT('Ctrl Pts',(-1.8221408173181,4.65374561007344,1.98452338203996));
#10931=CARTESIAN_POINT('Ctrl Pts',(-2.19621137270408,4.86207894340675,1.39605031831586));
#10932=CARTESIAN_POINT('Ctrl Pts',(-2.57028192809003,5.07041227674009,0.807577254591729));
#10933=CARTESIAN_POINT('Ctrl Pts',(-2.60000000000002,5.27874561007344,0.110909354270912));
#10934=CARTESIAN_POINT('Ctrl Pts',(-2.62971807190994,5.48707894340677,-0.585758546050172));
#10935=CARTESIAN_POINT('Ctrl Pts',(-2.30712072697502,5.69541227674011,-1.20394968168414));
#10936=CARTESIAN_POINT('Ctrl Pts',(-1.98452338204004,5.90374561007343,-1.82214081731821));
#10937=CARTESIAN_POINT('Ctrl Pts',(-1.39605031831596,6.11207894340677,-2.19621137270408));
#10938=CARTESIAN_POINT('Ctrl Pts',(-0.80757725459181,6.32041227674011,-2.57028192809014));
#10939=CARTESIAN_POINT('Ctrl Pts',(-0.110909354270912,6.52874561007346,
-2.60000000000008));
#10940=CARTESIAN_POINT('Ctrl Pts',(0.585758546050008,6.73707894340677,-2.62971807191004));
#10941=CARTESIAN_POINT('Ctrl Pts',(1.20394968168404,6.94541227674013,-2.30712072697508));
#10942=CARTESIAN_POINT('Ctrl Pts',(1.82214081731814,7.15374561007344,-1.98452338204004));
#10943=CARTESIAN_POINT('Ctrl Pts',(2.19621137270408,7.36207894340678,-1.39605031831594));
#10944=CARTESIAN_POINT('Ctrl Pts',(2.57028192809007,7.57041227674014,-0.807577254591929));
#10945=CARTESIAN_POINT('Ctrl Pts',(2.6,7.77874561007344,-0.110909354270907));
#10946=CARTESIAN_POINT('Ctrl Pts',(2.62971807190995,7.98707894340679,0.585758546049914));
#10947=CARTESIAN_POINT('Ctrl Pts',(2.30712072697498,8.19541227674011,1.20394968168406));
#10948=CARTESIAN_POINT('Ctrl Pts',(1.98452338204007,8.40374561007345,1.82214081731803));
#10949=CARTESIAN_POINT('Ctrl Pts',(1.39605031831592,8.6120789434068,2.19621137270408));
#10950=CARTESIAN_POINT('Ctrl Pts',(0.807577254591834,8.82041227674012,2.57028192808996));
#10951=CARTESIAN_POINT('Ctrl Pts',(0.110909354270891,9.02874561007344,2.59999999999996));
#10952=CARTESIAN_POINT('Ctrl Pts',(-0.585758546050005,9.2370789434068,2.6297180719099));
#10953=CARTESIAN_POINT('Ctrl Pts',(-1.20394968168408,9.44541227674011,2.30712072697499));
#10954=CARTESIAN_POINT('Ctrl Pts',(-1.8221408173181,9.65374561007347,1.98452338203995));
#10955=CARTESIAN_POINT('Ctrl Pts',(-2.1962113727041,9.8620789434068,1.39605031831586));
#10956=CARTESIAN_POINT('Ctrl Pts',(-2.57028192809005,10.0704122767401,0.807577254591745));
#10957=CARTESIAN_POINT('Ctrl Pts',(-2.6,10.2787456100734,0.110909354270912));
#10958=CARTESIAN_POINT('Ctrl Pts',(-2.62971807190994,10.4870789434068,-0.585758546050097));
#10959=CARTESIAN_POINT('Ctrl Pts',(-2.30712072697502,10.6954122767401,-1.20394968168415));
#10960=CARTESIAN_POINT('Ctrl Pts',(-1.98452338204002,10.9037456100735,-1.82214081731821));
#10961=CARTESIAN_POINT('Ctrl Pts',(-1.39605031831596,11.1120789434068,-2.19621137270408));
#10962=CARTESIAN_POINT('Ctrl Pts',(-0.807577254591831,11.3204122767401,
-2.57028192809014));
#10963=CARTESIAN_POINT('Ctrl Pts',(-0.110909354270912,11.5287456100735,
-2.60000000000007));
#10964=CARTESIAN_POINT('Ctrl Pts',(0.585758546050027,11.7370789434068,-2.62971807191004));
#10965=CARTESIAN_POINT('Ctrl Pts',(1.20394968168406,11.9454122767401,-2.30712072697508));
#10966=CARTESIAN_POINT('Ctrl Pts',(1.82214081731812,12.1537456100735,-1.98452338204013));
#10967=CARTESIAN_POINT('Ctrl Pts',(2.19621137270406,12.3620789434068,-1.39605031831594));
#10968=CARTESIAN_POINT('Ctrl Pts',(2.57028192809007,12.5704122767401,-0.807577254591923));
#10969=CARTESIAN_POINT('Ctrl Pts',(2.6,12.7787456100734,-0.110909354270907));
#10970=CARTESIAN_POINT('Ctrl Pts',(2.62971807190997,12.9870789434068,0.585758546049914));
#10971=CARTESIAN_POINT('Ctrl Pts',(2.30712072697498,13.1954122767401,1.20394968168406));
#10972=CARTESIAN_POINT('Ctrl Pts',(1.98452338204005,13.4037456100734,1.82214081731803));
#10973=CARTESIAN_POINT('Ctrl Pts',(1.39605031831592,13.6120789434068,2.19621137270407));
#10974=CARTESIAN_POINT('Ctrl Pts',(0.807577254591831,13.8204122767401,2.57028192808997));
#10975=CARTESIAN_POINT('Ctrl Pts',(0.110909354270912,14.0287456100735,2.59999999999999));
#10976=CARTESIAN_POINT('Ctrl Pts',(-0.585758546049984,14.2370789434068,
2.62971807190992));
#10977=CARTESIAN_POINT('Ctrl Pts',(-1.20394968168406,14.4454122767402,2.30712072697499));
#10978=CARTESIAN_POINT('Ctrl Pts',(-1.82214081731812,14.6537456100735,1.98452338203996));
#10979=CARTESIAN_POINT('Ctrl Pts',(-2.19621137270408,14.8620789434068,1.39605031831585));
#10980=CARTESIAN_POINT('Ctrl Pts',(-2.57028192809005,15.0704122767401,0.807577254591761));
#10981=CARTESIAN_POINT('Ctrl Pts',(-2.6,15.2787456100734,0.110909354270912));
#10982=CARTESIAN_POINT('Ctrl Pts',(-2.62971807190993,15.4870789434068,-0.585758546050097));
#10983=CARTESIAN_POINT('Ctrl Pts',(-2.307120726975,15.6954122767401,-1.20394968168414));
#10984=CARTESIAN_POINT('Ctrl Pts',(-1.98452338204004,15.9037456100734,-1.82214081731821));
#10985=CARTESIAN_POINT('Ctrl Pts',(-1.39605031831596,16.1120789434068,-2.19621137270408));
#10986=CARTESIAN_POINT('Ctrl Pts',(-0.80757725459181,16.3204122767401,-2.5702819280902));
#10987=CARTESIAN_POINT('Ctrl Pts',(-0.110909354270912,16.5287456100734,
-2.60000000000008));
#10988=CARTESIAN_POINT('Ctrl Pts',(0.58575854605003,16.7370789434068,-2.62971807191002));
#10989=CARTESIAN_POINT('Ctrl Pts',(1.20394968168404,16.9454122767401,-2.30712072697508));
#10990=CARTESIAN_POINT('Ctrl Pts',(1.82214081731814,17.1537456100735,-1.98452338204012));
#10991=CARTESIAN_POINT('Ctrl Pts',(2.19621137270406,17.3620789434068,-1.39605031831595));
#10992=CARTESIAN_POINT('Ctrl Pts',(2.57028192809007,17.5704122767402,-0.80757725459188));
#10993=CARTESIAN_POINT('Ctrl Pts',(2.59999999999998,17.7787456100734,-0.110909354270907));
#10994=CARTESIAN_POINT('Ctrl Pts',(2.62971807190997,17.9870789434068,0.585758546049935));
#10995=CARTESIAN_POINT('Ctrl Pts',(2.30712072697498,18.1954122767402,1.20394968168405));
#10996=CARTESIAN_POINT('Ctrl Pts',(1.98452338204005,18.4037456100735,1.82214081731802));
#10997=CARTESIAN_POINT('Ctrl Pts',(1.39605031831592,18.6120789434068,2.19621137270408));
#10998=CARTESIAN_POINT('Ctrl Pts',(0.807577254591834,18.8204122767402,2.57028192808997));
#10999=CARTESIAN_POINT('Ctrl Pts',(0.110909354270891,19.0287456100735,2.59999999999999));
#11000=CARTESIAN_POINT('Ctrl Pts',(-0.585758546050005,19.2370789434068,
2.62971807190989));
#11001=CARTESIAN_POINT('Ctrl Pts',(-1.20394968168408,19.4454122767402,2.30712072697499));
#11002=CARTESIAN_POINT('Ctrl Pts',(-1.82214081731812,19.6537456100735,1.98452338203994));
#11003=CARTESIAN_POINT('Ctrl Pts',(-2.1962113727041,19.8620789434068,1.39605031831591));
#11004=CARTESIAN_POINT('Ctrl Pts',(-2.57028192809004,20.0704122767402,0.807577254591761));
#11005=CARTESIAN_POINT('Ctrl Pts',(-2.6,20.2787456100735,0.110909354270902));
#11006=CARTESIAN_POINT('Ctrl Pts',(-2.62971807190994,20.4870789434068,-0.585758546050065));
#11007=CARTESIAN_POINT('Ctrl Pts',(-2.30712072697502,20.6954122767402,-1.20394968168415));
#11008=CARTESIAN_POINT('Ctrl Pts',(-1.98452338204004,20.9037456100735,-1.82214081731816));
#11009=CARTESIAN_POINT('Ctrl Pts',(-1.39605031831594,21.1120789434068,-2.19621137270408));
#11010=CARTESIAN_POINT('Ctrl Pts',(-0.807577254591831,21.3204122767402,
-2.57028192809015));
#11011=CARTESIAN_POINT('Ctrl Pts',(-0.110909354270933,21.5287456100735,
-2.60000000000005));
#11012=CARTESIAN_POINT('Ctrl Pts',(0.585758546050027,21.7370789434068,-2.62971807191006));
#11013=CARTESIAN_POINT('Ctrl Pts',(1.20394968168404,21.9454122767401,-2.30712072697508));
#11014=CARTESIAN_POINT('Ctrl Pts',(1.82214081731812,22.1537456100735,-1.98452338204008));
#11015=CARTESIAN_POINT('Ctrl Pts',(2.19621137270406,22.3620789434068,-1.39605031831599));
#11016=CARTESIAN_POINT('Ctrl Pts',(2.57028192809005,22.5704122767402,-0.807577254591907));
#11017=CARTESIAN_POINT('Ctrl Pts',(2.6,22.7787456100735,-0.110909354270912));
#11018=CARTESIAN_POINT('Ctrl Pts',(2.62971807190995,22.9870789434068,0.585758546049909));
#11019=CARTESIAN_POINT('Ctrl Pts',(2.30712072697499,23.1954122767402,1.20394968168404));
#11020=CARTESIAN_POINT('Ctrl Pts',(1.98452338204007,23.4037456100735,1.82214081731806));
#11021=CARTESIAN_POINT('Ctrl Pts',(1.39605031831592,23.6120789434068,2.19621137270408));
#11022=CARTESIAN_POINT('Ctrl Pts',(0.807577254591853,23.8204122767402,2.57028192808998));
#11023=CARTESIAN_POINT('Ctrl Pts',(0.110909354270891,24.0287456100735,2.59999999999999));
#11024=CARTESIAN_POINT('Ctrl Pts',(-0.585758546049984,24.2370789434068,
2.62971807190988));
#11025=CARTESIAN_POINT('Ctrl Pts',(-1.20394968168408,24.4454122767401,2.307120726975));
#11026=CARTESIAN_POINT('Ctrl Pts',(-1.82214081731811,24.6537456100735,1.98452338203996));
#11027=CARTESIAN_POINT('Ctrl Pts',(-2.19621137270408,24.8620789434068,1.39605031831592));
#11028=CARTESIAN_POINT('Ctrl Pts',(-2.57028192809004,25.0704122767402,0.807577254591788));
#11029=CARTESIAN_POINT('Ctrl Pts',(-2.6,25.2787456100735,0.110909354270902));
#11030=CARTESIAN_POINT('Ctrl Pts',(-2.62971807190995,25.4870789434068,-0.585758546050065));
#11031=CARTESIAN_POINT('Ctrl Pts',(-2.307120726975,25.6954122767402,-1.20394968168412));
#11032=CARTESIAN_POINT('Ctrl Pts',(-1.98452338204004,25.9037456100735,-1.82214081731821));
#11033=CARTESIAN_POINT('Ctrl Pts',(-1.39605031831596,26.1120789434069,-2.19621137270412));
#11034=CARTESIAN_POINT('Ctrl Pts',(-0.807577254591831,26.3204122767401,
-2.57028192809014));
#11035=CARTESIAN_POINT('Ctrl Pts',(-0.110909354270912,26.5287456100735,
-2.60000000000005));
#11036=CARTESIAN_POINT('Ctrl Pts',(0.585758546050008,26.7370789434069,-2.62971807191005));
#11037=CARTESIAN_POINT('Ctrl Pts',(1.20394968168406,26.9454122767402,-2.30712072697512));
#11038=CARTESIAN_POINT('Ctrl Pts',(1.82214081731812,27.1537456100735,-1.98452338204008));
#11039=CARTESIAN_POINT('Ctrl Pts',(2.19621137270408,27.3620789434068,-1.39605031831603));
#11040=CARTESIAN_POINT('Ctrl Pts',(2.57028192809005,27.5704122767402,-0.807577254591918));
#11041=CARTESIAN_POINT('Ctrl Pts',(2.59999999999998,27.7787456100735,-0.110909354271001));
#11042=CARTESIAN_POINT('Ctrl Pts',(2.62971807190995,27.9870789434069,0.585758546049935));
#11043=CARTESIAN_POINT('Ctrl Pts',(2.30712072697499,28.1954122767402,1.20394968168403));
#11044=CARTESIAN_POINT('Ctrl Pts',(1.98452338204005,28.4037456100735,1.82214081731803));
#11045=CARTESIAN_POINT('Ctrl Pts',(1.39605031831592,28.6120789434068,2.19621137270408));
#11046=CARTESIAN_POINT('Ctrl Pts',(0.807577254591834,28.8204122767402,2.57028192808996));
#11047=CARTESIAN_POINT('Ctrl Pts',(0.110909354270912,29.0287456100734,2.59999999999999));
#11048=CARTESIAN_POINT('Ctrl Pts',(-0.585758546050005,29.2370789434068,
2.6297180719099));
#11049=CARTESIAN_POINT('Ctrl Pts',(-1.20394968168408,29.4454122767402,2.307120726975));
#11050=CARTESIAN_POINT('Ctrl Pts',(-1.82214081731812,29.6537456100735,1.98452338203995));
#11051=CARTESIAN_POINT('Ctrl Pts',(-2.19621137270408,29.8620789434069,1.39605031831591));
#11052=CARTESIAN_POINT('Ctrl Pts',(-2.57028192809004,30.0704122767402,0.807577254591761));
#11053=CARTESIAN_POINT('Ctrl Pts',(-2.6,30.2787456100735,0.110909354270865));
#11054=CARTESIAN_POINT('Ctrl Pts',(-2.62971807190995,30.4870789434069,-0.58575854605007));
#11055=CARTESIAN_POINT('Ctrl Pts',(-2.30712072697502,30.6954122767402,-1.20394968168412));
#11056=CARTESIAN_POINT('Ctrl Pts',(-1.98452338204004,30.9037456100735,-1.82214081731818));
#11057=CARTESIAN_POINT('Ctrl Pts',(-1.39605031831594,31.1120789434069,-2.19621137270412));
#11058=CARTESIAN_POINT('Ctrl Pts',(-0.807577254591831,31.3204122767402,
-2.57028192809019));
#11059=CARTESIAN_POINT('Ctrl Pts',(-0.110909354270912,31.5287456100735,
-2.60000000000006));
#11060=CARTESIAN_POINT('Ctrl Pts',(0.585758546050008,31.7370789434068,-2.62971807191004));
#11061=CARTESIAN_POINT('Ctrl Pts',(1.20394968168404,31.9454122767402,-2.30712072697511));
#11062=CARTESIAN_POINT('Ctrl Pts',(1.82214081731812,32.1537456100735,-1.98452338204011));
#11063=CARTESIAN_POINT('Ctrl Pts',(2.19621137270404,32.3620789434068,-1.39605031831603));
#11064=CARTESIAN_POINT('Ctrl Pts',(2.57028192809005,32.5704122767402,-0.807577254591907));
#11065=CARTESIAN_POINT('Ctrl Pts',(2.6,32.7787456100735,-0.110909354270959));
#11066=CARTESIAN_POINT('Ctrl Pts',(2.62971807190995,32.9870789434069,0.585758546049903));
#11067=CARTESIAN_POINT('Ctrl Pts',(2.30712072697499,33.1954122767402,1.20394968168402));
#11068=CARTESIAN_POINT('Ctrl Pts',(1.98452338204004,33.4037456100735,1.82214081731806));
#11069=CARTESIAN_POINT('Ctrl Pts',(1.39605031831594,33.6120789434069,2.19621137270407));
#11070=CARTESIAN_POINT('Ctrl Pts',(0.807577254591853,33.8204122767402,2.57028192808998));
#11071=CARTESIAN_POINT('Ctrl Pts',(0.110909354270891,34.0287456100735,2.59999999999999));
#11072=CARTESIAN_POINT('Ctrl Pts',(-0.585758546050008,34.2370789434069,
2.62971807190989));
#11073=CARTESIAN_POINT('Ctrl Pts',(-1.20394968168408,34.4454122767402,2.30712072697499));
#11074=CARTESIAN_POINT('Ctrl Pts',(-1.82214081731812,34.6537456100735,1.98452338203996));
#11075=CARTESIAN_POINT('Ctrl Pts',(-2.1962113727041,34.8620789434069,1.39605031831591));
#11076=CARTESIAN_POINT('Ctrl Pts',(-2.57028192809004,35.0704122767402,0.807577254591772));
#11077=CARTESIAN_POINT('Ctrl Pts',(-2.6,35.2787456100735,0.110909354270876));
#11078=CARTESIAN_POINT('Ctrl Pts',(-2.62971807190993,35.4870789434068,-0.585758546050086));
#11079=CARTESIAN_POINT('Ctrl Pts',(-2.30712072697501,35.6954122767402,-1.20394968168413));
#11080=CARTESIAN_POINT('Ctrl Pts',(-1.98452338204002,35.9037456100735,-1.82214081731821));
#11081=CARTESIAN_POINT('Ctrl Pts',(-1.39605031831594,36.1120789434069,-2.19621137270412));
#11082=CARTESIAN_POINT('Ctrl Pts',(-0.80757725459181,36.3204122767402,-2.57028192809015));
#11083=CARTESIAN_POINT('Ctrl Pts',(-0.110909354270933,36.5287456100735,
-2.60000000000005));
#11084=CARTESIAN_POINT('Ctrl Pts',(0.585758546050008,36.7370789434069,-2.62971807191005));
#11085=CARTESIAN_POINT('Ctrl Pts',(1.20394968168406,36.9454122767402,-2.3071207269751));
#11086=CARTESIAN_POINT('Ctrl Pts',(1.82214081731814,37.1537456100735,-1.9845233820401));
#11087=CARTESIAN_POINT('Ctrl Pts',(2.19621137270408,37.3620789434068,-1.39605031831602));
#11088=CARTESIAN_POINT('Ctrl Pts',(2.57028192809005,37.5704122767402,-0.807577254591923));
#11089=CARTESIAN_POINT('Ctrl Pts',(2.6,37.7787456100735,-0.110909354270975));
#11090=CARTESIAN_POINT('Ctrl Pts',(2.62971807190995,37.9870789434069,0.585758546049941));
#11091=CARTESIAN_POINT('Ctrl Pts',(2.307120726975,38.1954122767402,1.20394968168401));
#11092=CARTESIAN_POINT('Ctrl Pts',(1.98452338204005,38.4037456100735,1.82214081731804));
#11093=CARTESIAN_POINT('Ctrl Pts',(1.39605031831594,38.6120789434069,2.19621137270407));
#11094=CARTESIAN_POINT('Ctrl Pts',(0.807577254591853,38.8204122767402,2.57028192808997));
#11095=CARTESIAN_POINT('Ctrl Pts',(0.110909354270891,39.0287456100735,2.59999999999999));
#11096=CARTESIAN_POINT('Ctrl Pts',(-0.585758546050005,39.2370789434069,
2.6297180719099));
#11097=CARTESIAN_POINT('Ctrl Pts',(-1.20394968168408,39.4454122767402,2.30712072697499));
#11098=CARTESIAN_POINT('Ctrl Pts',(-1.8221408173181,39.6537456100736,1.98452338203994));
#11099=CARTESIAN_POINT('Ctrl Pts',(-2.19621137270408,39.8620789434069,1.39605031831592));
#11100=CARTESIAN_POINT('Ctrl Pts',(-2.57028192809004,40.0704122767402,0.807577254591751));
#11101=CARTESIAN_POINT('Ctrl Pts',(-2.6,40.2787456100736,0.110909354270871));
#11102=CARTESIAN_POINT('Ctrl Pts',(-2.,0.278745610073468,0.110909354270813));
#11103=CARTESIAN_POINT('Ctrl Pts',(-2.02971807190995,0.487078943406699,
-0.424989030591362));
#11104=CARTESIAN_POINT('Ctrl Pts',(-1.78750548470433,0.695412276740089,
-0.90394968168412));
#11105=CARTESIAN_POINT('Ctrl Pts',(-1.54529289749872,0.903745610073333,
-1.3829103327768));
#11106=CARTESIAN_POINT('Ctrl Pts',(-1.09605031831593,1.11207894340676,-1.67659613043348));
#11107=CARTESIAN_POINT('Ctrl Pts',(-0.646807739133152,1.32041227674011,
-1.97028192809006));
#11108=CARTESIAN_POINT('Ctrl Pts',(-0.110909354270893,1.52874561007344,
-2.00000000000001));
#11109=CARTESIAN_POINT('Ctrl Pts',(0.42498903059134,1.7370789434067,-2.02971807190998));
#11110=CARTESIAN_POINT('Ctrl Pts',(0.903949681684066,1.94541227674011,-1.78750548470433));
#11111=CARTESIAN_POINT('Ctrl Pts',(1.38291033277679,2.15374561007344,-1.54529289749872));
#11112=CARTESIAN_POINT('Ctrl Pts',(1.67659613043343,2.36207894340677,-1.09605031831594));
#11113=CARTESIAN_POINT('Ctrl Pts',(1.97028192809005,2.57041227674009,-0.646807739133166));
#11114=CARTESIAN_POINT('Ctrl Pts',(2.00000000000003,2.77874561007344,-0.110909354270911));
#11115=CARTESIAN_POINT('Ctrl Pts',(2.02971807190995,2.98707894340676,0.424989030591319));
#11116=CARTESIAN_POINT('Ctrl Pts',(1.78750548470433,3.1954122767401,0.903949681684016));
#11117=CARTESIAN_POINT('Ctrl Pts',(1.54529289749872,3.40374561007338,1.38291033277678));
#11118=CARTESIAN_POINT('Ctrl Pts',(1.09605031831593,3.61207894340677,1.67659613043342));
#11119=CARTESIAN_POINT('Ctrl Pts',(0.646807739133154,3.82041227674006,1.97028192809004));
#11120=CARTESIAN_POINT('Ctrl Pts',(0.110909354270907,4.02874561007344,1.99999999999995));
#11121=CARTESIAN_POINT('Ctrl Pts',(-0.424989030591324,4.23707894340672,
2.02971807190993));
#11122=CARTESIAN_POINT('Ctrl Pts',(-0.903949681684066,4.44541227674011,
1.78750548470433));
#11123=CARTESIAN_POINT('Ctrl Pts',(-1.38291033277679,4.65374561007344,1.54529289749866));
#11124=CARTESIAN_POINT('Ctrl Pts',(-1.67659613043344,4.8620789434068,1.09605031831587));
#11125=CARTESIAN_POINT('Ctrl Pts',(-1.97028192809005,5.07041227674005,0.646807739133138));
#11126=CARTESIAN_POINT('Ctrl Pts',(-2.,5.27874561007342,0.110909354270813));
#11127=CARTESIAN_POINT('Ctrl Pts',(-2.02971807190995,5.48707894340671,-0.424989030591405));
#11128=CARTESIAN_POINT('Ctrl Pts',(-1.78750548470433,5.6954122767401,-0.90394968168412));
#11129=CARTESIAN_POINT('Ctrl Pts',(-1.54529289749872,5.90374561007338,-1.38291033277678));
#11130=CARTESIAN_POINT('Ctrl Pts',(-1.09605031831592,6.11207894340678,-1.67659613043342));
#11131=CARTESIAN_POINT('Ctrl Pts',(-0.646807739133139,6.3204122767401,-1.97028192809006));
#11132=CARTESIAN_POINT('Ctrl Pts',(-0.110909354270905,6.52874561007347,
-2.00000000000006));
#11133=CARTESIAN_POINT('Ctrl Pts',(0.424989030591338,6.73707894340672,-2.02971807190996));
#11134=CARTESIAN_POINT('Ctrl Pts',(0.903949681684068,6.94541227674014,-1.78750548470433));
#11135=CARTESIAN_POINT('Ctrl Pts',(1.38291033277681,7.15374561007342,-1.54529289749877));
#11136=CARTESIAN_POINT('Ctrl Pts',(1.6765961304334,7.36207894340677,-1.09605031831599));
#11137=CARTESIAN_POINT('Ctrl Pts',(1.97028192809006,7.57041227674011,-0.646807739133152));
#11138=CARTESIAN_POINT('Ctrl Pts',(2.,7.77874561007349,-0.110909354270917));
#11139=CARTESIAN_POINT('Ctrl Pts',(2.02971807190995,7.98707894340672,0.424989030591319));
#11140=CARTESIAN_POINT('Ctrl Pts',(1.78750548470433,8.19541227674012,0.903949681684058));
#11141=CARTESIAN_POINT('Ctrl Pts',(1.54529289749873,8.40374561007341,1.3829103327768));
#11142=CARTESIAN_POINT('Ctrl Pts',(1.09605031831593,8.6120789434068,1.67659613043337));
#11143=CARTESIAN_POINT('Ctrl Pts',(0.646807739133154,8.82041227674011,1.97028192809005));
#11144=CARTESIAN_POINT('Ctrl Pts',(0.110909354270904,9.02874561007346,1.99999999999994));
#11145=CARTESIAN_POINT('Ctrl Pts',(-0.424989030591337,9.23707894340678,
2.02971807190995));
#11146=CARTESIAN_POINT('Ctrl Pts',(-0.903949681684064,9.44541227674011,
1.78750548470427));
#11147=CARTESIAN_POINT('Ctrl Pts',(-1.38291033277679,9.65374561007344,1.54529289749871));
#11148=CARTESIAN_POINT('Ctrl Pts',(-1.67659613043342,9.86207894340678,1.09605031831593));
#11149=CARTESIAN_POINT('Ctrl Pts',(-1.97028192809005,10.0704122767401,0.646807739133152));
#11150=CARTESIAN_POINT('Ctrl Pts',(-1.99999999999999,10.2787456100735,0.110909354270841));
#11151=CARTESIAN_POINT('Ctrl Pts',(-2.02971807190994,10.4870789434068,-0.42498903059134));
#11152=CARTESIAN_POINT('Ctrl Pts',(-1.78750548470433,10.6954122767401,-0.903949681684169));
#11153=CARTESIAN_POINT('Ctrl Pts',(-1.54529289749871,10.9037456100734,-1.38291033277681));
#11154=CARTESIAN_POINT('Ctrl Pts',(-1.09605031831593,11.1120789434068,-1.67659613043348));
#11155=CARTESIAN_POINT('Ctrl Pts',(-0.646807739133152,11.3204122767401,
-1.97028192809006));
#11156=CARTESIAN_POINT('Ctrl Pts',(-0.110909354270907,11.5287456100735,
-2.00000000000002));
#11157=CARTESIAN_POINT('Ctrl Pts',(0.424989030591338,11.7370789434068,-2.02971807190997));
#11158=CARTESIAN_POINT('Ctrl Pts',(0.903949681684066,11.9454122767401,-1.78750548470433));
#11159=CARTESIAN_POINT('Ctrl Pts',(1.3829103327768,12.1537456100734,-1.54529289749877));
#11160=CARTESIAN_POINT('Ctrl Pts',(1.67659613043342,12.3620789434068,-1.09605031831594));
#11161=CARTESIAN_POINT('Ctrl Pts',(1.97028192809008,12.5704122767401,-0.646807739133166));
#11162=CARTESIAN_POINT('Ctrl Pts',(2.,12.7787456100735,-0.110909354270959));
#11163=CARTESIAN_POINT('Ctrl Pts',(2.02971807190995,12.9870789434068,0.42498903059134));
#11164=CARTESIAN_POINT('Ctrl Pts',(1.78750548470433,13.1954122767401,0.903949681684009));
#11165=CARTESIAN_POINT('Ctrl Pts',(1.54529289749872,13.4037456100734,1.38291033277679));
#11166=CARTESIAN_POINT('Ctrl Pts',(1.09605031831593,13.6120789434068,1.67659613043342));
#11167=CARTESIAN_POINT('Ctrl Pts',(0.646807739133154,13.8204122767401,1.97028192809006));
#11168=CARTESIAN_POINT('Ctrl Pts',(0.110909354270907,14.0287456100735,1.99999999999997));
#11169=CARTESIAN_POINT('Ctrl Pts',(-0.424989030591338,14.2370789434068,
2.02971807190995));
#11170=CARTESIAN_POINT('Ctrl Pts',(-0.903949681684066,14.4454122767402,
1.78750548470424));
#11171=CARTESIAN_POINT('Ctrl Pts',(-1.38291033277679,14.6537456100734,1.54529289749866));
#11172=CARTESIAN_POINT('Ctrl Pts',(-1.67659613043342,14.8620789434068,1.09605031831587));
#11173=CARTESIAN_POINT('Ctrl Pts',(-1.97028192809004,15.0704122767401,0.646807739133166));
#11174=CARTESIAN_POINT('Ctrl Pts',(-2.,15.2787456100735,0.110909354270848));
#11175=CARTESIAN_POINT('Ctrl Pts',(-2.02971807190995,15.4870789434068,-0.424989030591448));
#11176=CARTESIAN_POINT('Ctrl Pts',(-1.78750548470433,15.6954122767401,-0.903949681684079));
#11177=CARTESIAN_POINT('Ctrl Pts',(-1.54529289749872,15.9037456100734,-1.3829103327768));
#11178=CARTESIAN_POINT('Ctrl Pts',(-1.09605031831592,16.1120789434068,-1.67659613043346));
#11179=CARTESIAN_POINT('Ctrl Pts',(-0.646807739133152,16.3204122767401,
-1.97028192809011));
#11180=CARTESIAN_POINT('Ctrl Pts',(-0.110909354270907,16.5287456100735,
-2.00000000000005));
#11181=CARTESIAN_POINT('Ctrl Pts',(0.42498903059134,16.7370789434068,-2.02971807190995));
#11182=CARTESIAN_POINT('Ctrl Pts',(0.90394968168408,16.9454122767401,-1.78750548470433));
#11183=CARTESIAN_POINT('Ctrl Pts',(1.38291033277679,17.1537456100734,-1.54529289749872));
#11184=CARTESIAN_POINT('Ctrl Pts',(1.67659613043342,17.3620789434068,-1.09605031831599));
#11185=CARTESIAN_POINT('Ctrl Pts',(1.97028192809005,17.5704122767401,-0.646807739133152));
#11186=CARTESIAN_POINT('Ctrl Pts',(2.,17.7787456100735,-0.110909354270917));
#11187=CARTESIAN_POINT('Ctrl Pts',(2.02971807190995,17.9870789434068,0.424989030591283));
#11188=CARTESIAN_POINT('Ctrl Pts',(1.78750548470433,18.1954122767401,0.903949681684051));
#11189=CARTESIAN_POINT('Ctrl Pts',(1.54529289749873,18.4037456100734,1.3829103327768));
#11190=CARTESIAN_POINT('Ctrl Pts',(1.09605031831593,18.6120789434068,1.67659613043337));
#11191=CARTESIAN_POINT('Ctrl Pts',(0.646807739133154,18.8204122767401,1.97028192809005));
#11192=CARTESIAN_POINT('Ctrl Pts',(0.110909354270905,19.0287456100735,1.99999999999995));
#11193=CARTESIAN_POINT('Ctrl Pts',(-0.424989030591338,19.2370789434068,
2.02971807190995));
#11194=CARTESIAN_POINT('Ctrl Pts',(-0.903949681684064,19.4454122767402,
1.78750548470426));
#11195=CARTESIAN_POINT('Ctrl Pts',(-1.38291033277679,19.6537456100734,1.54529289749871));
#11196=CARTESIAN_POINT('Ctrl Pts',(-1.67659613043342,19.8620789434068,1.0960503183159));
#11197=CARTESIAN_POINT('Ctrl Pts',(-1.97028192809006,20.0704122767401,0.646807739133152));
#11198=CARTESIAN_POINT('Ctrl Pts',(-1.99999999999999,20.2787456100735,0.11090935427082));
#11199=CARTESIAN_POINT('Ctrl Pts',(-2.02971807190993,20.4870789434068,-0.424989030591398));
#11200=CARTESIAN_POINT('Ctrl Pts',(-1.78750548470433,20.6954122767402,-0.903949681684127));
#11201=CARTESIAN_POINT('Ctrl Pts',(-1.5452928974987,20.9037456100735,-1.38291033277683));
#11202=CARTESIAN_POINT('Ctrl Pts',(-1.09605031831595,21.1120789434068,-1.67659613043348));
#11203=CARTESIAN_POINT('Ctrl Pts',(-0.646807739133154,21.3204122767401,
-1.97028192809006));
#11204=CARTESIAN_POINT('Ctrl Pts',(-0.110909354270907,21.5287456100735,
-2.));
#11205=CARTESIAN_POINT('Ctrl Pts',(0.424989030591338,21.7370789434068,-2.02971807190994));
#11206=CARTESIAN_POINT('Ctrl Pts',(0.903949681684066,21.9454122767402,-1.78750548470436));
#11207=CARTESIAN_POINT('Ctrl Pts',(1.38291033277679,22.1537456100734,-1.54529289749877));
#11208=CARTESIAN_POINT('Ctrl Pts',(1.67659613043343,22.3620789434069,-1.09605031831595));
#11209=CARTESIAN_POINT('Ctrl Pts',(1.97028192809003,22.5704122767401,-0.646807739133152));
#11210=CARTESIAN_POINT('Ctrl Pts',(2.,22.7787456100735,-0.110909354270945));
#11211=CARTESIAN_POINT('Ctrl Pts',(2.02971807190997,22.9870789434068,0.42498903059134));
#11212=CARTESIAN_POINT('Ctrl Pts',(1.78750548470433,23.1954122767402,0.903949681684009));
#11213=CARTESIAN_POINT('Ctrl Pts',(1.54529289749872,23.4037456100734,1.38291033277679));
#11214=CARTESIAN_POINT('Ctrl Pts',(1.09605031831593,23.6120789434068,1.6765961304334));
#11215=CARTESIAN_POINT('Ctrl Pts',(0.646807739133168,23.8204122767401,1.97028192809006));
#11216=CARTESIAN_POINT('Ctrl Pts',(0.110909354270907,24.0287456100735,1.99999999999992));
#11217=CARTESIAN_POINT('Ctrl Pts',(-0.424989030591338,24.2370789434068,
2.02971807190996));
#11218=CARTESIAN_POINT('Ctrl Pts',(-0.903949681684066,24.4454122767402,
1.78750548470424));
#11219=CARTESIAN_POINT('Ctrl Pts',(-1.38291033277678,24.6537456100735,1.54529289749864));
#11220=CARTESIAN_POINT('Ctrl Pts',(-1.67659613043341,24.8620789434068,1.09605031831588));
#11221=CARTESIAN_POINT('Ctrl Pts',(-1.97028192809005,25.0704122767401,0.646807739133166));
#11222=CARTESIAN_POINT('Ctrl Pts',(-2.,25.2787456100735,0.110909354270855));
#11223=CARTESIAN_POINT('Ctrl Pts',(-2.02971807190995,25.4870789434068,-0.424989030591369));
#11224=CARTESIAN_POINT('Ctrl Pts',(-1.78750548470433,25.6954122767401,-0.903949681684079));
#11225=CARTESIAN_POINT('Ctrl Pts',(-1.54529289749871,25.9037456100735,-1.3829103327768));
#11226=CARTESIAN_POINT('Ctrl Pts',(-1.09605031831593,26.1120789434068,-1.67659613043345));
#11227=CARTESIAN_POINT('Ctrl Pts',(-0.646807739133152,26.3204122767401,
-1.97028192809011));
#11228=CARTESIAN_POINT('Ctrl Pts',(-0.110909354270907,26.5287456100735,
-2.00000000000004));
#11229=CARTESIAN_POINT('Ctrl Pts',(0.424989030591353,26.7370789434068,-2.02971807190995));
#11230=CARTESIAN_POINT('Ctrl Pts',(0.90394968168408,26.9454122767402,-1.78750548470438));
#11231=CARTESIAN_POINT('Ctrl Pts',(1.38291033277679,27.1537456100734,-1.54529289749872));
#11232=CARTESIAN_POINT('Ctrl Pts',(1.6765961304334,27.3620789434068,-1.09605031831597));
#11233=CARTESIAN_POINT('Ctrl Pts',(1.97028192809005,27.5704122767401,-0.64680773913318));
#11234=CARTESIAN_POINT('Ctrl Pts',(1.99999999999997,27.7787456100735,-0.110909354270911));
#11235=CARTESIAN_POINT('Ctrl Pts',(2.02971807190995,27.9870789434068,0.424989030591333));
#11236=CARTESIAN_POINT('Ctrl Pts',(1.78750548470433,28.1954122767402,0.903949681684037));
#11237=CARTESIAN_POINT('Ctrl Pts',(1.5452928974987,28.4037456100735,1.38291033277679));
#11238=CARTESIAN_POINT('Ctrl Pts',(1.09605031831593,28.6120789434068,1.67659613043337));
#11239=CARTESIAN_POINT('Ctrl Pts',(0.646807739133154,28.8204122767401,1.97028192809002));
#11240=CARTESIAN_POINT('Ctrl Pts',(0.110909354270921,29.0287456100735,1.99999999999997));
#11241=CARTESIAN_POINT('Ctrl Pts',(-0.424989030591338,29.2370789434068,
2.02971807190995));
#11242=CARTESIAN_POINT('Ctrl Pts',(-0.903949681684064,29.4454122767402,
1.78750548470427));
#11243=CARTESIAN_POINT('Ctrl Pts',(-1.38291033277679,29.6537456100735,1.54529289749868));
#11244=CARTESIAN_POINT('Ctrl Pts',(-1.67659613043342,29.8620789434068,1.09605031831586));
#11245=CARTESIAN_POINT('Ctrl Pts',(-1.97028192809005,30.0704122767401,0.646807739133123));
#11246=CARTESIAN_POINT('Ctrl Pts',(-2.,30.2787456100735,0.110909354270834));
#11247=CARTESIAN_POINT('Ctrl Pts',(-2.02971807190995,30.4870789434068,-0.424989030591398));
#11248=CARTESIAN_POINT('Ctrl Pts',(-1.78750548470432,30.6954122767402,-0.903949681684113));
#11249=CARTESIAN_POINT('Ctrl Pts',(-1.54529289749872,30.9037456100735,-1.38291033277676));
#11250=CARTESIAN_POINT('Ctrl Pts',(-1.09605031831593,31.1120789434068,-1.67659613043348));
#11251=CARTESIAN_POINT('Ctrl Pts',(-0.646807739133152,31.3204122767401,
-1.97028192809006));
#11252=CARTESIAN_POINT('Ctrl Pts',(-0.110909354270905,31.5287456100735,
-2.));
#11253=CARTESIAN_POINT('Ctrl Pts',(0.42498903059134,31.7370789434068,-2.02971807190996));
#11254=CARTESIAN_POINT('Ctrl Pts',(0.903949681684054,31.9454122767402,-1.78750548470435));
#11255=CARTESIAN_POINT('Ctrl Pts',(1.38291033277679,32.1537456100735,-1.54529289749877));
#11256=CARTESIAN_POINT('Ctrl Pts',(1.67659613043342,32.3620789434069,-1.09605031831598));
#11257=CARTESIAN_POINT('Ctrl Pts',(1.97028192809005,32.5704122767401,-0.646807739133152));
#11258=CARTESIAN_POINT('Ctrl Pts',(2.,32.7787456100735,-0.110909354270917));
#11259=CARTESIAN_POINT('Ctrl Pts',(2.02971807190995,32.9870789434069,0.424989030591311));
#11260=CARTESIAN_POINT('Ctrl Pts',(1.78750548470433,33.1954122767402,0.903949681684009));
#11261=CARTESIAN_POINT('Ctrl Pts',(1.54529289749872,33.4037456100734,1.38291033277681));
#11262=CARTESIAN_POINT('Ctrl Pts',(1.09605031831593,33.6120789434068,1.67659613043341));
#11263=CARTESIAN_POINT('Ctrl Pts',(0.646807739133154,33.8204122767401,1.97028192809006));
#11264=CARTESIAN_POINT('Ctrl Pts',(0.110909354270907,34.0287456100735,1.99999999999993));
#11265=CARTESIAN_POINT('Ctrl Pts',(-0.424989030591338,34.2370789434068,
2.02971807190994));
#11266=CARTESIAN_POINT('Ctrl Pts',(-0.903949681684066,34.4454122767402,
1.78750548470426));
#11267=CARTESIAN_POINT('Ctrl Pts',(-1.38291033277681,34.6537456100735,1.54529289749869));
#11268=CARTESIAN_POINT('Ctrl Pts',(-1.67659613043341,34.8620789434068,1.0960503183159));
#11269=CARTESIAN_POINT('Ctrl Pts',(-1.97028192809005,35.0704122767402,0.646807739133166));
#11270=CARTESIAN_POINT('Ctrl Pts',(-2.,35.2787456100736,0.110909354270855));
#11271=CARTESIAN_POINT('Ctrl Pts',(-2.02971807190995,35.4870789434068,-0.424989030591383));
#11272=CARTESIAN_POINT('Ctrl Pts',(-1.78750548470433,35.6954122767402,-0.903949681684099));
#11273=CARTESIAN_POINT('Ctrl Pts',(-1.54529289749872,35.9037456100735,-1.38291033277681));
#11274=CARTESIAN_POINT('Ctrl Pts',(-1.09605031831593,36.1120789434069,-1.67659613043344));
#11275=CARTESIAN_POINT('Ctrl Pts',(-0.646807739133139,36.3204122767402,
-1.97028192809006));
#11276=CARTESIAN_POINT('Ctrl Pts',(-0.110909354270907,36.5287456100735,
-2.00000000000004));
#11277=CARTESIAN_POINT('Ctrl Pts',(0.424989030591338,36.7370789434068,-2.02971807190996));
#11278=CARTESIAN_POINT('Ctrl Pts',(0.903949681684066,36.9454122767402,-1.78750548470439));
#11279=CARTESIAN_POINT('Ctrl Pts',(1.38291033277679,37.1537456100734,-1.54529289749872));
#11280=CARTESIAN_POINT('Ctrl Pts',(1.67659613043343,37.3620789434069,-1.09605031831598));
#11281=CARTESIAN_POINT('Ctrl Pts',(1.97028192809006,37.5704122767401,-0.646807739133152));
#11282=CARTESIAN_POINT('Ctrl Pts',(2.,37.7787456100735,-0.110909354270952));
#11283=CARTESIAN_POINT('Ctrl Pts',(2.02971807190997,37.9870789434069,0.424989030591333));
#11284=CARTESIAN_POINT('Ctrl Pts',(1.78750548470433,38.1954122767402,0.903949681684023));
#11285=CARTESIAN_POINT('Ctrl Pts',(1.54529289749872,38.4037456100734,1.3829103327768));
#11286=CARTESIAN_POINT('Ctrl Pts',(1.09605031831595,38.6120789434069,1.67659613043338));
#11287=CARTESIAN_POINT('Ctrl Pts',(0.646807739133154,38.8204122767402,1.97028192809006));
#11288=CARTESIAN_POINT('Ctrl Pts',(0.110909354270921,39.0287456100735,1.99999999999997));
#11289=CARTESIAN_POINT('Ctrl Pts',(-0.424989030591324,39.2370789434069,
2.02971807190996));
#11290=CARTESIAN_POINT('Ctrl Pts',(-0.903949681684052,39.4454122767402,
1.78750548470429));
#11291=CARTESIAN_POINT('Ctrl Pts',(-1.38291033277679,39.6537456100735,1.54529289749867));
#11292=CARTESIAN_POINT('Ctrl Pts',(-1.67659613043342,39.8620789434069,1.09605031831587));
#11293=CARTESIAN_POINT('Ctrl Pts',(-1.97028192809005,40.0704122767402,0.646807739133166));
#11294=CARTESIAN_POINT('Ctrl Pts',(-2.,40.2787456100735,0.110909354270834));
#11295=CARTESIAN_POINT('Ctrl Pts',(-2.00308415717522,0.327811454287795,
-0.0144742926159549));
#11296=CARTESIAN_POINT('Ctrl Pts',(-2.02960770809824,0.326083522404792,
-0.0117641501090121));
#11297=CARTESIAN_POINT('Ctrl Pts',(-2.05570512799209,0.320591728514443,
-0.00890360021891084));
#11298=CARTESIAN_POINT('Ctrl Pts',(-2.1162806096187,0.299064621655046,-0.00167442520673255));
#11299=CARTESIAN_POINT('Ctrl Pts',(-2.14909453914282,0.279784636444006,
0.00275906069350319));
#11300=CARTESIAN_POINT('Ctrl Pts',(-2.20027423277635,0.236305190619192,
0.0107637785694441));
#11301=CARTESIAN_POINT('Ctrl Pts',(-2.22004359368015,0.214292607972338,
0.0142777651219529));
#11302=CARTESIAN_POINT('Ctrl Pts',(-2.25554049776359,0.162900143744721,
0.021564697553154));
#11303=CARTESIAN_POINT('Ctrl Pts',(-2.27037406610162,0.133105928183891,
0.0253044485090571));
#11304=CARTESIAN_POINT('Ctrl Pts',(-2.28333129245606,0.0945494429191525,
0.029529898402844));
#11305=CARTESIAN_POINT('Ctrl Pts',(-2.28551379053089,0.087294323511717,
0.0303213415012689));
#11306=CARTESIAN_POINT('Ctrl Pts',(-2.28747252867205,0.0799568405573766,
0.0310811961015807));
#11307=CARTESIAN_POINT('Ctrl Pts',(-2.00000135271328,-0.264728740315192,
0.141133603659935));
#11308=CARTESIAN_POINT('Ctrl Pts',(-1.93317947679614,-0.140205665678286,
0.374694616019038));
#11309=CARTESIAN_POINT('Ctrl Pts',(-1.89576261275035,-0.0714195242393531,
0.563391879075593));
#11310=CARTESIAN_POINT('Ctrl Pts',(-1.85828016234107,-0.0141476745355931,
0.845995304749381));
#11311=CARTESIAN_POINT('Ctrl Pts',(-1.85721582540971,-0.0237125088868792,
0.935184056400945));
#11312=CARTESIAN_POINT('Ctrl Pts',(-1.86061638209651,-0.0666740172427863,
1.06187361715673));
#11313=CARTESIAN_POINT('Ctrl Pts',(-1.86640738686477,-0.101672715288381,
1.11012925637074));
#11314=CARTESIAN_POINT('Ctrl Pts',(-1.88833554246329,-0.235746153313808,
1.21545234876845));
#11315=CARTESIAN_POINT('Ctrl Pts',(-1.9033753276643,-0.335251316849042,
1.26604967753693));
#11316=CARTESIAN_POINT('Ctrl Pts',(-1.9189176957612,-0.518726439558199,
1.34035163842065));
#11317=CARTESIAN_POINT('Ctrl Pts',(-1.92137116451861,-0.585485291115871,
1.36832017615168));
#11318=CARTESIAN_POINT('Ctrl Pts',(-1.93896943688162,-0.724455435049461,
1.40322870297494));
#11319=CARTESIAN_POINT('Ctrl Pts',(-1.95325668725115,-0.796545227124419,
1.40888781048668));
#11320=CARTESIAN_POINT('Ctrl Pts',(-1.99209925627655,-1.01599260874888,
1.41219882843878));
#11321=CARTESIAN_POINT('Ctrl Pts',(-2.00898122237353,-1.16761549888469,
1.40420126611032));
#11322=CARTESIAN_POINT('Ctrl Pts',(-2.01271588366055,-1.60175062040053,
1.36576567629003));
#11323=CARTESIAN_POINT('Ctrl Pts',(-1.95046360827934,-1.85129221142242,
1.32547580954877));
#11324=CARTESIAN_POINT('Ctrl Pts',(-1.69792570410908,-2.14007513561928,
1.27973035876422));
#11325=CARTESIAN_POINT('Ctrl Pts',(-1.50788517190343,-2.24578075342313,
1.26508664601861));
#11326=CARTESIAN_POINT('Ctrl Pts',(-1.03351721040672,-2.37409803162741,
1.24662061906772));
#11327=CARTESIAN_POINT('Ctrl Pts',(-0.753928362614793,-2.39679255199907,
1.24243205928811));
#11328=CARTESIAN_POINT('Ctrl Pts',(-0.218845999430284,-2.35785399723118,
1.24055602083421));
#11329=CARTESIAN_POINT('Ctrl Pts',(0.0368662467341799,-2.29519092886669,
1.24322556456469));
#11330=CARTESIAN_POINT('Ctrl Pts',(0.411239882065782,-2.11406967659605,
1.2495991139221));
#11331=CARTESIAN_POINT('Ctrl Pts',(0.518384719875618,-2.00298884738698,
1.25072899682664));
#11332=CARTESIAN_POINT('Ctrl Pts',(0.571801954928687,-1.83523605217566,
1.25334679757698));
#11333=CARTESIAN_POINT('Ctrl Pts',(0.569023344394799,-1.74044478899434,
1.25599881503435));
#11334=CARTESIAN_POINT('Ctrl Pts',(0.494126240428662,-1.50788563057796,
1.25886663470126));
#11335=CARTESIAN_POINT('Ctrl Pts',(0.421606239831573,-1.37485017740085,
1.26041038383949));
#11336=CARTESIAN_POINT('Ctrl Pts',(0.127609128452456,-0.989034614321357,
1.26907008807672));
#11337=CARTESIAN_POINT('Ctrl Pts',(-0.170570542490676,-0.751894328558357,
1.28023791867232));
#11338=CARTESIAN_POINT('Ctrl Pts',(-0.569600762546571,-0.586703644418381,
1.30640573381989));
#11339=CARTESIAN_POINT('Ctrl Pts',(-0.692371618949951,-0.563856396440986,
1.31685387723007));
#11340=CARTESIAN_POINT('Ctrl Pts',(-0.882581236630141,-0.577499841895708,
1.33968897633028));
#11341=CARTESIAN_POINT('Ctrl Pts',(-0.949730803773584,-0.6053755874494,
1.35084566027416));
#11342=CARTESIAN_POINT('Ctrl Pts',(-1.08267031338154,-0.742643707380371,
1.38530535019886));
#11343=CARTESIAN_POINT('Ctrl Pts',(-1.14980571385887,-0.863823663666268,
1.41045379245241));
#11344=CARTESIAN_POINT('Ctrl Pts',(-1.22863752459304,-1.27359538565792,
1.48274964800499));
#11345=CARTESIAN_POINT('Ctrl Pts',(-1.23841278692706,-1.55826711159036,
1.52914339518866));
#11346=CARTESIAN_POINT('Ctrl Pts',(-1.19858468901873,-1.92998306793573,
1.58589472341859));
#11347=CARTESIAN_POINT('Ctrl Pts',(-1.41479641657991,-0.327027665826027,
0.0242831581950105));
#11348=CARTESIAN_POINT('Ctrl Pts',(-1.34348892337276,-0.181250738802885,
0.26897733822669));
#11349=CARTESIAN_POINT('Ctrl Pts',(-1.3008280875213,-0.0880638424496696,
0.476392819418064));
#11350=CARTESIAN_POINT('Ctrl Pts',(-1.25754057161045,0.0123013660558204,
0.831666797361881));
#11351=CARTESIAN_POINT('Ctrl Pts',(-1.25687388480527,0.0194522591100595,
0.979479411006855));
#11352=CARTESIAN_POINT('Ctrl Pts',(-1.2830830371466,-0.0336379080354797,
1.23391882276437));
#11353=CARTESIAN_POINT('Ctrl Pts',(-1.30959041125068,-0.0938600720654208,
1.34021747917579));
#11354=CARTESIAN_POINT('Ctrl Pts',(-1.38041341547889,-0.261824969553754,
1.53853407301497));
#11355=CARTESIAN_POINT('Ctrl Pts',(-1.42362766577653,-0.369411940643664,
1.63197959161429));
#11356=CARTESIAN_POINT('Ctrl Pts',(-1.51482462448403,-0.553055900414141,
1.7840154902546));
#11357=CARTESIAN_POINT('Ctrl Pts',(-1.55452145207106,-0.616871235334267,
1.84288502733572));
#11358=CARTESIAN_POINT('Ctrl Pts',(-1.61769237293684,-0.76088554847919,
1.90941994885935));
#11359=CARTESIAN_POINT('Ctrl Pts',(-1.63741652204799,-0.839819060706829,
1.91721278463516));
#11360=CARTESIAN_POINT('Ctrl Pts',(-1.67857813189676,-1.07311708366726,
1.92065626175757));
#11361=CARTESIAN_POINT('Ctrl Pts',(-1.69450638574114,-1.22468485755413,
1.91207917479615));
#11362=CARTESIAN_POINT('Ctrl Pts',(-1.69776273723848,-1.63025676912522,
1.87601769283407));
#11363=CARTESIAN_POINT('Ctrl Pts',(-1.63558587031057,-1.8094473554909,1.8484014728917));
#11364=CARTESIAN_POINT('Ctrl Pts',(-1.51744170723058,-1.93391724344097,
1.82161070104937));
#11365=CARTESIAN_POINT('Ctrl Pts',(-1.38720614355509,-2.01215777720118,
1.80651658245784));
#11366=CARTESIAN_POINT('Ctrl Pts',(-0.999318445532683,-2.1000372109959,
1.78142022672165));
#11367=CARTESIAN_POINT('Ctrl Pts',(-0.75320228279494,-2.109345485096,1.77049841986191));
#11368=CARTESIAN_POINT('Ctrl Pts',(-0.291144343481196,-2.05182844476988,
1.75300283223748));
#11369=CARTESIAN_POINT('Ctrl Pts',(-0.0746276920240247,-1.98390441220646,
1.74716065612451));
#11370=CARTESIAN_POINT('Ctrl Pts',(0.192072445804306,-1.83915272276575,
1.73915712563726));
#11371=CARTESIAN_POINT('Ctrl Pts',(0.210347585325089,-1.77773490581458,
1.73080489996179));
#11372=CARTESIAN_POINT('Ctrl Pts',(0.198976982175155,-1.81462152515841,
1.73113541660097));
#11373=CARTESIAN_POINT('Ctrl Pts',(0.213011996067426,-1.79205629656322,
1.73877515384333));
#11374=CARTESIAN_POINT('Ctrl Pts',(0.177186567758258,-1.65070903664641,
1.7504269870299));
#11375=CARTESIAN_POINT('Ctrl Pts',(0.129908624188708,-1.54404411523484,
1.75773877200305));
#11376=CARTESIAN_POINT('Ctrl Pts',(-0.0876107518951426,-1.21505608778235,
1.78559033317587));
#11377=CARTESIAN_POINT('Ctrl Pts',(-0.337497876869364,-0.989695956702306,
1.81129298511067));
#11378=CARTESIAN_POINT('Ctrl Pts',(-0.619417429815987,-0.851281642971048,
1.84410939565886));
#11379=CARTESIAN_POINT('Ctrl Pts',(-0.691821618472955,-0.839216119419207,
1.85456575460658));
#11380=CARTESIAN_POINT('Ctrl Pts',(-0.742506322151624,-0.836948971076064,
1.86696729841403));
#11381=CARTESIAN_POINT('Ctrl Pts',(-0.720038690828119,-0.826234748910869,
1.86596691745099));
#11382=CARTESIAN_POINT('Ctrl Pts',(-0.741001371120147,-0.843622783703197,
1.87515508429125));
#11383=CARTESIAN_POINT('Ctrl Pts',(-0.787635764756597,-0.899635885793011,
1.88970955146323));
#11384=CARTESIAN_POINT('Ctrl Pts',(-0.852118294742336,-1.21903207139812,
1.94900258458685));
#11385=CARTESIAN_POINT('Ctrl Pts',(-0.865431353370241,-1.47313529513962,
1.99195746223939));
#11386=CARTESIAN_POINT('Ctrl Pts',(-0.829509728173782,-1.82164035961998,
2.04637874141716));
#11387=CARTESIAN_POINT('Ctrl Pts',(-1.41479632875941,0.202424372508809,
-0.25799425695406));
#11388=CARTESIAN_POINT('Ctrl Pts',(-1.34782702531429,0.367995784832215,
0.0238273770113642));
#11389=CARTESIAN_POINT('Ctrl Pts',(-1.30808717043028,0.48478124421137,0.280929685456974));
#11390=CARTESIAN_POINT('Ctrl Pts',(-1.27980253042162,0.615948260124595,
0.792619532033457));
#11391=CARTESIAN_POINT('Ctrl Pts',(-1.29321476237305,0.626404567290167,
1.05659684088554));
#11392=CARTESIAN_POINT('Ctrl Pts',(-1.38946357811,0.488938846353634,1.53600410055517));
#11393=CARTESIAN_POINT('Ctrl Pts',(-1.46927966447622,0.34423952699714,1.72959611556546));
#11394=CARTESIAN_POINT('Ctrl Pts',(-1.64804633832672,0.0351654638783543,
1.99593663738672));
#11395=CARTESIAN_POINT('Ctrl Pts',(-1.74809047347069,-0.128192913728382,
2.08305283586927));
#11396=CARTESIAN_POINT('Ctrl Pts',(-1.93188952347472,-0.373532157725284,
2.17842710957436));
#11397=CARTESIAN_POINT('Ctrl Pts',(-2.00679552031709,-0.454457191434216,
2.20361434518665));
#11398=CARTESIAN_POINT('Ctrl Pts',(-2.10891108326887,-0.632484078259461,
2.2307813240385));
#11399=CARTESIAN_POINT('Ctrl Pts',(-2.13408587854556,-0.728563548890991,
2.23545023463704));
#11400=CARTESIAN_POINT('Ctrl Pts',(-2.18470343784499,-1.01580120595979,
2.23985105426332));
#11401=CARTESIAN_POINT('Ctrl Pts',(-2.20504953495422,-1.20449005728727,
2.22965055680831));
#11402=CARTESIAN_POINT('Ctrl Pts',(-2.20926209776938,-1.74080899784122,
2.18228791128134));
#11403=CARTESIAN_POINT('Ctrl Pts',(-2.13571406139752,-2.05748394873335,
2.12938063388729));
#11404=CARTESIAN_POINT('Ctrl Pts',(-1.80914039490605,-2.4116424454986,2.07707686166329));
#11405=CARTESIAN_POINT('Ctrl Pts',(-1.58558544675306,-2.52101501223511,
2.06437413078064));
#11406=CARTESIAN_POINT('Ctrl Pts',(-1.06274917012361,-2.63535508293751,
2.05380211046861));
#11407=CARTESIAN_POINT('Ctrl Pts',(-0.765526424774163,-2.63982623851908,
2.05574575179177));
#11408=CARTESIAN_POINT('Ctrl Pts',(-0.201198256641021,-2.55922793898205,
2.06506565863797));
#11409=CARTESIAN_POINT('Ctrl Pts',(0.0660448366282887,-2.47511972447648,
2.07245950804548));
#11410=CARTESIAN_POINT('Ctrl Pts',(0.475148760175511,-2.24745677674094,
2.08564829134537));
#11411=CARTESIAN_POINT('Ctrl Pts',(0.608134614732898,-2.10455710556735,
2.09040062351607));
#11412=CARTESIAN_POINT('Ctrl Pts',(0.692807377742016,-1.84294516771091,
2.09414100985965));
#11413=CARTESIAN_POINT('Ctrl Pts',(0.695288539321058,-1.71667259554446,
2.09510414856687));
#11414=CARTESIAN_POINT('Ctrl Pts',(0.624899286559479,-1.43522068083482,
2.09446462416269));
#11415=CARTESIAN_POINT('Ctrl Pts',(0.555414215357652,-1.2826933626758,2.0935057350151));
#11416=CARTESIAN_POINT('Ctrl Pts',(0.273957080557801,-0.835699802377016,
2.09178023085904));
#11417=CARTESIAN_POINT('Ctrl Pts',(-0.0144466890476935,-0.553079604701429,
2.09136454656141));
#11418=CARTESIAN_POINT('Ctrl Pts',(-0.45094860176887,-0.336574440271572,
2.10878602648762));
#11419=CARTESIAN_POINT('Ctrl Pts',(-0.595413630263608,-0.298852315146673,
2.11776209928019));
#11420=CARTESIAN_POINT('Ctrl Pts',(-0.85098489192329,-0.305627887932605,
2.14353553496541));
#11421=CARTESIAN_POINT('Ctrl Pts',(-0.96192160586922,-0.346842648185032,
2.15984784684465));
#11422=CARTESIAN_POINT('Ctrl Pts',(-1.15250413694999,-0.533505951798014,
2.20558401172234));
#11423=CARTESIAN_POINT('Ctrl Pts',(-1.23266332711506,-0.683289971881234,
2.23568288668276));
#11424=CARTESIAN_POINT('Ctrl Pts',(-1.32515666438693,-1.13327359192835,
2.31428720538256));
#11425=CARTESIAN_POINT('Ctrl Pts',(-1.33679811649895,-1.43203332580916,
2.36251628262105));
#11426=CARTESIAN_POINT('Ctrl Pts',(-1.29844891076763,-1.81475034924797,
2.42060937990806));
#11427=CARTESIAN_POINT('Ctrl Pts',(-2.00000126489276,0.264723298019645,
-0.141143811489164));
#11428=CARTESIAN_POINT('Ctrl Pts',(-1.93751757873767,0.409040857956806,
0.129544654803658));
#11429=CARTESIAN_POINT('Ctrl Pts',(-1.90302169565935,0.501425562421714,
0.367928745114527));
#11430=CARTESIAN_POINT('Ctrl Pts',(-1.88054212115223,0.589499219533149,
0.806948039420934));
#11431=CARTESIAN_POINT('Ctrl Pts',(-1.89355670297749,0.583239799293228,
1.01230148627963));
#11432=CARTESIAN_POINT('Ctrl Pts',(-1.96699692305992,0.455902737146338,
1.36395889494755));
#11433=CARTESIAN_POINT('Ctrl Pts',(-2.02609664009031,0.336426883774145,
1.4995078927604));
#11434=CARTESIAN_POINT('Ctrl Pts',(-2.15596846531113,0.0612442801182847,
1.67285491314019));
#11435=CARTESIAN_POINT('Ctrl Pts',(-2.22783813535845,-0.0940322899337931,
1.71712292179187));
#11436=CARTESIAN_POINT('Ctrl Pts',(-2.33598259475191,-0.33920269686933,
1.73476325774032));
#11437=CARTESIAN_POINT('Ctrl Pts',(-2.37364523276466,-0.423071247215849,
1.72904949400271));
#11438=CARTESIAN_POINT('Ctrl Pts',(-2.43018814721365,-0.596053964829743,
1.72459007815411));
#11439=CARTESIAN_POINT('Ctrl Pts',(-2.44992604374876,-0.685289715308575,
1.72712526048845));
#11440=CARTESIAN_POINT('Ctrl Pts',(-2.49822456222477,-0.958676731041413,
1.73139362094456));
#11441=CARTESIAN_POINT('Ctrl Pts',(-2.51952437158661,-1.14742069861778,
1.72177264812241));
#11442=CARTESIAN_POINT('Ctrl Pts',(-2.52421524419146,-1.71230284911647,
1.67203589473725));
#11443=CARTESIAN_POINT('Ctrl Pts',(-2.45059179936626,-2.09932880466486,
1.60645497054434));
#11444=CARTESIAN_POINT('Ctrl Pts',(-1.98962439178456,-2.61780033767695,
1.53519651937827));
#11445=CARTESIAN_POINT('Ctrl Pts',(-1.70626447510137,-2.75463798845714,
1.52294419434135));
#11446=CARTESIAN_POINT('Ctrl Pts',(-1.09694793499771,-2.90941590356896,
1.5190025028147));
#11447=CARTESIAN_POINT('Ctrl Pts',(-0.766252504594009,-2.92727330542218,
1.52767939121794));
#11448=CARTESIAN_POINT('Ctrl Pts',(-0.128899912590116,-2.86525349144335,
1.55261884723468));
#11449=CARTESIAN_POINT('Ctrl Pts',(0.177538775386479,-2.78640624113666,
1.56852441648561));
#11450=CARTESIAN_POINT('Ctrl Pts',(0.694316196436971,-2.52237373057128,
1.59609027963019));
#11451=CARTESIAN_POINT('Ctrl Pts',(0.916171749283459,-2.32981104713974,
1.610324720381));
#11452=CARTESIAN_POINT('Ctrl Pts',(1.06563235049552,-1.86355969472816,1.61635239083565));
#11453=CARTESIAN_POINT('Ctrl Pts',(1.05129988764842,-1.66506108797555,1.61232780975798));
#11454=CARTESIAN_POINT('Ctrl Pts',(0.941838959229918,-1.29239727476634,
1.60290427183405));
#11455=CARTESIAN_POINT('Ctrl Pts',(0.847111831000521,-1.11349942484178,
1.59617734685152));
#11456=CARTESIAN_POINT('Ctrl Pts',(0.48917696090542,-0.609678328916015,
1.57525998575984));
#11457=CARTESIAN_POINT('Ctrl Pts',(0.152480645331013,-0.315277976557456,
1.560309480123));
#11458=CARTESIAN_POINT('Ctrl Pts',(-0.401131934499451,-0.0719964417188537,
1.57108236464872));
#11459=CARTESIAN_POINT('Ctrl Pts',(-0.595963630740598,-0.0234925921684045,
1.58005022190368));
#11460=CARTESIAN_POINT('Ctrl Pts',(-0.99105980640179,-0.0461787587522702,
1.61625721288154));
#11461=CARTESIAN_POINT('Ctrl Pts',(-1.19161371881466,-0.12598348672354,
1.64472658966789));
#11462=CARTESIAN_POINT('Ctrl Pts',(-1.49417307921139,-0.432526875475132,
1.71573427762991));
#11463=CARTESIAN_POINT('Ctrl Pts',(-1.5948332762173,-0.647477749754412,
1.75642712767188));
#11464=CARTESIAN_POINT('Ctrl Pts',(-1.70167589423767,-1.18783690618816,
1.84803426880073));
#11465=CARTESIAN_POINT('Ctrl Pts',(-1.70977955005583,-1.51716514225989,
1.89970221556995));
#11466=CARTESIAN_POINT('Ctrl Pts',(-1.66752387161256,-1.92309305756368,
1.96012536190953));
#11467=CARTESIAN_POINT('Ctrl Pts',(-2.58520620102617,0.327022223530482,
-0.0242933660241372));
#11468=CARTESIAN_POINT('Ctrl Pts',(-2.52720813216107,0.450085931081367,
0.235261932595972));
#11469=CARTESIAN_POINT('Ctrl Pts',(-2.49795622088845,0.518069880632045,
0.454927804771985));
#11470=CARTESIAN_POINT('Ctrl Pts',(-2.48128171188284,0.563050178941749,
0.821276546808376));
#11471=CARTESIAN_POINT('Ctrl Pts',(-2.49389864358197,0.540075031296315,
0.968006131673827));
#11472=CARTESIAN_POINT('Ctrl Pts',(-2.54453026800985,0.422866627938986,
1.19191368933997));
#11473=CARTESIAN_POINT('Ctrl Pts',(-2.58291361570442,0.32861424055116,1.26941966995528));
#11474=CARTESIAN_POINT('Ctrl Pts',(-2.66389059229556,0.0873230963582133,
1.34977318889387));
#11475=CARTESIAN_POINT('Ctrl Pts',(-2.70758579724625,-0.0598716661391885,
1.35119300771448));
#11476=CARTESIAN_POINT('Ctrl Pts',(-2.74007566602911,-0.304873236013411,
1.29109940590619));
#11477=CARTESIAN_POINT('Ctrl Pts',(-2.74049494521224,-0.391685302997432,
1.25448464281861));
#11478=CARTESIAN_POINT('Ctrl Pts',(-2.75146521115844,-0.559623851400008,
1.21839883226965));
#11479=CARTESIAN_POINT('Ctrl Pts',(-2.76576620895198,-0.642015881726228,
1.21880028633987));
#11480=CARTESIAN_POINT('Ctrl Pts',(-2.81174568660457,-0.901552256123071,
1.22293618762564));
#11481=CARTESIAN_POINT('Ctrl Pts',(-2.83399920821904,-1.09035133994834,
1.21389473943648));
#11482=CARTESIAN_POINT('Ctrl Pts',(-2.83916839061358,-1.68379670039174,
1.16178387819315));
#11483=CARTESIAN_POINT('Ctrl Pts',(-2.76546953733502,-2.14117366059643,
1.08352930720148));
#11484=CARTESIAN_POINT('Ctrl Pts',(-2.17010838866312,-2.82395822985523,
0.99331617709322));
#11485=CARTESIAN_POINT('Ctrl Pts',(-1.8269435034497,-2.98826096467916,0.981514257902072));
#11486=CARTESIAN_POINT('Ctrl Pts',(-1.13114669987181,-3.18347672420042,
0.984202895160761));
#11487=CARTESIAN_POINT('Ctrl Pts',(-0.766978584413879,-3.21472037232524,
0.99961303064418));
#11488=CARTESIAN_POINT('Ctrl Pts',(-0.0566015685392616,-3.1712790439046,
1.04017203583152));
#11489=CARTESIAN_POINT('Ctrl Pts',(0.289032714144647,-3.09769275779683,
1.0645893249258));
#11490=CARTESIAN_POINT('Ctrl Pts',(0.913483632698393,-2.79729068440162,
1.10653226791493));
#11491=CARTESIAN_POINT('Ctrl Pts',(1.22420888383399,-2.55506498871208,1.13024881724595));
#11492=CARTESIAN_POINT('Ctrl Pts',(1.43845732324901,-1.88417422174541,1.13856377181168));
#11493=CARTESIAN_POINT('Ctrl Pts',(1.40731123597572,-1.61344958040663,1.12955147094911));
#11494=CARTESIAN_POINT('Ctrl Pts',(1.25877863190032,-1.14957386869789,1.11134391950535));
#11495=CARTESIAN_POINT('Ctrl Pts',(1.13880944664334,-0.944305487007855,
1.09884895868796));
#11496=CARTESIAN_POINT('Ctrl Pts',(0.704396841252997,-0.383656855455022,
1.05873974066059));
#11497=CARTESIAN_POINT('Ctrl Pts',(0.3194079797097,-0.0774763484135167,
1.02925441368461));
#11498=CARTESIAN_POINT('Ctrl Pts',(-0.351315267230051,0.19258155683384,
1.03337870280986));
#11499=CARTESIAN_POINT('Ctrl Pts',(-0.596513631217612,0.251867130809852,
1.0423383445272));
#11500=CARTESIAN_POINT('Ctrl Pts',(-1.13113472088033,0.213270370428087,
1.08897889079772));
#11501=CARTESIAN_POINT('Ctrl Pts',(-1.42130583176012,0.0948756747378918,
1.12960533249102));
#11502=CARTESIAN_POINT('Ctrl Pts',(-1.83584202147282,-0.331547799152291,
1.22588454353743));
#11503=CARTESIAN_POINT('Ctrl Pts',(-1.95700322531958,-0.611665527627663,
1.277171368661));
#11504=CARTESIAN_POINT('Ctrl Pts',(-2.07819512408842,-1.242400220448,1.38178133221873));
#11505=CARTESIAN_POINT('Ctrl Pts',(-2.08276098361269,-1.6022969587106,1.43688814851895));
#11506=CARTESIAN_POINT('Ctrl Pts',(-2.03659883245755,-2.03143576587941,
1.49964134391094));
#11507=CARTESIAN_POINT('Ctrl Pts',(-2.58520628884668,-0.202429814804338,
0.257984049124923));
#11508=CARTESIAN_POINT('Ctrl Pts',(-2.52287003021952,-0.0991605925537074,
0.48041189381135));
#11509=CARTESIAN_POINT('Ctrl Pts',(-2.49069713797941,-0.0547752060290418,
0.650390938733111));
#11510=CARTESIAN_POINT('Ctrl Pts',(-2.45901975307171,-0.0405967151270361,
0.860323812136826));
#11511=CARTESIAN_POINT('Ctrl Pts',(-2.45755776601418,-0.0668772768837554,
0.890888701795052));
#11512=CARTESIAN_POINT('Ctrl Pts',(-2.43814972704647,-0.0997101264501223,
0.889828411549012));
#11513=CARTESIAN_POINT('Ctrl Pts',(-2.42322436247891,-0.109485358511338,
0.880041033565627));
#11514=CARTESIAN_POINT('Ctrl Pts',(-2.39625766944769,-0.209667337073921,
0.892370624522099));
#11515=CARTESIAN_POINT('Ctrl Pts',(-2.38312298955208,-0.301090693054413,
0.900119763459602));
#11516=CARTESIAN_POINT('Ctrl Pts',(-2.32301076703839,-0.484396978702216,
0.896687786586603));
#11517=CARTESIAN_POINT('Ctrl Pts',(-2.2882208769662,-0.554099346897494,
0.893755324967696));
#11518=CARTESIAN_POINT('Ctrl Pts',(-2.26024650082642,-0.688025321619785,
0.897037457090494));
#11519=CARTESIAN_POINT('Ctrl Pts',(-2.26909685245436,-0.753271393542086,
0.90056283633815));
#11520=CARTESIAN_POINT('Ctrl Pts',(-2.30562038065636,-0.958868133830514,
0.903741395119929));
#11521=CARTESIAN_POINT('Ctrl Pts',(-2.32345605900597,-1.11054614021518,
0.896323357424417));
#11522=CARTESIAN_POINT('Ctrl Pts',(-2.32766903008263,-1.57324447167574,
0.855513659745901));
#11523=CARTESIAN_POINT('Ctrl Pts',(-2.26534134624811,-1.89313706735396,
0.802550146205944));
#11524=CARTESIAN_POINT('Ctrl Pts',(-1.8784097009876,-2.34623302779759,0.737850016479276));
#11525=CARTESIAN_POINT('Ctrl Pts',(-1.62856420025181,-2.47940372964513,
0.723656709579273));
#11526=CARTESIAN_POINT('Ctrl Pts',(-1.0677159752808,-2.64815885225886,0.711821011413811));
#11527=CARTESIAN_POINT('Ctrl Pts',(-0.754654442434687,-2.68423961890214,
0.7143656987144));
#11528=CARTESIAN_POINT('Ctrl Pts',(-0.146547655379389,-2.66387954969245,
0.728109209430922));
#11529=CARTESIAN_POINT('Ctrl Pts',(0.148360185492318,-2.60647744552693,
0.739290473004851));
#11530=CARTESIAN_POINT('Ctrl Pts',(0.630407318327205,-2.38898663042632,
0.760041102206871));
#11531=CARTESIAN_POINT('Ctrl Pts',(0.826421854426146,-2.22824278895934,
0.770653093691493));
#11532=CARTESIAN_POINT('Ctrl Pts',(0.944626927682175,-1.85585057919288,
0.775558178553095));
#11533=CARTESIAN_POINT('Ctrl Pts',(0.925034692722124,-1.68883328142547,
0.773222476225436));
#11534=CARTESIAN_POINT('Ctrl Pts',(0.811065913099062,-1.36506222450943,
0.767306282372666));
#11535=CARTESIAN_POINT('Ctrl Pts',(0.713303855474414,-1.20565623956688,
0.763081995675995));
#11536=CARTESIAN_POINT('Ctrl Pts',(0.34282900880003,-0.763013140860391,
0.752549842977497));
#11537=CARTESIAN_POINT('Ctrl Pts',(-0.00364320811200702,-0.51409270041443,
0.749182852233819));
#11538=CARTESIAN_POINT('Ctrl Pts',(-0.51978409527715,-0.322125645865647,
0.768702071980997));
#11539=CARTESIAN_POINT('Ctrl Pts',(-0.692921619426966,-0.288496673462745,
0.779141999853542));
#11540=CARTESIAN_POINT('Ctrl Pts',(-1.02265615110868,-0.318050712715351,
0.812410654246396));
#11541=CARTESIAN_POINT('Ctrl Pts',(-1.17942291671907,-0.38451642598792,
0.835724403097336));
#11542=CARTESIAN_POINT('Ctrl Pts',(-1.42433925564296,-0.641664631057489,
0.895455616106331));
#11543=CARTESIAN_POINT('Ctrl Pts',(-1.51197566296117,-0.828011441539482,
0.931198033441523));
#11544=CARTESIAN_POINT('Ctrl Pts',(-1.60515675444377,-1.32815869991775,
1.016496711423));
#11545=CARTESIAN_POINT('Ctrl Pts',(-1.61139422048387,-1.6433989280412,1.06632932813794));
#11546=CARTESIAN_POINT('Ctrl Pts',(-1.5676596498637,-2.03832577625144,1.12541070542012));
#11547=CARTESIAN_POINT('Ctrl Pts',(-2.00000135271328,-0.264728740315192,
0.141133603659935));
#11548=CARTESIAN_POINT('Ctrl Pts',(-1.93317947679614,-0.140205665678286,
0.374694616019038));
#11549=CARTESIAN_POINT('Ctrl Pts',(-1.89576261275035,-0.0714195242393531,
0.563391879075593));
#11550=CARTESIAN_POINT('Ctrl Pts',(-1.85828016234107,-0.0141476745355931,
0.845995304749381));
#11551=CARTESIAN_POINT('Ctrl Pts',(-1.85721582540971,-0.0237125088868792,
0.935184056400945));
#11552=CARTESIAN_POINT('Ctrl Pts',(-1.86061638209651,-0.0666740172427863,
1.06187361715673));
#11553=CARTESIAN_POINT('Ctrl Pts',(-1.86640738686477,-0.101672715288381,
1.11012925637074));
#11554=CARTESIAN_POINT('Ctrl Pts',(-1.88833554246329,-0.235746153313808,
1.21545234876845));
#11555=CARTESIAN_POINT('Ctrl Pts',(-1.9033753276643,-0.335251316849042,
1.26604967753693));
#11556=CARTESIAN_POINT('Ctrl Pts',(-1.9189176957612,-0.518726439558199,
1.34035163842065));
#11557=CARTESIAN_POINT('Ctrl Pts',(-1.92137116451861,-0.585485291115871,
1.36832017615168));
#11558=CARTESIAN_POINT('Ctrl Pts',(-1.93896943688162,-0.724455435049461,
1.40322870297494));
#11559=CARTESIAN_POINT('Ctrl Pts',(-1.95325668725115,-0.796545227124419,
1.40888781048668));
#11560=CARTESIAN_POINT('Ctrl Pts',(-1.99209925627655,-1.01599260874888,
1.41219882843878));
#11561=CARTESIAN_POINT('Ctrl Pts',(-2.00898122237353,-1.16761549888469,
1.40420126611032));
#11562=CARTESIAN_POINT('Ctrl Pts',(-2.01271588366055,-1.60175062040053,
1.36576567629003));
#11563=CARTESIAN_POINT('Ctrl Pts',(-1.95046360827934,-1.85129221142242,
1.32547580954877));
#11564=CARTESIAN_POINT('Ctrl Pts',(-1.69792570410908,-2.14007513561928,
1.27973035876422));
#11565=CARTESIAN_POINT('Ctrl Pts',(-1.50788517190343,-2.24578075342313,
1.26508664601861));
#11566=CARTESIAN_POINT('Ctrl Pts',(-1.03351721040672,-2.37409803162741,
1.24662061906772));
#11567=CARTESIAN_POINT('Ctrl Pts',(-0.753928362614793,-2.39679255199907,
1.24243205928811));
#11568=CARTESIAN_POINT('Ctrl Pts',(-0.218845999430284,-2.35785399723118,
1.24055602083421));
#11569=CARTESIAN_POINT('Ctrl Pts',(0.0368662467341799,-2.29519092886669,
1.24322556456469));
#11570=CARTESIAN_POINT('Ctrl Pts',(0.411239882065782,-2.11406967659605,
1.2495991139221));
#11571=CARTESIAN_POINT('Ctrl Pts',(0.518384719875618,-2.00298884738698,
1.25072899682664));
#11572=CARTESIAN_POINT('Ctrl Pts',(0.571801954928687,-1.83523605217566,
1.25334679757698));
#11573=CARTESIAN_POINT('Ctrl Pts',(0.569023344394799,-1.74044478899434,
1.25599881503435));
#11574=CARTESIAN_POINT('Ctrl Pts',(0.494126240428662,-1.50788563057796,
1.25886663470126));
#11575=CARTESIAN_POINT('Ctrl Pts',(0.421606239831573,-1.37485017740085,
1.26041038383949));
#11576=CARTESIAN_POINT('Ctrl Pts',(0.127609128452456,-0.989034614321357,
1.26907008807672));
#11577=CARTESIAN_POINT('Ctrl Pts',(-0.170570542490676,-0.751894328558357,
1.28023791867232));
#11578=CARTESIAN_POINT('Ctrl Pts',(-0.569600762546571,-0.586703644418381,
1.30640573381989));
#11579=CARTESIAN_POINT('Ctrl Pts',(-0.692371618949951,-0.563856396440986,
1.31685387723007));
#11580=CARTESIAN_POINT('Ctrl Pts',(-0.882581236630141,-0.577499841895708,
1.33968897633028));
#11581=CARTESIAN_POINT('Ctrl Pts',(-0.949730803773584,-0.6053755874494,
1.35084566027416));
#11582=CARTESIAN_POINT('Ctrl Pts',(-1.08267031338154,-0.742643707380371,
1.38530535019886));
#11583=CARTESIAN_POINT('Ctrl Pts',(-1.14980571385887,-0.863823663666268,
1.41045379245241));
#11584=CARTESIAN_POINT('Ctrl Pts',(-1.22863752459304,-1.27359538565792,
1.48274964800499));
#11585=CARTESIAN_POINT('Ctrl Pts',(-1.23841278692706,-1.55826711159036,
1.52914339518866));
#11586=CARTESIAN_POINT('Ctrl Pts',(-1.19858468901873,-1.92998306793573,
1.58589472341859));
#11587=CARTESIAN_POINT('Origin',(-2.,-2.08166817117217E-14,-3.46944695195361E-14));
#11588=CARTESIAN_POINT('Origin',(-1.43305428031565,-1.92653806274973,1.77301004266414));
#11589=CARTESIAN_POINT('Origin',(-1.43305428031565,-1.92653806274973,1.77301004266414));
#11590=CARTESIAN_POINT('Origin',(-2.,-2.08166817117217E-14,-3.46944695195361E-14));
#11591=CARTESIAN_POINT('Origin',(-1.99999999999999,40.0000000000001,-6.24500451351651E-14));
#11592=CARTESIAN_POINT('Origin',(-1.99999999999999,40.0000000000001,-6.24500451351651E-14));
#11593=CARTESIAN_POINT('Ctrl Pts',(-2.00000000001811,42.8890026416775,-1.69451425055562));
#11594=CARTESIAN_POINT('Ctrl Pts',(-2.00000000001811,42.7138340471106,-1.69451425055564));
#11595=CARTESIAN_POINT('Ctrl Pts',(-2.00000000001811,42.5195868694293,-1.69664685121079));
#11596=CARTESIAN_POINT('Ctrl Pts',(-2.00000000001818,42.1727041659024,-1.69763022720131));
#11597=CARTESIAN_POINT('Ctrl Pts',(-2.00000000001809,42.0075453806213,-1.69643582812033));
#11598=CARTESIAN_POINT('Ctrl Pts',(-2.000000000018,41.5447432182596,-1.67506238348623));
#11599=CARTESIAN_POINT('Ctrl Pts',(-2.00000000001759,41.2824586218001,-1.63529714422004));
#11600=CARTESIAN_POINT('Ctrl Pts',(-2.00000000001559,40.8726877368524,-1.45751662005935));
#11601=CARTESIAN_POINT('Ctrl Pts',(-2.00000000001428,40.7146168625301,-1.32576584773803));
#11602=CARTESIAN_POINT('Ctrl Pts',(-2.00000000000915,40.4347106414413,-0.836444527344903));
#11603=CARTESIAN_POINT('Ctrl Pts',(-2.00000000000487,40.3213171458309,-0.475216515464907));
#11604=CARTESIAN_POINT('Ctrl Pts',(-2.,40.247426591683,0.0357782298078951));
#11605=CARTESIAN_POINT('Ctrl Pts',(-1.50000000001812,42.8890026416775,-1.69451425056007));
#11606=CARTESIAN_POINT('Ctrl Pts',(-1.50000000001811,42.7138340471107,-1.6945142505601));
#11607=CARTESIAN_POINT('Ctrl Pts',(-1.50000000001814,42.5195868694296,-1.69664685121553));
#11608=CARTESIAN_POINT('Ctrl Pts',(-1.50000000001815,42.1727041659021,-1.69763022720547));
#11609=CARTESIAN_POINT('Ctrl Pts',(-1.50000000001812,42.0075453806213,-1.69643582812505));
#11610=CARTESIAN_POINT('Ctrl Pts',(-1.50000000001802,41.5447432182596,-1.6750623834901));
#11611=CARTESIAN_POINT('Ctrl Pts',(-1.50000000001758,41.2824586218004,-1.635297144225));
#11612=CARTESIAN_POINT('Ctrl Pts',(-1.50000000001562,40.8726877368527,-1.45751662006339));
#11613=CARTESIAN_POINT('Ctrl Pts',(-1.50000000001431,40.7146168625313,-1.32576584774273));
#11614=CARTESIAN_POINT('Ctrl Pts',(-1.50000000000914,40.4347106414414,-0.836444527349893));
#11615=CARTESIAN_POINT('Ctrl Pts',(-1.50000000000502,40.321317145827,-0.475216515469928));
#11616=CARTESIAN_POINT('Ctrl Pts',(-1.5,40.2474265916837,0.0357782298028141));
#11617=CARTESIAN_POINT('Ctrl Pts',(-1.50000000002261,42.8890026416775,-2.19451425056016));
#11618=CARTESIAN_POINT('Ctrl Pts',(-1.5000000000226,42.6924352393214,-2.19451425056018));
#11619=CARTESIAN_POINT('Ctrl Pts',(-1.50000000002262,42.5242279803483,-2.196635703513));
#11620=CARTESIAN_POINT('Ctrl Pts',(-1.50000000002264,42.1708979670303,-2.19763735653693));
#11621=CARTESIAN_POINT('Ctrl Pts',(-1.50000000002256,41.9983311272475,-2.19654321697105));
#11622=CARTESIAN_POINT('Ctrl Pts',(-1.50000000002256,41.4939715199041,-2.1732505327887));
#11623=CARTESIAN_POINT('Ctrl Pts',(-1.50000000002207,41.1721096008011,-2.1324514159462));
#11624=CARTESIAN_POINT('Ctrl Pts',(-1.50000000001927,40.5850276451855,-1.87774381002253));
#11625=CARTESIAN_POINT('Ctrl Pts',(-1.50000000001706,40.3267157332556,-1.65463617720806));
#11626=CARTESIAN_POINT('Ctrl Pts',(-1.50000000001012,39.9545934323558,-1.00410633608771));
#11627=CARTESIAN_POINT('Ctrl Pts',(-1.50000000000546,39.831903366932,-0.584389540167537));
#11628=CARTESIAN_POINT('Ctrl Pts',(-1.50000000000002,39.752573408318,-0.0357782298130924));
#11629=CARTESIAN_POINT('Ctrl Pts',(-2.00000000002259,42.8890026416775,-2.19451425055564));
#11630=CARTESIAN_POINT('Ctrl Pts',(-2.0000000000226,42.6924352393214,-2.19451425055565));
#11631=CARTESIAN_POINT('Ctrl Pts',(-2.00000000002263,42.5242279803487,-2.19663570350848));
#11632=CARTESIAN_POINT('Ctrl Pts',(-2.00000000002263,42.17089796703,-2.19763735653241));
#11633=CARTESIAN_POINT('Ctrl Pts',(-2.00000000002255,41.9983311272475,-2.19654321696658));
#11634=CARTESIAN_POINT('Ctrl Pts',(-2.00000000002255,41.4939715199041,-2.17325053278423));
#11635=CARTESIAN_POINT('Ctrl Pts',(-2.00000000002206,41.1721096008009,-2.13245141594075));
#11636=CARTESIAN_POINT('Ctrl Pts',(-2.00000000001923,40.5850276451852,-1.87774381001891));
#11637=CARTESIAN_POINT('Ctrl Pts',(-2.00000000001706,40.3267157332544,-1.65463617720347));
#11638=CARTESIAN_POINT('Ctrl Pts',(-2.00000000001007,39.9545934323557,-1.0041063360826));
#11639=CARTESIAN_POINT('Ctrl Pts',(-2.00000000000546,39.8319033669359,-0.58438954016253));
#11640=CARTESIAN_POINT('Ctrl Pts',(-2.,39.7525734083173,-0.03577822980802));
#11641=CARTESIAN_POINT('Ctrl Pts',(-2.50000000002261,42.8890026416775,-2.19451425055115));
#11642=CARTESIAN_POINT('Ctrl Pts',(-2.5000000000226,42.6924352393213,-2.19451425055115));
#11643=CARTESIAN_POINT('Ctrl Pts',(-2.50000000002264,42.524227980349,-2.19663570350397));
#11644=CARTESIAN_POINT('Ctrl Pts',(-2.50000000002262,42.1708979670296,-2.19763735652791));
#11645=CARTESIAN_POINT('Ctrl Pts',(-2.50000000002255,41.9983311272475,-2.19654321696204));
#11646=CARTESIAN_POINT('Ctrl Pts',(-2.50000000002259,41.493971519904,-2.17325053277969));
#11647=CARTESIAN_POINT('Ctrl Pts',(-2.5000000000221,41.1721096008005,-2.13245141593522));
#11648=CARTESIAN_POINT('Ctrl Pts',(-2.50000000001924,40.5850276451849,-1.87774381001523));
#11649=CARTESIAN_POINT('Ctrl Pts',(-2.50000000001709,40.3267157332532,-1.65463617719887));
#11650=CARTESIAN_POINT('Ctrl Pts',(-2.50000000001009,39.9545934323556,-1.00410633607742));
#11651=CARTESIAN_POINT('Ctrl Pts',(-2.50000000000545,39.8319033669398,-0.584389540157467));
#11652=CARTESIAN_POINT('Ctrl Pts',(-2.50000000000002,39.7525734083165,-0.0357782298028245));
#11653=CARTESIAN_POINT('Ctrl Pts',(-2.50000000001813,42.8890026416775,-1.69451425055113));
#11654=CARTESIAN_POINT('Ctrl Pts',(-2.50000000001811,42.7138340471106,-1.69451425055112));
#11655=CARTESIAN_POINT('Ctrl Pts',(-2.50000000001808,42.519586869429,-1.69664685120596));
#11656=CARTESIAN_POINT('Ctrl Pts',(-2.50000000001821,42.1727041659027,-1.6976302271971));
#11657=CARTESIAN_POINT('Ctrl Pts',(-2.50000000001814,42.0075453806212,-1.69643582811551));
#11658=CARTESIAN_POINT('Ctrl Pts',(-2.50000000001799,41.5447432182596,-1.67506238348225));
#11659=CARTESIAN_POINT('Ctrl Pts',(-2.50000000001761,41.2824586217998,-1.63529714421497));
#11660=CARTESIAN_POINT('Ctrl Pts',(-2.5000000000156,40.872687736852,-1.45751662005523));
#11661=CARTESIAN_POINT('Ctrl Pts',(-2.50000000001424,40.7146168625289,-1.32576584773326));
#11662=CARTESIAN_POINT('Ctrl Pts',(-2.50000000000921,40.4347106414412,-0.836444527339844));
#11663=CARTESIAN_POINT('Ctrl Pts',(-2.50000000000473,40.3213171458348,-0.475216515459863));
#11664=CARTESIAN_POINT('Ctrl Pts',(-2.5,40.2474265916822,0.0357782298130767));
#11665=CARTESIAN_POINT('Ctrl Pts',(-2.00000000001811,42.8890026416775,-1.69451425055562));
#11666=CARTESIAN_POINT('Ctrl Pts',(-2.00000000001811,42.7138340471106,-1.69451425055564));
#11667=CARTESIAN_POINT('Ctrl Pts',(-2.00000000001811,42.5195868694293,-1.69664685121079));
#11668=CARTESIAN_POINT('Ctrl Pts',(-2.00000000001818,42.1727041659024,-1.69763022720131));
#11669=CARTESIAN_POINT('Ctrl Pts',(-2.00000000001809,42.0075453806213,-1.69643582812033));
#11670=CARTESIAN_POINT('Ctrl Pts',(-2.000000000018,41.5447432182596,-1.67506238348623));
#11671=CARTESIAN_POINT('Ctrl Pts',(-2.00000000001759,41.2824586218001,-1.63529714422004));
#11672=CARTESIAN_POINT('Ctrl Pts',(-2.00000000001559,40.8726877368524,-1.45751662005935));
#11673=CARTESIAN_POINT('Ctrl Pts',(-2.00000000001428,40.7146168625301,-1.32576584773803));
#11674=CARTESIAN_POINT('Ctrl Pts',(-2.00000000000915,40.4347106414413,-0.836444527344903));
#11675=CARTESIAN_POINT('Ctrl Pts',(-2.00000000000487,40.3213171458309,-0.475216515464907));
#11676=CARTESIAN_POINT('Ctrl Pts',(-2.,40.247426591683,0.0357782298078951));
#11677=CARTESIAN_POINT('Origin',(-2.0000000000128,41.3499760178345,-1.22177579428992));
#12118=UNCERTAINTY_MEASURE_WITH_UNIT(LENGTH_MEASURE(0.01),#12138,
'DISTANCE_ACCURACY_VALUE',
'Maximum model space distance between geometric entities at asserted c
onnectivities');
#12123=UNCERTAINTY_MEASURE_WITH_UNIT(LENGTH_MEASURE(0.01),#12138,
'DISTANCE_ACCURACY_VALUE',
'Maximum model space distance between geometric entities at asserted c
onnectivities');
#12132=(
GEOMETRIC_REPRESENTATION_CONTEXT(3)
GLOBAL_UNCERTAINTY_ASSIGNED_CONTEXT((#12118))
GLOBAL_UNIT_ASSIGNED_CONTEXT((#12138,#12140,#12141))
REPRESENTATION_CONTEXT('','3D')
);
#12137=(
GEOMETRIC_REPRESENTATION_CONTEXT(3)
GLOBAL_UNCERTAINTY_ASSIGNED_CONTEXT((#12123))
GLOBAL_UNIT_ASSIGNED_CONTEXT((#12138,#12140,#12141))
REPRESENTATION_CONTEXT('','3D')
);
#12138=(
LENGTH_UNIT()
NAMED_UNIT(*)
SI_UNIT(.MILLI.,.METRE.)
);
#12140=(
NAMED_UNIT(*)
PLANE_ANGLE_UNIT()
SI_UNIT($,.RADIAN.)
);
#12141=(
NAMED_UNIT(*)
SI_UNIT($,.STERADIAN.)
SOLID_ANGLE_UNIT()
);
#12150=SHAPE_DEFINITION_REPRESENTATION(#12166,#12191);
#12166=PRODUCT_DEFINITION_SHAPE('',$,#12205);
#12191=SHAPE_REPRESENTATION('',(#2049),#12132);
#12196=PRODUCT_DEFINITION_CONTEXT('part definition',#12237,'design');
#12205=PRODUCT_DEFINITION('Corkscrew','Corkscrew',#12218,#12196);
#12218=PRODUCT_DEFINITION_FORMATION('',$,#12247);
#12237=APPLICATION_CONTEXT(
'Core Data for Automotive Mechanical Design Process');
#12238=PRODUCT_CONTEXT('part definition',#12237,'mechanical');
#12247=PRODUCT('Corkscrew','Corkscrew',$,(#12238));
#12253=PRESENTATION_STYLE_ASSIGNMENT((#12255));
#12255=SURFACE_STYLE_USAGE(.BOTH.,#12257);
#12257=SURFACE_SIDE_STYLE('',(#12259));
#12259=SURFACE_STYLE_FILL_AREA(#12261);
#12261=FILL_AREA_STYLE('Opaque(23,69,131)',(#12263));
#12263=FILL_AREA_STYLE_COLOUR('Opaque(23,69,131)',#12265);
#12265=COLOUR_RGB('Opaque(23,69,131)',0.0901960784313725,0.270588235294118,
0.513725490196078);
ENDSEC;
END-ISO-10303-21;
